ISO-10303-21;
HEADER;
FILE_DESCRIPTION (('STEP AP214'),
    '1' );
FILE_NAME ('Spring.step',
    '2026-10-07T19:06:49',
    ( '' ),
    ( '' ),
    'SwSTEP 2.0',
    'SolidWorks 2020',
    '' );
FILE_SCHEMA (( 'AUTOMOTIVE_DESIGN' ));
ENDSEC;

DATA;
#6=EDGE_CURVE ( 'NONE', #36712, #34390, #42931, .T. ) ;
#24=CARTESIAN_POINT ( 'NONE',  ( -2.375816180258031540, -86.25171435493598437, 3.206979491546134931 ) ) ;
#60=CARTESIAN_POINT ( 'NONE',  ( 3.757989199629864441, -86.07389998728977787, 2.729540522068179875 ) ) ;
#63=CARTESIAN_POINT ( 'NONE',  ( 1.978576907476575553, -78.62148120184446043, -3.425895241845613892 ) ) ;
#75=CARTESIAN_POINT ( 'NONE',  ( -4.006190210801564788, -78.54828561723800817, 2.263637798799203349 ) ) ;
#117=CARTESIAN_POINT ( 'NONE',  ( 2.039467698388000017, -84.90729426542299052, -3.154669836245999726 ) ) ;
#145=CARTESIAN_POINT ( 'NONE',  ( 2.284785568762000008, -82.74324735065199832, 3.494178859388000102 ) ) ;
#171=EDGE_CURVE ( 'NONE', #313, #521, #53642, .T. ) ;
#181=CARTESIAN_POINT ( 'NONE',  ( -3.368292805027000014, -80.61420806598900413, -1.663121790705999858 ) ) ;
#191=CARTESIAN_POINT ( 'NONE',  ( -1.569340319482204205, -86.39318692756697260, -3.437241610844480988 ) ) ;
#199=CARTESIAN_POINT ( 'NONE',  ( 3.909622331879000434, -81.21546018839499936, -0.6487244410423000929 ) ) ;
#203=CARTESIAN_POINT ( 'NONE',  ( 0.7883518021343000060, -81.29032046129098887, 3.458764816093999883 ) ) ;
#225=CARTESIAN_POINT ( 'NONE',  ( 3.634969262962000069, -85.51626360600299392, 2.053437490576000446 ) ) ;
#229=EDGE_LOOP ( 'NONE', ( #45666, #3172, #6374, #35575 ) ) ;
#247=CARTESIAN_POINT ( 'NONE',  ( 3.992904449609000483, -78.77851881763733388, -2.356505974700060513 ) ) ;
#260=CARTESIAN_POINT ( 'NONE',  ( 0.8807115773125999691, -80.96678455456799384, 3.863978249925000164 ) ) ;
#266=CARTESIAN_POINT ( 'NONE',  ( 1.862898869916999933, -85.71183183321298316, 3.018969991366999839 ) ) ;
#284=CARTESIAN_POINT ( 'NONE',  ( 3.273752395723000586, -82.55440783550699280, -1.206381456434000077 ) ) ;
#288=CARTESIAN_POINT ( 'NONE',  ( -2.857465951524460479, -84.55833334385054911, 1.921468474764645995 ) ) ;
#313=VERTEX_POINT ( 'NONE', #37790 ) ;
#322=CARTESIAN_POINT ( 'NONE',  ( -3.677663026309978989, -86.17851881763699851, 1.555017880481419423 ) ) ;
#325=CARTESIAN_POINT ( 'NONE',  ( 1.131620348041424196, -79.14322915056125396, -3.849499586317910449 ) ) ;
#352=CARTESIAN_POINT ( 'NONE',  ( 3.647699722740942452, -86.02148118236289065, -1.624060551956035381 ) ) ;
#357=CARTESIAN_POINT ( 'NONE',  ( 3.485499217011998940, -78.48547957940618858, -2.057048905967550745 ) ) ;
#367=CARTESIAN_POINT ( 'NONE',  ( -2.309340847114626616, -78.43735716284257364, 3.830055409267042688 ) ) ;
#408=CARTESIAN_POINT ( 'NONE',  ( 3.473823996146999882, -83.70093064074599454, -0.9034887262636999150 ) ) ;
#438=CARTESIAN_POINT ( 'NONE',  ( -3.903103493260999812, -86.12136169985498668, 1.102340964906999954 ) ) ;
#464=CARTESIAN_POINT ( 'NONE',  ( -0.3695879074652637097, -80.54999998998307831, -3.516391212123742616 ) ) ;
#466=CARTESIAN_POINT ( 'NONE',  ( 0.7977265213099999919, -81.45982051858098316, 3.499625350527999945 ) ) ;
#475=CARTESIAN_POINT ( 'NONE',  ( 3.620209227049934420, -86.25171438276198899, -1.611820994701147480 ) ) ;
#482=CARTESIAN_POINT ( 'NONE',  ( 1.620852308002999953, -80.65768892718899963, -3.844855067022000306 ) ) ;
#486=CARTESIAN_POINT ( 'NONE',  ( -3.412705351263000342, -78.68490379462421913, 0.4935355394736000156 ) ) ;
#511=CARTESIAN_POINT ( 'NONE',  ( 3.297963199104999799, -82.02128429901999596, -1.885709654497000010 ) ) ;
#519=CARTESIAN_POINT ( 'NONE',  ( -3.992904449609034678, -78.77851881763731967, 7.985808899218018730 ) ) ;
#521=VERTEX_POINT ( 'NONE', #12372 ) ;
#540=CARTESIAN_POINT ( 'NONE',  ( 3.999999999999675815, -78.69999999999997442, -1.477225460011499791E-15 ) ) ;
#554=CARTESIAN_POINT ( 'NONE',  ( -2.970001969328999625, -81.56803455456798702, -2.623941025421000273 ) ) ;
#576=CARTESIAN_POINT ( 'NONE',  ( 3.640440263105999552, -84.31421544543098889, 0.9265833904223998996 ) ) ;
#580=CARTESIAN_POINT ( 'NONE',  ( 1.992291055985653481, -85.67604167370414814, 2.768826960839078311 ) ) ;
#641=CARTESIAN_POINT ( 'NONE',  ( -0.4871519710315541096, -86.07390000031791999, 3.917790784211977240 ) ) ;
#644=CARTESIAN_POINT ( 'NONE',  ( -2.171318179221914058, -78.40681307385639798, -3.601143365367586835 ) ) ;
#655=CARTESIAN_POINT ( 'NONE',  ( -2.089807114238836583, -78.48547957940617437, 3.465957419068643297 ) ) ;
#698=CARTESIAN_POINT ( 'NONE',  ( 1.964355310900000262, -82.49842648807799605, 3.004164177009000181 ) ) ;
#711=CARTESIAN_POINT ( 'NONE',  ( -6.019522479259990178, -85.88547957940599531, -4.950643703664905360 ) ) ;
#725=CARTESIAN_POINT ( 'NONE',  ( -3.976098536387000060, -86.16144503318800218, 0.4347513405908999817 ) ) ;
#751=CARTESIAN_POINT ( 'NONE',  ( 3.425474844296876764, -80.97395832166205309, 0.3498287032621968939 ) ) ;
#771=CARTESIAN_POINT ( 'NONE',  ( 2.775756403448000231, -81.13869062511399477, 3.115324875632000001 ) ) ;
#796=CARTESIAN_POINT ( 'NONE',  ( -4.092573046463000352, -82.97942814914499365, 0.5562009154790999998 ) ) ;
#838=CARTESIAN_POINT ( 'NONE',  ( 2.359552285272000116, -78.92253455456848599, -3.184099749658000356 ) ) ;
#859=CARTESIAN_POINT ( 'NONE',  ( -3.348285028641999617, -83.47632450217398059, -1.293338634809000132 ) ) ;
#862=CARTESIAN_POINT ( 'NONE',  ( 0.8812128323519314854, -85.13645834205065910, -3.328407071930476580 ) ) ;
#896=CARTESIAN_POINT ( 'NONE',  ( -3.485499217011999828, -78.48547958007489456, -1.904403262310999906E-08 ) ) ;
#899=CARTESIAN_POINT ( 'NONE',  ( 0.8163124805188861632, -79.12395831701307714, -3.929161116704327217 ) ) ;
#928=CARTESIAN_POINT ( 'NONE',  ( 3.549939863155112008, -85.80681307243297340, 2.578428034955769999 ) ) ;
#942=CARTESIAN_POINT ( 'NONE',  ( 3.485499217012000717, -78.48547957940617437, 2.057048811703057645 ) ) ;
#961=CARTESIAN_POINT ( 'NONE',  ( 3.441149770290139909, -83.94166667910380397, -0.1250751152382284792 ) ) ;
#984=CARTESIAN_POINT ( 'NONE',  ( -3.341510155812000171, -84.42243313234698121, 1.310745937740000144 ) ) ;
#995=CARTESIAN_POINT ( 'NONE',  ( 0.3402453830687809933, -86.10000000000019327, -7.595013698427217186 ) ) ;
#1038=CARTESIAN_POINT ( 'NONE',  ( 0.6175300363197693265, -81.28229165379221399, 3.388491480252034282 ) ) ;
#1051=CARTESIAN_POINT ( 'NONE',  ( -0.7770281622696295631, -85.98458445108748549, 3.914531931580598645 ) ) ;
#1055=CARTESIAN_POINT ( 'NONE',  ( 4.163357712510999953, -79.52423699984079519, 0.3099401135692000375 ) ) ;
#1071=CIRCLE ( 'NONE', #52915, 4.000000000000000000 ) ;
#1084=CARTESIAN_POINT ( 'NONE',  ( 3.835477222130000197, -83.58453969748799750, -0.9975492235297998000 ) ) ;
#1092=CARTESIAN_POINT ( 'NONE',  ( -3.999999999999815259, -78.72610001270986402, -1.678385095468384722E-14 ) ) ;
#1104=CARTESIAN_POINT ( 'NONE',  ( -3.480702090310999974, -78.73368213548980066, -0.6826041573473999868 ) ) ;
#1112=CARTESIAN_POINT ( 'NONE',  ( 2.318769295210185710, -78.77851881763733388, -4.014936526035610243 ) ) ;
#1123=CARTESIAN_POINT ( 'NONE',  ( -3.617957113613000431, -78.32128455456849281, 1.158813396440000032 ) ) ;
#1144=CARTESIAN_POINT ( 'NONE',  ( -2.892792818793000542, -85.03957450217399128, -2.124967581011000028 ) ) ;
#1154=CARTESIAN_POINT ( 'NONE',  ( 4.000000000000000000, -78.69999999999998863, 0.000000000000000000 ) ) ;
#1210=CARTESIAN_POINT ( 'NONE',  ( 4.020839152126976401, -85.88547957940600952, 0.4615274515358095964 ) ) ;
#1244=CARTESIAN_POINT ( 'NONE',  ( 0.8378965770218049780, -83.63333334673063746, -3.340896199513284870 ) ) ;
#1268=CARTESIAN_POINT ( 'NONE',  ( -2.936781018647000252, -85.86543811554798822, 2.063666607083000315 ) ) ;
#1278=CARTESIAN_POINT ( 'NONE',  ( 3.380118192975977820, -85.79678895079199208, -1.504925579246050527 ) ) ;
#1289=CARTESIAN_POINT ( 'NONE',  ( -0.3065357972716182267, -82.84322915123868825, 4.000656104458952811 ) ) ;
#1292=CARTESIAN_POINT ( 'NONE',  ( 3.044330217611999956, -84.11092953870900146, 2.852822925048999814 ) ) ;
#1321=CARTESIAN_POINT ( 'NONE',  ( 3.159418921492714638, -79.54791666055969301, 1.368597868856442856 ) ) ;
#1341=CARTESIAN_POINT ( 'NONE',  ( -2.068348282409000038, -80.00523869776598929, 3.626505972287000112 ) ) ;
#1345=CARTESIAN_POINT ( 'NONE',  ( 2.971106681726000343, -79.60682046129089429, 1.938318254092999959 ) ) ;
#1364=CARTESIAN_POINT ( 'NONE',  ( 3.755995663163999687, -82.14153471428599573, -0.05909197296705000213 ) ) ;
#1387=CARTESIAN_POINT ( 'NONE',  ( -3.180479912003000287, -80.29693765374598513, -1.570387657113000213 ) ) ;
#1412=CARTESIAN_POINT ( 'NONE',  ( -0.4317228448582000055, -80.36167549782599906, -4.107568489194999728 ) ) ;
#1434=CARTESIAN_POINT ( 'NONE',  ( -1.739781828957000176, -86.23821544543099549, 3.560805514105999769 ) ) ;
#1441=CARTESIAN_POINT ( 'NONE',  ( 2.283260173233999879, -82.70557145154198508, 3.491877656328999713 ) ) ;
#1449=CARTESIAN_POINT ( 'NONE',  ( 0.000000000000000000, -78.69999999999998863, 0.000000000000000000 ) ) ;
#1468=FACE_OUTER_BOUND ( 'NONE', #54531, .T. ) ;
#1474=CARTESIAN_POINT ( 'NONE',  ( -1.711240663526480743, -78.96979164862780465, -3.629922989123440136 ) ) ;
#1482=CARTESIAN_POINT ( 'NONE',  ( -3.518657424384993959, -85.83735716284299144, 1.566607219110014659 ) ) ;
#1498=CARTESIAN_POINT ( 'NONE',  ( 1.387607402548059143, -85.88547957940599531, 3.197381817704088469 ) ) ;
#1513=CARTESIAN_POINT ( 'NONE',  ( -3.444390397065229426, -78.62148120184446043, 1.946201225192911943 ) ) ;
#1548=CARTESIAN_POINT ( 'NONE',  ( -0.4361047888467999845, -80.56882046129099706, -4.149259901320998978 ) ) ;
#1552=CARTESIAN_POINT ( 'NONE',  ( -2.265281180526000249, -84.43400986860198998, 2.726439490990999914 ) ) ;
#1563=CARTESIAN_POINT ( 'NONE',  ( 0.4002886859638069006, -86.07389998728979208, -8.935310233444662131 ) ) ;
#1574=CARTESIAN_POINT ( 'NONE',  ( -2.959121675647450989, -86.02291668546635606, 2.710146891174588291 ) ) ;
#1579=CARTESIAN_POINT ( 'NONE',  ( -4.137408106676000230, -84.71844503318800434, -0.5402929373543000624 ) ) ;
#1607=CARTESIAN_POINT ( 'NONE',  ( 2.124321423109925444, -81.16666665424342852, 2.711257319178282277 ) ) ;
#1628=CARTESIAN_POINT ( 'NONE',  ( 3.793743692741000206, -79.33493425789589537, -1.737118776092000161 ) ) ;
#1657=CARTESIAN_POINT ( 'NONE',  ( 2.151616641007000119, -84.90729426542299052, -3.328142986482999888 ) ) ;
#1678=CARTESIAN_POINT ( 'NONE',  ( -2.502852178527999794, -81.49944189855800403, 2.513424115303000139 ) ) ;
#1699=CARTESIAN_POINT ( 'NONE',  ( 2.137066360725999647, -79.03892549782628407, -2.883865937898999920 ) ) ;
#1704=CARTESIAN_POINT ( 'NONE',  ( -3.778552491321000240, -78.99318692756679638, -1.585466545969598184E-14 ) ) ;
#1723=CARTESIAN_POINT ( 'NONE',  ( 3.766997741046000048, -82.55440783550699280, -1.388142923443000054 ) ) ;
#1730=CARTESIAN_POINT ( 'NONE',  ( -0.8074440912466001041, -83.54732435840999472, -4.093237021270000220 ) ) ;
#1736=CARTESIAN_POINT ( 'NONE',  ( 2.433585806321822531, -78.97658474417778507, -2.631032898609783288 ) ) ;
#1766=CARTESIAN_POINT ( 'NONE',  ( -1.213234814083022917, -81.39791667569573974, 3.866117327208635324 ) ) ;
#1773=CARTESIAN_POINT ( 'NONE',  ( -3.576074390005993475, -85.88547955769999476, 1.592170899228015024 ) ) ;
#1849=CARTESIAN_POINT ( 'NONE',  ( -0.6865545683297000767, -83.54732435840999472, -3.480402676389000138 ) ) ;
#1873=CARTESIAN_POINT ( 'NONE',  ( -0.9057240420843423179, -85.02083334134603376, -3.948137167706869288 ) ) ;
#1923=CARTESIAN_POINT ( 'NONE',  ( -3.198047453352999892, -78.84766706549169157, -2.679415071575999896 ) ) ;
#1955=CARTESIAN_POINT ( 'NONE',  ( -2.415600723022000462, -83.10353803642099990, -2.876846102162000207 ) ) ;
#1975=CARTESIAN_POINT ( 'NONE',  ( -2.719239774786999853, -78.84766706549169157, -2.278256386769999864 ) ) ;
#1999=CARTESIAN_POINT ( 'NONE',  ( 0.5992999846766000616, -81.80853455456798429, -3.708388589188999607 ) ) ;
#2017=CARTESIAN_POINT ( 'NONE',  ( 3.437035393651000081, -82.51432450217399150, -1.965223482742000316 ) ) ;
#2025=CARTESIAN_POINT ( 'NONE',  ( 3.962812355711000212, -78.85171438276199751, 0.000000000000000000 ) ) ;
#2028=CARTESIAN_POINT ( 'NONE',  ( 1.942774989866609348, -78.95669558350101624, -2.968542881336678985 ) ) ;
#2034=AXIS2_PLACEMENT_3D ( 'NONE', #39750, #40643, #9350 ) ;
#2097=CARTESIAN_POINT ( 'NONE',  ( 3.437187628289000152, -78.54828564506388489, -4.209340827053006789E-16 ) ) ;
#2136=CARTESIAN_POINT ( 'NONE',  ( -1.473215862480999894, -82.93980678759699288, 3.226639527409000063 ) ) ;
#2160=CARTESIAN_POINT ( 'NONE',  ( -4.027474705542414490, -84.67395833761210611, 0.4353081749068463124 ) ) ;
#2234=CARTESIAN_POINT ( 'NONE',  ( -3.999289405514485196, -78.69999999999998863, -0.07539397150088360255 ) ) ;
#2239=CARTESIAN_POINT ( 'NONE',  ( -3.497086053584999910, -84.30604218908899838, 1.371772379829000021 ) ) ;
#2256=CARTESIAN_POINT ( 'NONE',  ( 2.359935201127000060, -81.13242513063499928, 2.648634738920000231 ) ) ;
#2271=CARTESIAN_POINT ( 'NONE',  ( -1.412116703021428998, -86.12609999968209706, -3.092883188393197091 ) ) ;
#2282=CARTESIAN_POINT ( 'NONE',  ( -2.650684130113999615, -81.20728455456799111, 2.661810600175999575 ) ) ;
#2300=CARTESIAN_POINT ( 'NONE',  ( 3.648112879021999877, -82.75482450217398878, 1.936488760383000107 ) ) ;
#2307=CARTESIAN_POINT ( 'NONE',  ( 3.685137227213000521, -82.58532103627599952, 1.956153376060999927 ) ) ;
#2343=CARTESIAN_POINT ( 'NONE',  ( -3.873114923184498348, -81.62916667827332162, 1.189743371674534256 ) ) ;
#2381=CARTESIAN_POINT ( 'NONE',  ( -3.436577016645513627, -78.54828564506388489, -0.06478580652260451656 ) ) ;
#2387=CARTESIAN_POINT ( 'NONE',  ( 3.911994926767235370, -82.33721874605919311, -0.8315198071374734212 ) ) ;
#2420=CARTESIAN_POINT ( 'NONE',  ( -1.557310112275000158, -85.94606716926699619, 3.186928280003000324 ) ) ;
#2445=CARTESIAN_POINT ( 'NONE',  ( -2.729547995496241164, -86.00364585192558309, 2.940596197643096321 ) ) ;
#2484=CARTESIAN_POINT ( 'NONE',  ( 4.614362421889810051, -86.12610001270964233, 0.5296543453898773235 ) ) ;
#2541=CARTESIAN_POINT ( 'NONE',  ( -3.402914194239000434, -81.68874464050298911, 0.9925453996215999330 ) ) ;
#2555=CARTESIAN_POINT ( 'NONE',  ( -4.101471859984844315, -86.36264282632896538, -0.3926127889848393115 ) ) ;
#2564=CARTESIAN_POINT ( 'NONE',  ( 2.817646679242999941, -80.60217549782598212, -2.223646712691999650 ) ) ;
#2569=CARTESIAN_POINT ( 'NONE',  ( 2.949810794156999982, -82.38249735065198820, -1.686638855401999981 ) ) ;
#2587=CARTESIAN_POINT ( 'NONE',  ( 3.308356911591999960, -85.80681307385599155, -1.472975398278999926 ) ) ;
#2601=CARTESIAN_POINT ( 'NONE',  ( -0.5454189353424065967, -78.86967215500642681, -3.431877180009151651 ) ) ;
#2604=DIRECTION ( 'NONE',  ( 0.000000000000000000, -1.000000000000000000, 0.000000000000000000 ) ) ;
#2628=CARTESIAN_POINT ( 'NONE',  ( 0.06506789018937424174, -81.32083334150291876, 4.050171521248369544 ) ) ;
#2630=CARTESIAN_POINT ( 'NONE',  ( -3.808791273250000220, -78.64482046129089099, 1.219936614250999973 ) ) ;
#2723=CARTESIAN_POINT ( 'NONE',  ( -3.106054555984679055, -86.10000000000019327, 1.382904586457923246 ) ) ;
#2730=CARTESIAN_POINT ( 'NONE',  ( -4.043785186575674651, -78.67389998729009903, -2.284879765406155006 ) ) ;
#2734=CARTESIAN_POINT ( 'NONE',  ( -3.903296333128821516, -84.63541667053057438, 1.088434527864090340 ) ) ;
#2777=DIRECTION ( 'NONE',  ( 0.000000000000000000, -1.000000000000000000, 0.000000000000000000 ) ) ;
#2826=CARTESIAN_POINT ( 'NONE',  ( -1.280865346364000068, -79.04323530191599900, -3.305193740963000337 ) ) ;
#2839=CARTESIAN_POINT ( 'NONE',  ( -1.412116703021476960, -86.09999999999996589, -3.092883188393807270 ) ) ;
#2850=CARTESIAN_POINT ( 'NONE',  ( 3.779826922834999881, -82.16928455456799441, 0.3812749626282999627 ) ) ;
#2854=CARTESIAN_POINT ( 'NONE',  ( 1.924356497468000082, -85.26849735065199809, -2.976880213510999962 ) ) ;
#2870=CARTESIAN_POINT ( 'NONE',  ( 3.106054555984999688, -86.09999999999999432, -1.382904586457999851 ) ) ;
#2875=CARTESIAN_POINT ( 'NONE',  ( -4.136973154815000164, -84.74982851107797899, -0.5403780116516999632 ) ) ;
#2883=CARTESIAN_POINT ( 'NONE',  ( 2.936298172289618869, -78.99844905003692475, -2.194537220288346191 ) ) ;
#2898=CARTESIAN_POINT ( 'NONE',  ( -2.218416052576314801, -79.00321104920828930, -3.679255452198593179 ) ) ;
#2902=CARTESIAN_POINT ( 'NONE',  ( -4.000000000000000000, -78.69999999915415856, 2.834003763004000336E-08 ) ) ;
#2971=CARTESIAN_POINT ( 'NONE',  ( 1.353569424327119686, -86.09999999999998010, 3.118950113985159867 ) ) ;
#2976=MECHANICAL_DESIGN_GEOMETRIC_PRESENTATION_REPRESENTATION('',(#53896),#30306);
#3123=CARTESIAN_POINT ( 'NONE',  ( -0.3706195565557000027, -80.60649082017198452, -3.525281893971000002 ) ) ;
#3145=CARTESIAN_POINT ( 'NONE',  ( -3.236022287149000309, -78.56950264934789629, 1.036481599910999973 ) ) ;
#3149=CARTESIAN_POINT ( 'NONE',  ( -1.557146760448999911, -85.92094503318799070, 3.187006944544999776 ) ) ;
#3169=CARTESIAN_POINT ( 'NONE',  ( 2.265106641207000227, -85.23083017214499080, -3.503690498526999875 ) ) ;
#3172=ORIENTED_EDGE ( 'NONE', *, *, #20214, .T. ) ;
#3175=CARTESIAN_POINT ( 'NONE',  ( -1.507301607646650332, -78.84234659871619044, -3.678386913577406769 ) ) ;
#3195=CARTESIAN_POINT ( 'NONE',  ( 3.437187628289000152, -78.85171435493610659, -2.028536691635913325 ) ) ;
#3240=DIRECTION ( 'NONE',  ( -1.000000000000000000, 0.000000000000000000, 0.000000000000000000 ) ) ;
#3242=CARTESIAN_POINT ( 'NONE',  ( 4.000000000000000000, -78.69999999999998863, 0.000000000000000000 ) ) ;
#3284=CARTESIAN_POINT ( 'NONE',  ( 0.6655869891369000646, -82.09442852648498956, -4.118674637652000037 ) ) ;
#3378=CARTESIAN_POINT ( 'NONE',  ( -4.139728944602000027, -84.78749735065200355, -0.5405960093036000780 ) ) ;
#3405=CARTESIAN_POINT ( 'NONE',  ( 3.380803704886000016, -82.53049761187099875, 0.3410288241623999905 ) ) ;
#3417=CARTESIAN_POINT ( 'NONE',  ( -3.272863771658545584, -86.25171435493597016, -2.284202767185578242 ) ) ;
#3424=CARTESIAN_POINT ( 'NONE',  ( -3.964978550598999618, -81.82057179202399766, 1.156485587164000295 ) ) ;
#3427=CARTESIAN_POINT ( 'NONE',  ( 3.225105726725999933, -79.36005496681158888, -1.476568833565000238 ) ) ;
#3429=CARTESIAN_POINT ( 'NONE',  ( 3.546855337703000544, -85.43994503318799616, 0.03714407394458000417 ) ) ;
#3446=CARTESIAN_POINT ( 'NONE',  ( -3.362678705222999831, -84.86381343186599224, -2.470316658220000239 ) ) ;
#3452=CARTESIAN_POINT ( 'NONE',  ( 3.399999999999689937, -78.72609999968184979, -4.163799117100620920E-16 ) ) ;
#3471=CARTESIAN_POINT ( 'NONE',  ( -0.03630073495416798190, -78.96264283715740362, -3.851479002382501182 ) ) ;
#3481=CARTESIAN_POINT ( 'NONE',  ( 3.496576729809000028, -79.53150264934789959, 2.281129299029000190 ) ) ;
#3522=CARTESIAN_POINT ( 'NONE',  ( 3.433232437268999959, -83.87042953870898998, -0.8930104441242000535 ) ) ;
#3531=VERTEX_POINT ( 'NONE', #20100 ) ;
#3545=CARTESIAN_POINT ( 'NONE',  ( 3.549939863155374464, -86.39318692756700102, 2.578428034955390746 ) ) ;
#3578=CARTESIAN_POINT ( 'NONE',  ( 4.614362421890620070, -86.07389998728977787, 0.5296543453901456644 ) ) ;
#3584=CARTESIAN_POINT ( 'NONE',  ( 2.301294140410000022, -78.54828561723799396, -3.984678389768961271 ) ) ;
#3623=CARTESIAN_POINT ( 'NONE',  ( -0.5731199659188802586, -86.12610001270964233, 4.609165628484651833 ) ) ;
#3659=CARTESIAN_POINT ( 'NONE',  ( -3.844914979824000323, -84.79907450217399401, 1.508354171302999980 ) ) ;
#3686=CARTESIAN_POINT ( 'NONE',  ( 3.534928549350000004, -79.52423699984079519, 0.2631568632097999738 ) ) ;
#3699=CARTESIAN_POINT ( 'NONE',  ( -1.599699822274783134, -86.36264283715696877, -3.503736395301632722 ) ) ;
#3700=CARTESIAN_POINT ( 'NONE',  ( 3.266119435496772194, -85.82533526675824476, 1.464745090892502155 ) ) ;
#3709=CARTESIAN_POINT ( 'NONE',  ( 0.7877379977805000211, -81.21500264934797997, 3.456071849709000166 ) ) ;
#3712=CARTESIAN_POINT ( 'NONE',  ( 2.575494480515000184, -83.75644503318798684, -2.438932253181000043 ) ) ;
#3732=CARTESIAN_POINT ( 'NONE',  ( -4.137391094169000638, -84.74356301659899771, -0.5404326035545999884 ) ) ;
#3739=CARTESIAN_POINT ( 'NONE',  ( 0.8501357521078367618, -78.91365707727138101, -3.816953471012215715 ) ) ;
#3758=CARTESIAN_POINT ( 'NONE',  ( -2.347024683480479545, -78.91452044229970397, -3.892553587101836410 ) ) ;
#3767=CARTESIAN_POINT ( 'NONE',  ( 3.981833447626999423, -82.41750264934799475, 0.4016515649867999915 ) ) ;
#3831=CARTESIAN_POINT ( 'NONE',  ( -0.5518643889783007017, -86.36264283715698298, 4.438223277016744461 ) ) ;
#3849=CARTESIAN_POINT ( 'NONE',  ( -4.071647054251999798, -81.73367725304099451, -0.9100801767057999925 ) ) ;
#3850=( GEOMETRIC_REPRESENTATION_CONTEXT ( 3 ) GLOBAL_UNCERTAINTY_ASSIGNED_CONTEXT ( ( #34253 ) ) GLOBAL_UNIT_ASSIGNED_CONTEXT ( ( #26747, #50387, #27627 ) ) REPRESENTATION_CONTEXT ( 'NONE', 'WORKASPACE' ) );
#3864=CARTESIAN_POINT ( 'NONE',  ( -2.764837346329003687, -86.07389998728977787, 3.732097096069626474 ) ) ;
#3941=CARTESIAN_POINT ( 'NONE',  ( 3.046345631554999933, -84.18624735065199616, 2.854711556928000160 ) ) ;
#3972=CARTESIAN_POINT ( 'NONE',  ( -0.05794900967641999218, -80.13320636806399477, 3.962654676452000757 ) ) ;
#3985=CARTESIAN_POINT ( 'NONE',  ( 3.518657424384936672, -86.36264283715698298, -1.566607219110143223 ) ) ;
#3986=CARTESIAN_POINT ( 'NONE',  ( 0.4177217270225673240, -85.94664870426311154, 3.455032609703315494 ) ) ;
#3991=CARTESIAN_POINT ( 'NONE',  ( 3.939216039107999556, -82.66232476339300206, 0.3973570580265000651 ) ) ;
#3995=CARTESIAN_POINT ( 'NONE',  ( -2.689955776593000003, -81.68442549782599826, -2.376525467545999692 ) ) ;
#4015=CARTESIAN_POINT ( 'NONE',  ( -2.666500435283000403, -84.50306218606498021, 3.209337609828999849 ) ) ;
#4022=CARTESIAN_POINT ( 'NONE',  ( 0.8592843842366197915, -78.91394566548676437, -3.814601581028083555 ) ) ;
#4042=CARTESIAN_POINT ( 'NONE',  ( 3.407095545933000125, -78.77851879815550262, -2.010777145231034346 ) ) ;
#4053=CARTESIAN_POINT ( 'NONE',  ( -1.405170778590000058, -82.00555496681198520, -3.928813311532000530 ) ) ;
#4081=DIRECTION ( 'NONE',  ( 0.000000000000000000, -1.000000000000000000, 0.000000000000000000 ) ) ;
#4096=CARTESIAN_POINT ( 'NONE',  ( -2.902373257307000021, -86.03492953870899385, 2.039717538649000073 ) ) ;
#4121=CARTESIAN_POINT ( 'NONE',  ( 3.576074390005824721, -86.31452044229999387, -1.592170899228392944 ) ) ;
#4157=CARTESIAN_POINT ( 'NONE',  ( -3.677663026310137084, -86.02148118236289065, 1.555017880480947801 ) ) ;
#4164=CARTESIAN_POINT ( 'NONE',  ( 2.148673102446170713, -78.39678895079168797, -3.720415885850087534 ) ) ;
#4177=CARTESIAN_POINT ( 'NONE',  ( -0.03734817897619031879, -78.54828561723799396, 3.962636354764707658 ) ) ;
#4195=CARTESIAN_POINT ( 'NONE',  ( 3.325701842495000005, -82.39999999999999147, -0.7068997487804000723 ) ) ;
#4242=CARTESIAN_POINT ( 'NONE',  ( -0.7781692987085999658, -84.55857450217399673, 4.056224359023000048 ) ) ;
#4274=CARTESIAN_POINT ( 'NONE',  ( 3.746144170002000173, -79.77245509461999973, 0.2788807567526999653 ) ) ;
#4284=CARTESIAN_POINT ( 'NONE',  ( 3.647699722740934014, -86.17851881763699851, -1.624060551956148624 ) ) ;
#4291=CARTESIAN_POINT ( 'NONE',  ( 3.242112172283999616, -80.97881882065600223, -2.558754062436000343 ) ) ;
#4294=CARTESIAN_POINT ( 'NONE',  ( -3.445820259768999971, -81.44392549782598678, 1.005017585769000021 ) ) ;
#4315=CARTESIAN_POINT ( 'NONE',  ( 2.168860615702000061, -82.38203554481998481, 3.316922010221999617 ) ) ;
#4323=CARTESIAN_POINT ( 'NONE',  ( 0.9410294744130467404, -78.91653188272211139, -3.792696602583483845 ) ) ;
#4355=CARTESIAN_POINT ( 'NONE',  ( -2.384909972384000376, -80.44230496681200293, -3.423779596157999983 ) ) ;
#4380=CARTESIAN_POINT ( 'NONE',  ( 3.318044994455000118, -82.87121544543099105, 1.761282353723000016 ) ) ;
#4386=CARTESIAN_POINT ( 'NONE',  ( -1.673666828592297096, -85.94583333953119109, 3.009623589966792689 ) ) ;
#4397=CARTESIAN_POINT ( 'NONE',  ( 3.133406165714999858, -82.54767953870899078, 1.663272498094999996 ) ) ;
#4421=CARTESIAN_POINT ( 'NONE',  ( -2.355016251976907782, -86.17851879815599148, 3.178902848252080915 ) ) ;
#4457=CARTESIAN_POINT ( 'NONE',  ( 3.548349909811000735, -78.43735717367049176, -1.307818870560639724E-15 ) ) ;
#4513=CARTESIAN_POINT ( 'NONE',  ( -3.579678601589999953, -85.86929758755698572, 0.3912085550186999994 ) ) ;
#4523=CARTESIAN_POINT ( 'NONE',  ( 3.380118192976000469, -86.40321104920799655, -1.504925579245999900 ) ) ;
#4537=CARTESIAN_POINT ( 'NONE',  ( 3.986964100386339638, -82.47708331396407289, 0.4532267925817293208 ) ) ;
#4540=CARTESIAN_POINT ( 'NONE',  ( -3.894441588578999802, -83.34449735065199150, -1.504301970839000191 ) ) ;
#4572=CARTESIAN_POINT ( 'NONE',  ( -1.357398369685000050, -79.29145339669528880, -3.502682470260999992 ) ) ;
#4582=CARTESIAN_POINT ( 'NONE',  ( 2.668955399247460392, -86.25171438276200320, -3.748372073262821846 ) ) ;
#4593=CARTESIAN_POINT ( 'NONE',  ( 3.755245102247999789, -79.53581372688118734, -1.719490641506999928 ) ) ;
#4619=CARTESIAN_POINT ( 'NONE',  ( 3.437033289993999929, -82.13767524227699823, -1.965227161882999951 ) ) ;
#4626=CARTESIAN_POINT ( 'NONE',  ( -3.999999999999708233, -78.70000000000000284, 7.999999999999366729 ) ) ;
#4660=CARTESIAN_POINT ( 'NONE',  ( 3.936869704505999490, -80.97450264934799691, 1.389480733867999751 ) ) ;
#4666=CARTESIAN_POINT ( 'NONE',  ( 3.437841776182999798, -84.02832601947699231, 0.8751022178784999550 ) ) ;
#4682=CARTESIAN_POINT ( 'NONE',  ( -3.504176354730999865, -83.59271544543099708, -1.353554617958000028 ) ) ;
#4699=CARTESIAN_POINT ( 'NONE',  ( -2.281219053130000063, -83.38942953870899544, -2.716724548313999676 ) ) ;
#4719=CARTESIAN_POINT ( 'NONE',  ( 3.241578942234842220, -86.36264282632899381, -1.443243930775356176 ) ) ;
#4723=CARTESIAN_POINT ( 'NONE',  ( 1.734545068753198915, -79.18177081765752234, -3.617932226706877863 ) ) ;
#4750=CARTESIAN_POINT ( 'NONE',  ( -2.042798770927881868, -78.62148120184446043, -3.387993206663131307 ) ) ;
#4762=CARTESIAN_POINT ( 'NONE',  ( 3.778552491321000684, -78.40681307243320930, 2.230001049574967809 ) ) ;
#4781=CARTESIAN_POINT ( 'NONE',  ( 3.420569553252711614, -82.47708335033021854, 0.3941913140830599627 ) ) ;
#4805=CARTESIAN_POINT ( 'NONE',  ( 1.095285505811000037, -84.19350903806798669, 3.371249143215000021 ) ) ;
#4816=CARTESIAN_POINT ( 'NONE',  ( 3.518657424385000176, -86.36264283715698298, -1.566607219110000004 ) ) ;
#4830=CARTESIAN_POINT ( 'NONE',  ( 3.936689796931376772, -82.49635414750480322, 0.7746042215944272114 ) ) ;
#4834=CARTESIAN_POINT ( 'NONE',  ( -3.413427344757999915, -86.03492953870899385, 2.398873957536999946 ) ) ;
#4864=CARTESIAN_POINT ( 'NONE',  ( -3.391956917632873214, -80.24166665785288899, -0.5931127412343725203 ) ) ;
#4866=CARTESIAN_POINT ( 'NONE',  ( 3.705840671984999890, -81.21546018839499936, -0.6149109081260000220 ) ) ;
#4878=CARTESIAN_POINT ( 'NONE',  ( 3.514555345245232942, -85.82264533963498820, 1.481929043551247549 ) ) ;
#4883=CARTESIAN_POINT ( 'NONE',  ( -3.811244649200000278, -78.68248402847228817, 1.220956923171000019 ) ) ;
#4887=CARTESIAN_POINT ( 'NONE',  ( 3.537670483016999601, -79.48657046129088144, 0.2635152204372000484 ) ) ;
#4911=CARTESIAN_POINT ( 'NONE',  ( 2.168906614795000021, -85.50468686974798516, 3.514878928686000048 ) ) ;
#4947=CARTESIAN_POINT ( 'NONE',  ( 3.939216473890999826, -82.28567549782599144, 0.3973527477657000095 ) ) ;
#4966=CARTESIAN_POINT ( 'NONE',  ( 0.1743933192647000030, -85.86974735065199127, 3.540409746406000036 ) ) ;
#4969=CARTESIAN_POINT ( 'NONE',  ( -0.7698650111177089972, -85.02083334241058310, -3.355916637785700374 ) ) ;
#5008=CARTESIAN_POINT ( 'NONE',  ( -3.805607895093767290, -78.77708331314624957, -1.272258977157935345 ) ) ;
#5024=B_SPLINE_SURFACE_WITH_KNOTS ( 'NONE', 3, 3, ( 
 ( #2630, #7621, #28380, #12058, #29748, #33894, #19251, #38628, #46426, #38912, #41977, #20339, #25623, #11774, #20627, #56358, #29466, #1548, #47522, #56645, #39196, #56930, #37246, #52500, #43351, #16203, #43646, #7051, #14518, #55258, #41684, #32510, #50555, #14807, #10107 ),
 ( #50848, #25334, #5662, #32800, #5955, #34180, #38334, #47803, #7333, #57211, #17640, #8484, #31192, #34760, #48939, #57787, #4355, #53960, #35629, #53657, #13497, #13197, #39493, #12340, #22660, #26478, #45107, #58081, #9081, #4053, #8198, #30621, #48370, #49231, #43932 ),
 ( #17940, #25910, #7908, #12906, #57497, #58378, #8783, #31489, #52786, #3481, #44502, #16778, #22056, #44218, #53358, #21486, #35931, #35039, #21769, #22357, #26774, #4660, #44803, #27068, #40064, #26200, #48654, #17059, #40370, #53074, #12625, #49535, #30904, #30328, #3767 ),
 ( #39773, #17343, #35332, #36233, #31788, #32372, #40669, #5520, #27657, #36813, #49831, #41837, #18532, #5238, #5811, #19111, #9379, #1412, #32660, #28236, #27945, #50414, #23529, #54831, #37102, #14372, #45406, #45699, #46287, #51001, #10549, #37393, #13787, #23243, #4947 ),
 ( #1123, #41541, #14958, #10252, #23818, #41251, #838, #32956, #28532, #9964, #46581, #45994, #27368, #18820, #22953, #19402, #54256, #55119, #6108, #55412, #14662, #36524, #50712, #260, #50125, #18243, #40963, #54546, #554, #14088, #32085, #9668, #34411, #16139, #2850 ),
 ( #11715, #52158, #6983, #52440, #42716, #38851, #28823, #33251, #42134, #47741, #24414, #20847, #12000, #16428, #11425, #29118, #11144, #29692, #24987, #56292, #56869, #55712, #51871, #19993, #25275, #2282, #37693, #43007, #24704, #15845, #1999, #34114, #7274, #24115, #56004 ),
 ( #15259, #48031, #33833, #29405, #43294, #29978, #1699, #19693, #20565, #37980, #51293, #10850, #46872, #15554, #20278, #6399, #42430, #33547, #51586, #2564, #47458, #56579, #47164, #38563, #38271, #6696, #4294, #44443, #3995, #22294, #21997, #48312, #21133, #31433, #17281 ),
 ( #3145, #40310, #52729, #58319, #17881, #31130, #53014, #35871, #43583, #26712, #34699, #16717, #21712, #7851, #8721, #40005, #53900, #39142, #57152, #57725, #7563, #30846, #12567, #3709, #12280, #44743, #43879, #30564, #49169, #58021, #30270, #13432, #17582, #53595, #53304 ),
 ( #39718, #35569, #35271, #25852, #48595, #13135, #25563, #3427, #21428, #39436, #8141, #57443, #17003, #34984, #26141, #44162, #12847, #48881, #8424, #26421, #45927, #28169, #37330, #23463, #23754, #37038, #40896, #36747, #41768, #45337, #46221, #5460, #9605, #36171, #14307 ),
 ( #55053, #486, #55346, #50059, #27304, #18178, #14600, #32017, #4887, #1345, #41475, #5746, #54484, #9312, #19047, #32594, #18466, #31725, #19336, #27591, #50644, #14889, #54764, #203, #36457, #54190, #10191, #45043, #45633, #49473, #9023, #27879, #22885, #5174, #27009 ) ),
 .UNSPECIFIED., .F., .F., .F.,
 ( 4, 1, 1, 1, 1, 1, 1, 4 ),
 ( 4, 1, 1, 1, 1, 1, 1, 1, 1, 1, 1, 1, 1, 1, 1, 1, 1, 1, 1, 1, 1, 1, 1, 1, 1, 1, 1, 1, 1, 1, 1, 1, 4 ),
 ( 0.4899999999999999911, 0.5000000000000000000, 0.5999999999999999778, 0.6999999999999999556, 0.8000000000000000444, 0.9000000000000000222, 1.000000000000000000, 1.010000000000000009 ),
 ( -0.02000000000000000042, 0.01250000000000000069, 0.04499999999999999833, 0.07749999999999999944, 0.1100000000000000006, 0.1424999999999999878, 0.1749999999999999889, 0.2074999999999999900, 0.2399999999999999911, 0.2725000000000000200, 0.3049999999999999933, 0.3375000000000000222, 0.3699999999999999956, 0.4025000000000000244, 0.4349999999999999978, 0.4675000000000000266, 0.5000000000000000000, 0.5324999999999999734, 0.5649999999999999467, 0.5975000000000000311, 0.6300000000000000044, 0.6624999999999999778, 0.6949999999999999512, 0.7275000000000000355, 0.7600000000000000089, 0.7924999999999999822, 0.8249999999999999556, 0.8575000000000000400, 0.8900000000000000133, 0.9224999999999999867, 0.9549999999999999600, 0.9875000000000000444, 1.020000000000000018 ),
 .UNSPECIFIED. ) ;
#5036=CARTESIAN_POINT ( 'NONE',  ( 3.930393413736106734, -86.02148120184399716, 0.4511457402663626159 ) ) ;
#5042=CARTESIAN_POINT ( 'NONE',  ( -2.309341173333539388, -78.43735716284257364, -3.830055274395752551 ) ) ;
#5055=CARTESIAN_POINT ( 'NONE',  ( -3.547719550341454475, -78.43735717367049176, -0.06688104799386529464 ) ) ;
#5098=CARTESIAN_POINT ( 'NONE',  ( -0.6946676981835000486, -83.34017939494499672, -3.521531175359999821 ) ) ;
#5110=CARTESIAN_POINT ( 'NONE',  ( -3.241578942234993654, -85.83735717367099483, 1.443243930775013784 ) ) ;
#5124=CARTESIAN_POINT ( 'NONE',  ( 4.008581223418561379, -82.43854164688262642, -0.1919510447721787250 ) ) ;
#5153=CARTESIAN_POINT ( 'NONE',  ( 0.5992844399098999908, -82.41796443320698984, -3.708392236748999871 ) ) ;
#5164=CARTESIAN_POINT ( 'NONE',  ( 3.047808061981939876, -85.85448694835680783, 2.394986058418032471 ) ) ;
#5170=CARTESIAN_POINT ( 'NONE',  ( -2.067188713461000305, -79.93618638030199008, 3.624472860286000131 ) ) ;
#5174=CARTESIAN_POINT ( 'NONE',  ( 3.440741359840000069, -82.45273712795798815, -0.2267907360308999976 ) ) ;
#5200=CARTESIAN_POINT ( 'NONE',  ( -1.832953822565000168, -85.87701485180299699, 3.751014218058000171 ) ) ;
#5225=CARTESIAN_POINT ( 'NONE',  ( -0.03769889196560047978, -78.72610001270986402, -3.999822345247734834 ) ) ;
#5238=CARTESIAN_POINT ( 'NONE',  ( -3.523827339823000226, -79.88067549782599031, 2.154331540686999613 ) ) ;
#5258=CARTESIAN_POINT ( 'NONE',  ( 3.170434149039000005, -82.75482450217398878, 1.682927666644999931 ) ) ;
#5297=CARTESIAN_POINT ( 'NONE',  ( 1.990533724726763820, -79.70208332345784186, 3.529387283865522473 ) ) ;
#5327=CARTESIAN_POINT ( 'NONE',  ( 3.106054555984665289, -86.07390000031791999, -1.382904586457468943 ) ) ;
#5330=CARTESIAN_POINT ( 'NONE',  ( -0.03344221497652981323, -78.43735717367049176, -3.548192314505119960 ) ) ;
#5341=CARTESIAN_POINT ( 'NONE',  ( 3.548349909811000291, -78.43735717367052018, 2.094141616746843404 ) ) ;
#5360=CARTESIAN_POINT ( 'NONE',  ( 0.01567759588933310619, -82.82395834925023337, 3.411067620805362299 ) ) ;
#5382=CARTESIAN_POINT ( 'NONE',  ( -3.559158646470999887, -84.54268354761398996, -0.4649029617932999847 ) ) ;
#5393=CARTESIAN_POINT ( 'NONE',  ( 3.647699722740940675, -86.02148118236289065, -1.624060551956039822 ) ) ;
#5408=CARTESIAN_POINT ( 'NONE',  ( -3.362425624285000136, -84.83242953870899328, -2.469947173108999916 ) ) ;
#5432=CARTESIAN_POINT ( 'NONE',  ( -3.277886346742791890, -80.12604165830404668, 1.054380925102407218 ) ) ;
#5450=CARTESIAN_POINT ( 'NONE',  ( 3.586328456911428653, -85.81453820040007940, 1.233688378895768434 ) ) ;
#5456=CARTESIAN_POINT ( 'NONE',  ( -4.005627318223000444, -81.61969232303898991, 1.168341821262999902 ) ) ;
#5460=CARTESIAN_POINT ( 'NONE',  ( 2.185735370214000106, -82.24605496681199668, -2.793614180511000189 ) ) ;
#5480=CARTESIAN_POINT ( 'NONE',  ( -1.715416423673999935, -82.73892731861099037, 3.757107549244000033 ) ) ;
#5488=CARTESIAN_POINT ( 'NONE',  ( 3.962812355711001544, -78.85171438276199751, 7.925624711422035062 ) ) ;
#5498=CARTESIAN_POINT ( 'NONE',  ( 3.225040040299000044, -79.33493425789589537, -1.476714839321999984 ) ) ;
#5520=CARTESIAN_POINT ( 'NONE',  ( 3.755321587697000307, -79.15917549782629692, -1.719320632020000073 ) ) ;
#5539=CARTESIAN_POINT ( 'NONE',  ( 3.126065026453999973, -82.63071544543198854, -1.787417263702000048 ) ) ;
#5608=CARTESIAN_POINT ( 'NONE',  ( -0.5084075448453283519, -85.83735717367099483, 4.088733110535459403 ) ) ;
#5624=CARTESIAN_POINT ( 'NONE',  ( 3.914500761937000028, -78.48547955770028750, -4.793880828366022505E-16 ) ) ;
#5631=( BOUNDED_SURFACE ( )  B_SPLINE_SURFACE ( 3, 3, ( 
 ( #43413, #56706, #20970, #2971, #52563, #20402, #16263 ),
 ( #43709, #11832, #34241, #46998, #33384, #16548, #52277 ),
 ( #24538, #4421, #21548, #22421, #44867, #35697, #17712 ),
 ( #40433, #24, #21830, #35390, #9147, #35103, #54020 ),
 ( #13560, #18004, #35995, #30677, #22122, #12402, #57850 ),
 ( #31552, #16838, #53726, #12685, #25968, #26261, #4719 ),
 ( #53137, #17408, #27131, #49599, #45169, #22718, #8848 ),
 ( #39552, #40731, #34821, #58145, #52849, #53421, #30393 ),
 ( #43994, #48429, #7971, #17118, #3545, #57557, #48716 ),
 ( #8261, #44274, #3831, #39836, #12965, #30964, #49001 ),
 ( #13265, #8549, #26540, #31256, #44567, #49297, #4121 ),
 ( #26839, #40132, #51063, #32719, #9728, #23880, #46054 ),
 ( #322, #37167, #31852, #41602, #55180, #25195, #42929 ),
 ( #56501, #48508, #3623, #20771, #21629, #2484, #38772 ),
 ( #47952, #43798, #38483, #56790, #43213, #21057, #16056 ) ),
 .UNSPECIFIED., .F., .F., .T. ) 
 B_SPLINE_SURFACE_WITH_KNOTS ( ( 4, 1, 1, 1, 1, 1, 1, 1, 1, 1, 1, 1, 4 ),
 ( 4, 3, 4 ),
 ( 0.009836358961777999163, 0.09153385889397000486, 0.1732268882812000033, 0.2549245844128000260, 0.3366128623372000028, 0.4183102317861999708, 0.5000049915032999115, 0.5816997502458999270, 0.6633970872647999562, 0.7450853589770999319, 0.8267830756728000718, 0.9084760833474000430, 0.9901736252444659492 ),
 ( 0.000000000000000000, 0.5000000000000000000, 1.000000000000000000 ),
 .UNSPECIFIED. ) 
 GEOMETRIC_REPRESENTATION_ITEM ( )  RATIONAL_B_SPLINE_SURFACE ( (
 ( 1.000000000000000000, 0.8025111637939407183, 0.8025111637939407183, 1.000000000000000000, 0.8025111637939407183, 0.8025111637939407183, 1.000000000000000000),
 ( 1.000000000000000000, 0.8025111637939407183, 0.8025111637939407183, 1.000000000000000000, 0.8025111637939407183, 0.8025111637939407183, 1.000000000000000000),
 ( 1.000000000000000000, 0.8025111637939407183, 0.8025111637939407183, 1.000000000000000000, 0.8025111637939407183, 0.8025111637939407183, 1.000000000000000000),
 ( 1.000000000000000000, 0.8025111637939407183, 0.8025111637939407183, 1.000000000000000000, 0.8025111637939407183, 0.8025111637939407183, 1.000000000000000000),
 ( 1.000000000000000000, 0.8025111637939407183, 0.8025111637939407183, 1.000000000000000000, 0.8025111637939407183, 0.8025111637939407183, 1.000000000000000000),
 ( 1.000000000000000000, 0.8025111637939407183, 0.8025111637939407183, 1.000000000000000000, 0.8025111637939407183, 0.8025111637939407183, 1.000000000000000000),
 ( 1.000000000000000000, 0.8025111637939407183, 0.8025111637939407183, 1.000000000000000000, 0.8025111637939407183, 0.8025111637939407183, 1.000000000000000000),
 ( 1.000000000000000000, 0.8025111637939407183, 0.8025111637939407183, 1.000000000000000000, 0.8025111637939407183, 0.8025111637939407183, 1.000000000000000000),
 ( 1.000000000000000000, 0.8025111637939407183, 0.8025111637939407183, 1.000000000000000000, 0.8025111637939407183, 0.8025111637939407183, 1.000000000000000000),
 ( 1.000000000000000000, 0.8025111637939407183, 0.8025111637939407183, 1.000000000000000000, 0.8025111637939407183, 0.8025111637939407183, 1.000000000000000000),
 ( 1.000000000000000000, 0.8025111637939407183, 0.8025111637939407183, 1.000000000000000000, 0.8025111637939407183, 0.8025111637939407183, 1.000000000000000000),
 ( 1.000000000000000000, 0.8025111637939407183, 0.8025111637939407183, 1.000000000000000000, 0.8025111637939407183, 0.8025111637939407183, 1.000000000000000000),
 ( 1.000000000000000000, 0.8025111637939407183, 0.8025111637939407183, 1.000000000000000000, 0.8025111637939407183, 0.8025111637939407183, 1.000000000000000000),
 ( 1.000000000000000000, 0.8025111637939407183, 0.8025111637939407183, 1.000000000000000000, 0.8025111637939407183, 0.8025111637939407183, 1.000000000000000000),
 ( 1.000000000000000000, 0.8025111637939407183, 0.8025111637939407183, 1.000000000000000000, 0.8025111637939407183, 0.8025111637939407183, 1.000000000000000000) ) ) 
 REPRESENTATION_ITEM ( '' )  SURFACE ( )  );
#5643=CARTESIAN_POINT ( 'NONE',  ( 2.297158073433503755, -83.74895834637031555, -2.566498985648576703 ) ) ;
#5661=B_SPLINE_CURVE_WITH_KNOTS ( 'NONE', 3,
 ( #1154, #51030, #10283, #2025, #42457, #19140, #37134, #10579, #46610, #55145, #14691, #6136, #32693, #28264, #24143 ),
 .UNSPECIFIED., .F., .F.,
 ( 4, 1, 1, 1, 1, 1, 1, 1, 1, 1, 1, 1, 4 ),
 ( 0.000000000000000000, 0.08333615748455000527, 0.1666676910119000155, 0.2500040280097000078, 0.3333307305850000124, 0.4166666802908000067, 0.5000000000075000006, 0.5833333207182000990, 0.6666693035046000748, 0.7499960124165999664, 0.8333323284379000606, 0.9166638841133999405, 1.000000000000000000 ),
 .UNSPECIFIED. ) ;
#5662=CARTESIAN_POINT ( 'NONE',  ( -4.094444587552000137, -78.75880496681158149, -0.8031955627257999497 ) ) ;
#5666=CARTESIAN_POINT ( 'NONE',  ( 0.1846283042134000130, -85.50854634175698266, 3.751963089900000270 ) ) ;
#5678=CARTESIAN_POINT ( 'NONE',  ( -6.389969351467987835, -85.79678895079197787, -5.255310806705900006 ) ) ;
#5690=CARTESIAN_POINT ( 'NONE',  ( 0.6616348183234056490, -82.78541665061636934, 3.958011967683783716 ) ) ;
#5694=CARTESIAN_POINT ( 'NONE',  ( -0.8075922533534999337, -83.51594503318798957, -4.093636164257000054 ) ) ;
#5707=ADVANCED_FACE ( 'NONE', ( #38553 ), #18061, .F. ) ;
#5723=CARTESIAN_POINT ( 'NONE',  ( -1.432607641878103744, -80.47291665695050256, -3.131646614799266537 ) ) ;
#5742=CARTESIAN_POINT ( 'NONE',  ( 3.934691878955999922, -81.01844020063299467, 1.388622521904000040 ) ) ;
#5746=CARTESIAN_POINT ( 'NONE',  ( -0.05200678273669999407, -79.84732046129099103, 3.547090062506000230 ) ) ;
#5770=CARTESIAN_POINT ( 'NONE',  ( -2.532643299141000170, -84.18579177382198964, 3.048230288908000407 ) ) ;
#5778=CARTESIAN_POINT ( 'NONE',  ( 3.999999999999816147, -78.72610001270986402, 7.999999999999665157 ) ) ;
#5791=CARTESIAN_POINT ( 'NONE',  ( -1.757305424856000053, -79.93618638030199008, 3.081143863716000464 ) ) ;
#5811=CARTESIAN_POINT ( 'NONE',  ( -4.126007527045000067, -80.00092549782598894, 0.1859177100975999974 ) ) ;
#5832=CARTESIAN_POINT ( 'NONE',  ( 1.204906488280999888, -83.95346544543099299, -3.775470985156000214 ) ) ;
#5898=CARTESIAN_POINT ( 'NONE',  ( -0.5188809666119423847, -85.80681307385597734, 4.172962832911210285 ) ) ;
#5916=CARTESIAN_POINT ( 'NONE',  ( -3.437217181655167320, -78.70000000000000284, 1.942148107221286724 ) ) ;
#5955=CARTESIAN_POINT ( 'NONE',  ( -1.507531252938999922, -78.99930496681159298, -3.890673863795999665 ) ) ;
#5961=CARTESIAN_POINT ( 'NONE',  ( -1.556282511482000253, -85.87701485180299699, 3.184825365493999527 ) ) ;
#5972=CARTESIAN_POINT ( 'NONE',  ( 0.4002886859631615835, -86.09999999999999432, -8.935310233444422323 ) ) ;
#5983=CARTESIAN_POINT ( 'NONE',  ( -0.4114167394185317961, -85.84947918359929986, 3.991239199179264840 ) ) ;
#5986=CARTESIAN_POINT ( 'NONE',  ( 0.2052812982897999905, -85.80069503318799207, 4.167475636592000932 ) ) ;
#6015=CARTESIAN_POINT ( 'NONE',  ( -3.384237465907204534, -81.74479165198742692, -0.6379114951690191271 ) ) ;
#6033=CARTESIAN_POINT ( 'NONE',  ( -0.4365072073316000334, -80.60649082017198452, -4.151996103213000389 ) ) ;
#6061=CARTESIAN_POINT ( 'NONE',  ( -3.707226347175000214, -85.82921411580198878, 1.046803743307999968 ) ) ;
#6083=CARTESIAN_POINT ( 'NONE',  ( 2.359654807561999856, -81.13869062511399477, 2.648320043780999722 ) ) ;
#6108=CARTESIAN_POINT ( 'NONE',  ( 1.539579185250999904, -80.36553455456798645, -3.651804586294000288 ) ) ;
#6111=CARTESIAN_POINT ( 'NONE',  ( -3.437187628289000152, -78.85171435493609238, -1.442231121412212840E-14 ) ) ;
#6128=CARTESIAN_POINT ( 'NONE',  ( 0.2633489006888999895, -85.39646544543099083, -3.747266932773000381 ) ) ;
#6136=CARTESIAN_POINT ( 'NONE',  ( 3.437187628289000152, -78.85171435493609238, 0.000000000000000000 ) ) ;
#6142=CARTESIAN_POINT ( 'NONE',  ( 2.682229413215286851, -78.98086027728551528, -2.699476886104560158 ) ) ;
#6194=CARTESIAN_POINT ( 'NONE',  ( 4.268285239867494418, -85.79678895079199208, 0.4899302694423579019 ) ) ;
#6250=CARTESIAN_POINT ( 'NONE',  ( 0.2488026545057999972, -85.10431426239898656, -3.538314140727000456 ) ) ;
#6262=CARTESIAN_POINT ( 'NONE',  ( 0.3965672376479022487, -85.94828561723799965, -8.852239448800926169 ) ) ;
#6273=CARTESIAN_POINT ( 'NONE',  ( 4.012235213810621204, -85.44479167924301066, -0.08669540122018622175 ) ) ;
#6328=CARTESIAN_POINT ( 'NONE',  ( -2.943907793430999842, -81.49317640407899432, 2.956342729591999952 ) ) ;
#6355=CARTESIAN_POINT ( 'NONE',  ( 1.142167996899000171, -83.34403886695498898, -3.578662123773000303 ) ) ;
#6374=ORIENTED_EDGE ( 'NONE', *, *, #14831, .T. ) ;
#6377=CARTESIAN_POINT ( 'NONE',  ( -1.281711091423999971, -78.97418298445228402, -3.307376133738999968 ) ) ;
#6399=CARTESIAN_POINT ( 'NONE',  ( -3.218396486835000125, -80.12117549782598758, -1.589233011689999975 ) ) ;
#6420=CARTESIAN_POINT ( 'NONE',  ( -3.776500157906000243, -86.47871544543099276, 0.4129270166134999531 ) ) ;
#6433=CARTESIAN_POINT ( 'NONE',  ( 2.592083719635297712, -78.97662554493233245, -2.800471138597825149 ) ) ;
#6454=CARTESIAN_POINT ( 'NONE',  ( 3.399999999999724576, -78.69999999999998863, -2.006589542798634440 ) ) ;
#6462=CARTESIAN_POINT ( 'NONE',  ( -1.615392861586334883, -81.97604168214044762, -3.673578837756669824 ) ) ;
#6503=CARTESIAN_POINT ( 'NONE',  ( 1.996052162998995350, -78.54828564506389910, 3.456153249904594382 ) ) ;
#6547=CARTESIAN_POINT ( 'NONE',  ( -2.847654145493000222, -83.06005720286400162, 2.114813391968999756 ) ) ;
#6571=CARTESIAN_POINT ( 'NONE',  ( 1.791187267989293064, -85.71458334881383223, 3.590998125927075790 ) ) ;
#6650=CARTESIAN_POINT ( 'NONE',  ( -2.548432965028000208, -83.10353803642099990, -3.035041914084000148 ) ) ;
#6672=CARTESIAN_POINT ( 'NONE',  ( -0.9789553397924000144, -81.37292597959698526, 3.409722363132999590 ) ) ;
#6696=CARTESIAN_POINT ( 'NONE',  ( -2.532762364124999888, -81.32367549782598815, 2.543393847634999538 ) ) ;
#6716=CARTESIAN_POINT ( 'NONE',  ( 3.500502033605999763, -82.87121544543099105, 1.858134073305999889 ) ) ;
#6728=CARTESIAN_POINT ( 'NONE',  ( 2.215346327408018734, -78.96753941592319848, -2.793036654489012616 ) ) ;
#6834=AXIS2_PLACEMENT_3D ( 'NONE', #17669, #4081, #35959 ) ;
#6835=CARTESIAN_POINT ( 'NONE',  ( 1.862677531273999820, -85.70556633873299290, 3.018611295180000376 ) ) ;
#6862=CARTESIAN_POINT ( 'NONE',  ( 2.171690589435127716, -83.71041666057348607, -3.419483144129718877 ) ) ;
#6960=CARTESIAN_POINT ( 'NONE',  ( -2.717122596634000242, -78.92298487743470048, -2.276482554725000274 ) ) ;
#6973=CARTESIAN_POINT ( 'NONE',  ( -3.448314610046759210, -86.39318692614396866, -2.406653721002784074 ) ) ;
#6983=CARTESIAN_POINT ( 'NONE',  ( -3.686203466609999868, -78.44153455456849144, -0.7231120618135999933 ) ) ;
#6987=CARTESIAN_POINT ( 'NONE',  ( -2.858667760471000019, -84.83869503318800298, -2.099900233581000197 ) ) ;
#7010=CARTESIAN_POINT ( 'NONE',  ( -3.891846913306999944, -83.30682352787700040, -1.503357179412999844 ) ) ;
#7031=CARTESIAN_POINT ( 'NONE',  ( -3.184161968443000479, -86.31452041982799983, 1.417680270903999951 ) ) ;
#7045=B_SPLINE_CURVE_WITH_KNOTS ( 'NONE', 3,
 ( #47479, #7582, #20298, #29711, #39455, #52459, #21444, #56891, #2587, #25007, #42738, #12017, #38290, #11448, #2870 ),
 .UNSPECIFIED., .F., .F.,
 ( 4, 1, 1, 1, 1, 1, 1, 1, 1, 1, 1, 1, 4 ),
 ( 0.000000000000000000, 0.08333615748455000527, 0.1666676910119000155, 0.2500040280097000078, 0.3333307305850000124, 0.4166666802908000067, 0.5000000000075000006, 0.5833333207182000990, 0.6666693035046000748, 0.7499960124165999664, 0.8333323284379000606, 0.9166638841133999405, 1.000000000000000000 ),
 .UNSPECIFIED. ) ;
#7049=CARTESIAN_POINT ( 'NONE',  ( -2.873766102139449163, -81.51354167698465858, 2.856429910244337123 ) ) ;
#7051=CARTESIAN_POINT ( 'NONE',  ( -4.071637125700000581, -81.77132046129098342, -0.9101188877549001299 ) ) ;
#7128=CARTESIAN_POINT ( 'NONE',  ( -1.488962551357000175, -84.91501152966898758, -3.216824776211999914 ) ) ;
#7147=CARTESIAN_POINT ( 'NONE',  ( -0.03734840871947565227, -78.54828561723799396, -3.962636352599350875 ) ) ;
#7151=CARTESIAN_POINT ( 'NONE',  ( 2.740721837759387824, -85.25208334383526676, -2.982738968832581605 ) ) ;
#7225=CARTESIAN_POINT ( 'NONE',  ( 3.962812355710999768, -78.54828561723800817, 2.338746314310086394 ) ) ;
#7250=CARTESIAN_POINT ( 'NONE',  ( 0.4735443828009999745, -79.16348572639719805, -3.512938801767000019 ) ) ;
#7265=CARTESIAN_POINT ( 'NONE',  ( -3.113118550637747894, -86.25171435493595595, 1.456966602822371559 ) ) ;
#7274=CARTESIAN_POINT ( 'NONE',  ( 3.455307625259000037, -82.04903455456799577, -1.473715123765999779 ) ) ;
#7278=CARTESIAN_POINT ( 'NONE',  ( 1.925627134546000097, -85.19944503318799889, -2.978845823512000113 ) ) ;
#7299=CARTESIAN_POINT ( 'NONE',  ( -1.733002789576000069, -82.93980678759699288, 3.795625233452999847 ) ) ;
#7305=CARTESIAN_POINT ( 'NONE',  ( 2.437122208593068162, -78.97673430672129768, -2.628241071105698712 ) ) ;
#7322=CARTESIAN_POINT ( 'NONE',  ( -0.03284986460708162054, -78.91452042059380290, -3.485344413137181352 ) ) ;
#7331=CARTESIAN_POINT ( 'NONE',  ( -2.448851404991599701, -81.91822918149604504, -3.178239416597233191 ) ) ;
#7333=CARTESIAN_POINT ( 'NONE',  ( 4.161008951361999664, -79.48030496681158752, 0.3099466714955000368 ) ) ;
#7377=CARTESIAN_POINT ( 'NONE',  ( 3.325194823509913800, -82.39999680491617084, -0.7067916523664262707 ) ) ;
#7417=CARTESIAN_POINT ( 'NONE',  ( 0.2488322192806999844, -85.11057975687899102, -3.538734592273999890 ) ) ;
#7440=CARTESIAN_POINT ( 'NONE',  ( 2.273238512818713808, -78.48547955770027329, -3.936100221940973309 ) ) ;
#7462=( NAMED_UNIT ( * ) SI_UNIT ( $, .STERADIAN. ) SOLID_ANGLE_UNIT ( ) );
#7518=CARTESIAN_POINT ( 'NONE',  ( 2.322889965704216575, -78.67389998729011324, 4.022071092609738052 ) ) ;
#7541=CARTESIAN_POINT ( 'NONE',  ( -2.501200655902999781, -81.56849421602200323, 2.511765616718999894 ) ) ;
#7554=CARTESIAN_POINT ( 'NONE',  ( 2.439046057298411174, -86.39318692614398287, -3.425479544976959279 ) ) ;
#7563=CARTESIAN_POINT ( 'NONE',  ( 3.496909181595999616, -80.85425264934799827, -0.5801637387983998861 ) ) ;
#7566=CARTESIAN_POINT ( 'NONE',  ( -1.490065003087000184, -84.95894503318798741, -3.218892454984999763 ) ) ;
#7582=CARTESIAN_POINT ( 'NONE',  ( 3.654181830570000233, -86.07389998728999103, -1.626946572303000105 ) ) ;
#7588=CARTESIAN_POINT ( 'NONE',  ( 0.3144568442405999975, -82.75050405486598493, 4.163020961247000606 ) ) ;
#7595=CARTESIAN_POINT ( 'NONE',  ( 3.399999999999725908, -78.70000000000000284, 6.799999999999479350 ) ) ;
#7611=CARTESIAN_POINT ( 'NONE',  ( -0.03413113949348758891, -78.99318692614357929, -3.621286655835656898 ) ) ;
#7621=CARTESIAN_POINT ( 'NONE',  ( -4.013619453071000542, -78.68490379462421913, 0.5804379921871000159 ) ) ;
#7703=CARTESIAN_POINT ( 'NONE',  ( -2.066979895997999694, -79.92992088582298038, 3.624106733465999763 ) ) ;
#7802=CARTESIAN_POINT ( 'NONE',  ( 0.1949762683977999955, -86.11796544543098264, 3.958270212781000108 ) ) ;
#7829=CARTESIAN_POINT ( 'NONE',  ( -2.026146017328999793, -80.48624039569099864, -2.908556962501000154 ) ) ;
#7848=CARTESIAN_POINT ( 'NONE',  ( -0.4318353353321000010, -80.73831797169299307, -4.107557903773000341 ) ) ;
#7851=CARTESIAN_POINT ( 'NONE',  ( -3.024299354891000213, -80.01250264934799361, 1.848939479835000066 ) ) ;
#7854=CARTESIAN_POINT ( 'NONE',  ( 0.2671888637738000227, -82.79444503318798354, 3.536973918679999773 ) ) ;
#7873=CARTESIAN_POINT ( 'NONE',  ( -3.349809558510000063, -83.06005720286400162, 2.487739645664000410 ) ) ;
#7878=CARTESIAN_POINT ( 'NONE',  ( 0.8524051983356712991, -78.91372865514620116, -3.816371284592112278 ) ) ;
#7892=CARTESIAN_POINT ( 'NONE',  ( -3.518657424328000438, -86.36264283715298973, 1.566607219238000059 ) ) ;
#7898=CARTESIAN_POINT ( 'NONE',  ( -0.03344221497652981323, -78.96264282632948550, -3.548192314505119960 ) ) ;
#7908=CARTESIAN_POINT ( 'NONE',  ( -4.096741325518999943, -78.68975264934786651, -0.8036461072880000112 ) ) ;
#7971=CARTESIAN_POINT ( 'NONE',  ( -0.5413909687619357092, -86.39318692756700102, 4.353993567106698492 ) ) ;
#7989=CARTESIAN_POINT ( 'NONE',  ( 3.979198690588999998, -82.45517979992798985, 0.4013901926927000430 ) ) ;
#8005=CARTESIAN_POINT ( 'NONE',  ( -0.5518643889788126256, -85.83735716284300565, 4.438223277016693835 ) ) ;
#8089=EDGE_CURVE ( 'NONE', #35853, #313, #16069, .T. ) ;
#8090=CARTESIAN_POINT ( 'NONE',  ( -1.753806336804000221, -85.02799735065198661, -3.788636048325999983 ) ) ;
#8117=CARTESIAN_POINT ( 'NONE',  ( 1.394325645166000216, -80.85856839617498792, -3.307506794681999818 ) ) ;
#8130=CARTESIAN_POINT ( 'NONE',  ( 0.4312503660543859918, -86.36264282632897960, -4.097589455045484108 ) ) ;
#8131=CARTESIAN_POINT ( 'NONE',  ( 2.968901491624184263, -85.84407030804550232, 1.939968274069872045 ) ) ;
#8138=CARTESIAN_POINT ( 'NONE',  ( 2.747588261965000278, -81.33957009409999728, 3.083710821981000105 ) ) ;
#8141=CARTESIAN_POINT ( 'NONE',  ( 1.666332141969999903, -79.72080496681199691, 3.131277625125000075 ) ) ;
#8145=CARTESIAN_POINT ( 'NONE',  ( -3.318400460481999659, -86.11509620537599119, 0.9372051681108999333 ) ) ;
#8165=CARTESIAN_POINT ( 'NONE',  ( -3.884382724393999897, -84.62331260133198896, 1.523693970455000102 ) ) ;
#8171=CARTESIAN_POINT ( 'NONE',  ( -3.399999999999753886, -78.70000000000000284, 6.799999999999466027 ) ) ;
#8189=CARTESIAN_POINT ( 'NONE',  ( -3.406490272659980612, -78.77851879815550262, 0.06421901112149767943 ) ) ;
#8198=CARTESIAN_POINT ( 'NONE',  ( 0.6656714966510000053, -82.12580496681198383, -4.119086676869000208 ) ) ;
#8233=CARTESIAN_POINT ( 'NONE',  ( 4.000000000000000000, -78.67389998729011324, 0.000000000000000000 ) ) ;
#8234=CARTESIAN_POINT ( 'NONE',  ( 0.2486943578317000192, -85.07292953870899055, -3.538743245300000062 ) ) ;
#8251=AXIS2_PLACEMENT_3D ( 'NONE', #54486, #23181, #8722 ) ;
#8261=CARTESIAN_POINT ( 'NONE',  ( -3.547560735670414633, -86.36264283715698298, 1.500007025275827521 ) ) ;
#8277=CARTESIAN_POINT ( 'NONE',  ( 1.620688577297000110, -80.65142343270998992, -3.844466678252000058 ) ) ;
#8291=CARTESIAN_POINT ( 'NONE',  ( -3.684198380124617866, -86.09999999999999432, 1.557781209248835008 ) ) ;
#8297=CARTESIAN_POINT ( 'NONE',  ( 3.999999999999605649, -78.67389998729009903, -2.360693579763057492 ) ) ;
#8315=PRODUCT ( 'Spring', 'Spring', '', ( #42338 ) ) ;
#8371=CARTESIAN_POINT ( 'NONE',  ( 2.169073408916999846, -85.88132450217399594, 3.514774583532000118 ) ) ;
#8399=CARTESIAN_POINT ( 'NONE',  ( 0.9618768815558239593, -79.14322916213880887, -3.272074968132094863 ) ) ;
#8402=CARTESIAN_POINT ( 'NONE',  ( 3.952142091860000317, -79.77245509461999973, 0.2942162200264000216 ) ) ;
#8414=CARTESIAN_POINT ( 'NONE',  ( -2.746347158439794267, -86.07377126432851355, 2.036105618457984434 ) ) ;
#8420=CARTESIAN_POINT ( 'NONE',  ( -3.867642873348000165, -82.05721315976299479, -0.8644818823220999926 ) ) ;
#8424=CARTESIAN_POINT ( 'NONE',  ( 1.377960558539999880, -80.68280496681198599, -3.268453312188999593 ) ) ;
#8447=CARTESIAN_POINT ( 'NONE',  ( 2.283490840499000196, -82.69930595706300380, 3.492230424653999687 ) ) ;
#8453=CARTESIAN_POINT ( 'NONE',  ( -3.490339670599558630, -78.76207911824394614, -1.975393177341282946 ) ) ;
#8471=CARTESIAN_POINT ( 'NONE',  ( -2.089807409446279074, -78.91452042059378869, -3.465957297018673611 ) ) ;
#8476=ADVANCED_FACE ( 'NONE', ( #51158 ), #42206, .F. ) ;
#8484=CARTESIAN_POINT ( 'NONE',  ( -0.06117039151549000242, -79.84105496681198133, 4.172088263230999239 ) ) ;
#8520=CARTESIAN_POINT ( 'NONE',  ( 3.778552491321000240, -78.40681307243319509, 0.000000000000000000 ) ) ;
#8521=CARTESIAN_POINT ( 'NONE',  ( -0.6683785725393999178, -84.35142953870898452, 3.483937815952000250 ) ) ;
#8549=CARTESIAN_POINT ( 'NONE',  ( -2.705739474708485748, -86.31452044230000809, 3.652324231546889788 ) ) ;
#8583=CARTESIAN_POINT ( 'NONE',  ( 3.654181830570427003, -86.09999999999999432, -1.626946572303645366 ) ) ;
#8587=CARTESIAN_POINT ( 'NONE',  ( -0.03284986460708162054, -78.48547957940618858, -3.485344413137181352 ) ) ;
#8668=CARTESIAN_POINT ( 'NONE',  ( -3.886511739433000212, -84.66724735065199070, 1.524672515453000088 ) ) ;
#8699=CARTESIAN_POINT ( 'NONE',  ( -3.429316649911000159, -78.93070212325169166, 1.098603813411000107 ) ) ;
#8712=CARTESIAN_POINT ( 'NONE',  ( 2.137738514688780178, -85.88386088149393061, 2.761283067625453835 ) ) ;
#8718=CARTESIAN_POINT ( 'NONE',  ( -4.126002678693000192, -80.37756669824999278, 0.1860526405827999941 ) ) ;
#8721=CARTESIAN_POINT ( 'NONE',  ( -3.541116149846999850, -80.13275264934799225, 0.1595625314431999842 ) ) ;
#8722=DIRECTION ( 'NONE',  ( -0.9135454576429105078, 0.000000000000000000, 0.4067366430751048201 ) ) ;
#8744=CARTESIAN_POINT ( 'NONE',  ( 4.040457884044000636, -83.83275779226799784, -1.050861572499000030 ) ) ;
#8752=CARTESIAN_POINT ( 'NONE',  ( 0.8695890703638051722, -78.91427086690823955, -3.811935123611656984 ) ) ;
#8783=CARTESIAN_POINT ( 'NONE',  ( 2.485654608723999903, -79.17075264934788947, -3.354268632559000096 ) ) ;
#8804=CARTESIAN_POINT ( 'NONE',  ( 2.741068799628999741, -84.43446544543100174, 2.568638535162999670 ) ) ;
#8809=CARTESIAN_POINT ( 'NONE',  ( 2.329613959545419277, -85.25208334169079194, -2.535327851541462785 ) ) ;
#8848=CARTESIAN_POINT ( 'NONE',  ( 3.308356911591838312, -86.39318692614399708, -1.472975398279363191 ) ) ;
#8885=CARTESIAN_POINT ( 'NONE',  ( -2.060841138106245474, -78.54828564506388489, -3.417916573713450479 ) ) ;
#8939=CARTESIAN_POINT ( 'NONE',  ( 0.2669918255893000136, -82.75050405486598493, 3.534642628288999777 ) ) ;
#8964=CARTESIAN_POINT ( 'NONE',  ( 3.317493147027334555, -82.59270831520866807, 2.257618346177341806 ) ) ;
#8968=CARTESIAN_POINT ( 'NONE',  ( 3.596156905650000013, -85.76107450217398309, 2.031294216177999878 ) ) ;
#8999=CARTESIAN_POINT ( 'NONE',  ( 0.5294349409057999001, -79.41170382117660154, -3.927556981920999668 ) ) ;
#9003=ORIENTED_EDGE ( 'NONE', *, *, #50958, .F. ) ;
#9011=CARTESIAN_POINT ( 'NONE',  ( -4.367558755064909093, -86.39318692756695839, -0.4180839177783179372 ) ) ;
#9018=CARTESIAN_POINT ( 'NONE',  ( 2.458896070359999797, -79.41556330239998829, -3.318484741470999921 ) ) ;
#9023=CARTESIAN_POINT ( 'NONE',  ( 0.5659508144816000064, -82.13207046129099353, -3.502028359967999549 ) ) ;
#9044=CARTESIAN_POINT ( 'NONE',  ( 3.677350641359999450, -85.27576277546900485, -1.976537971046000042 ) ) ;
#9081=CARTESIAN_POINT ( 'NONE',  ( -3.126974709266999941, -81.88530496681200077, -2.762623496493000097 ) ) ;
#9088=CARTESIAN_POINT ( 'NONE',  ( 3.124713657347000240, -85.35108058741198533, -1.679501302629999859 ) ) ;
#9104=CARTESIAN_POINT ( 'NONE',  ( -2.415641975597000002, -83.71296544543099571, -2.876810031038000037 ) ) ;
#9110=CARTESIAN_POINT ( 'NONE',  ( -0.3497048678475328520, -85.84947917316429766, 3.392553434455469752 ) ) ;
#9147=CARTESIAN_POINT ( 'NONE',  ( 3.229228496053007103, -86.25171435493598437, 2.345485728341277554 ) ) ;
#9150=CARTESIAN_POINT ( 'NONE',  ( 3.700621377604330853, -79.35520831959095744, -1.552723024119195827 ) ) ;
#9180=CARTESIAN_POINT ( 'NONE',  ( 1.974456364586158141, -78.67390000031812747, -3.418760544059161077 ) ) ;
#9191=CARTESIAN_POINT ( 'NONE',  ( -3.661088694550203471, -78.40681307385641219, 2.068643353826707720 ) ) ;
#9233=CARTESIAN_POINT ( 'NONE',  ( -3.512421248448999833, -83.11125530066698275, 0.4773554171805000079 ) ) ;
#9261=CARTESIAN_POINT ( 'NONE',  ( 4.174305119369000394, -82.50274735065200105, -0.06567590414889999673 ) ) ;
#9291=CARTESIAN_POINT ( 'NONE',  ( -1.432040783484000102, -79.29145339669528880, -3.695292598717999866 ) ) ;
#9300=CARTESIAN_POINT ( 'NONE',  ( 0.4592281444767835619, -86.39318692756698681, -4.363424475405689229 ) ) ;
#9308=CARTESIAN_POINT ( 'NONE',  ( -3.559879492179999882, -80.05643680478300439, 2.176540992451000189 ) ) ;
#9312=CARTESIAN_POINT ( 'NONE',  ( -3.026655884748000069, -80.08782046129100252, 1.850380170909999844 ) ) ;
#9339=CARTESIAN_POINT ( 'NONE',  ( 2.242347041487000148, -85.02368520868098756, -3.468485713094000111 ) ) ;
#9350=DIRECTION ( 'NONE',  ( -0.9135454576426007556, 0.000000000000000000, 0.4067366430758003193 ) ) ;
#9353=PRODUCT_DEFINITION_FORMATION_WITH_SPECIFIED_SOURCE ( 'ANY', '', #8315, .NOT_KNOWN. ) ;
#9365=CARTESIAN_POINT ( 'NONE',  ( -4.006190475301194098, -78.85171438276198330, -2.263637441416614493 ) ) ;
#9379=CARTESIAN_POINT ( 'NONE',  ( -2.360708107464999816, -80.24142549782600042, -3.389035370063000041 ) ) ;
#9400=CARTESIAN_POINT ( 'NONE',  ( -2.308176599197000023, -83.59657450217399344, -2.748828535461000033 ) ) ;
#9403=CARTESIAN_POINT ( 'NONE',  ( -3.366989981489502348, -84.75104167658417964, -0.7261064475801897178 ) ) ;
#9470=CARTESIAN_POINT ( 'NONE',  ( -0.4881686207928203070, -86.02148120184399716, 3.925966920820129769 ) ) ;
#9473=CARTESIAN_POINT ( 'NONE',  ( -3.777881228421892335, -78.40681307243319509, 0.07122045777464609817 ) ) ;
#9485=CARTESIAN_POINT ( 'NONE',  ( 2.024107789166968985, -78.48547957940617437, 3.504731411014806230 ) ) ;
#9525=CARTESIAN_POINT ( 'NONE',  ( 0.2517727111220999792, -84.90343479341399302, -3.580552409225000066 ) ) ;
#9537=CARTESIAN_POINT ( 'NONE',  ( 3.106054555984999688, -86.09999999999999432, -1.382904586457999851 ) ) ;
#9540=CARTESIAN_POINT ( 'NONE',  ( 0.3550910806849119639, -85.83735717367099483, -7.926401815244934923 ) ) ;
#9554=CARTESIAN_POINT ( 'NONE',  ( 1.289254494606999923, -84.23117953870900010, 3.967917333274999958 ) ) ;
#9582=CARTESIAN_POINT ( 'NONE',  ( -2.725819353531988121, -80.35729165740173130, -2.104322176367662056 ) ) ;
#9584=CARTESIAN_POINT ( 'NONE',  ( -1.208807979972000179, -82.18132306546799271, -3.379724958325999840 ) ) ;
#9595=CARTESIAN_POINT ( 'NONE',  ( -3.474676814090385424, -86.08685047304777527, 2.030121440354399898 ) ) ;
#9601=CARTESIAN_POINT ( 'NONE',  ( -4.094489195923999958, -78.73368213548981487, -0.8029745938706001063 ) ) ;
#9605=CARTESIAN_POINT ( 'NONE',  ( 3.262642866299000133, -82.36630496681199531, -1.391542130826000090 ) ) ;
#9629=CARTESIAN_POINT ( 'NONE',  ( 3.013671259490000143, -83.94143147127900306, 2.824234233979999953 ) ) ;
#9656=CARTESIAN_POINT ( 'NONE',  ( 2.273238512818713808, -78.91452044229970397, -3.936100221940973309 ) ) ;
#9668=CARTESIAN_POINT ( 'NONE',  ( 2.442096516908000225, -81.92878455456799713, -3.121272388588999913 ) ) ;
#9690=CARTESIAN_POINT ( 'NONE',  ( 3.125281217184999960, -85.76107450217398309, 1.765319430424000080 ) ) ;
#9728=CARTESIAN_POINT ( 'NONE',  ( 3.723051508230308393, -86.25171438276198899, 2.704164226566200924 ) ) ;
#9759=CARTESIAN_POINT ( 'NONE',  ( 3.194290819684705962, -86.07390000031791999, 2.320109443757823797 ) ) ;
#9763=CARTESIAN_POINT ( 'NONE',  ( 3.699999999669999262, -78.39678895079168797, -2.183641561086286487 ) ) ;
#9774=CARTESIAN_POINT ( 'NONE',  ( -3.523652292752748938, -78.48547957940617437, 1.990986972659168019 ) ) ;
#9796=CARTESIAN_POINT ( 'NONE',  ( -2.473589675488696571, -83.01666668198382126, 2.395243405415722560 ) ) ;
#9818=CARTESIAN_POINT ( 'NONE',  ( -0.6860200224810000247, -83.47200654646700002, -3.477692862941000218 ) ) ;
#9832=CARTESIAN_POINT ( 'NONE',  ( -3.112536659741993894, -86.02148120184399716, 1.385790604991013142 ) ) ;
#9848=CARTESIAN_POINT ( 'NONE',  ( -3.883940484920999747, -84.59192953870899601, 1.523663816304000163 ) ) ;
#9865=VERTEX_POINT ( 'NONE', #52221 ) ;
#9874=CARTESIAN_POINT ( 'NONE',  ( 0.1004720478954561208, -79.81770832617392841, 3.442836509308329074 ) ) ;
#9888=CARTESIAN_POINT ( 'NONE',  ( 2.485958775866533355, -85.88010983227711392, 3.011055413551058990 ) ) ;
#9893=CARTESIAN_POINT ( 'NONE',  ( -2.385010427669000066, -80.41718807822699944, -3.423711137155000195 ) ) ;
#9921=CARTESIAN_POINT ( 'NONE',  ( 1.269372913341999976, -83.59225696173399456, -3.977222946407999782 ) ) ;
#9929=CARTESIAN_POINT ( 'NONE',  ( 3.992904449609000483, -78.77851881763731967, -4.889897653514886385E-16 ) ) ;
#9939=B_SPLINE_SURFACE_WITH_KNOTS ( 'NONE', 3, 3, ( 
 ( #51561, #19970, #15530, #1975, #33524, #28209, #41812, #37373, #24680, #28801, #19668, #50395, #11119, #37956, #50975, #37667, #20256, #55980, #37079, #29096, #47140, #15232, #2256, #10525, #6672, #55097, #41520, #9943, #42692, #32637, #38247, #14641, #50689, #46848, #27923 ),
 ( #46266, #56270, #1104, #32350, #6377, #33225, #45974, #5498, #51271, #24391, #10231, #19090, #5791, #42405, #23796, #1387, #19380, #55388, #14934, #32932, #28508, #46559, #6083, #24091, #42109, #1678, #55686, #26117, #39415, #52419, #47430, #20824, #24964, #44138, #33809 ),
 ( #20544, #11977, #48290, #6960, #2826, #7250, #43558, #38539, #3686, #29955, #21114, #43272, #21688, #25540, #25254, #11692, #7829, #3123, #39121, #56555, #42983, #48006, #38829, #56846, #16404, #7541, #2541, #11403, #34388, #57128, #16115, #16695, #39696, #34094, #3405 ),
 ( #52134, #29668, #51847, #48575, #47717, #25829, #34676, #12257, #12543, #52705, #52994, #30249, #43857, #21403, #29382, #15821, #16981, #30542, #8117, #17858, #45316, #13998, #40584, #466, #54166, #31996, #53280, #53576, #13410, #9584, #21974, #50037, #36149, #45018, #22572 ),
 ( #8699, #13113, #31701, #26984, #4572, #39985, #26399, #31410, #4274, #26689, #58297, #49453, #44421, #12826, #22270, #181, #30826, #18155, #27568, #57999, #4866, #40286, #35249, #13706, #49748, #45612, #27280, #22865, #35847, #53877, #5153, #17555, #36434, #57704, #54462 ),
 ( #48860, #23154, #31107, #17259, #9291, #8999, #40874, #18445, #8402, #49148, #44721, #3972, #35547, #49165, #58017, #30267, #31429, #40307, #48878, #17579, #199, #58316, #17000, #17877, #35868, #53592, #40602, #8420, #27005, #34981, #21425, #48308, #53897, #12563, #45039 ),
 ( #44740, #53010, #30561, #13131, #13428, #48592, #9018, #4593, #17278, #31127, #22589, #40002, #57721, #18174, #8718, #36167, #12277, #7848, #26709, #4291, #25848, #22291, #8138, #43875, #39433, #26418, #3424, #57440, #26138, #44159, #21709, #39715, #35268, #53300, #3991 ),
 ( #4883, #24042, #13724, #41470, #22880, #55341, #46215, #41763, #1055, #45922, #37033, #50343, #1341, #19043, #18462, #32590, #19332, #6033, #42057, #50926, #27298, #36742, #36452, #19618, #54480, #32013, #31720, #28460, #14015, #28165, #54760, #50639, #10474, #50055, #32882 ),
 ( #37326, #14885, #9601, #55048, #49767, #14303, #46508, #1628, #54186, #10187, #27586, #40891, #5170, #9308, #32296, #45629, #9893, #45333, #482, #23173, #41180, #5742, #771, #18748, #27875, #23750, #5456, #23458, #14596, #48734, #15769, #44013, #11354, #39573, #57575 ),
 ( #29050, #12424, #42355, #1923, #43732, #21567, #37908, #25987, #17139, #42643, #39284, #35123, #7703, #24631, #26280, #57295, #44294, #53156, #8277, #16858, #34839, #12703, #52869, #33473, #30413, #6328, #33762, #3849, #48448, #37616, #3284, #47089, #11069, #28752, #7989 ) ),
 .UNSPECIFIED., .F., .F., .F.,
 ( 4, 1, 1, 1, 1, 1, 1, 4 ),
 ( 4, 1, 1, 1, 1, 1, 1, 1, 1, 1, 1, 1, 1, 1, 1, 1, 1, 1, 1, 1, 1, 1, 1, 1, 1, 1, 1, 1, 1, 1, 1, 1, 4 ),
 ( -0.01000000000000000021, 0.000000000000000000, 0.1000000000000000056, 0.2000000000000000111, 0.2999999999999999889, 0.4000000000000000222, 0.5000000000000000000, 0.5100000000000000089 ),
 ( -0.02000360058914000053, 0.01249651413551000102, 0.04499662886017000152, 0.07749674358482000480, 0.1099968583094999980, 0.1424969730340999996, 0.1749970877587999907, 0.2074972024834000062, 0.2399973172080999972, 0.2724974319326999850, 0.3049975466574000316, 0.3374976613821000226, 0.3699977761066999826, 0.4024978908314000292, 0.4349980055560000447, 0.4674981202807000358, 0.4999982350052999958, 0.5324983497299999868, 0.5649984644546000023, 0.5974985791793000489, 0.6299986939038999534, 0.6624988086286000000, 0.6949989233532000155, 0.7274990380779000620, 0.7599991528025999976, 0.7924992675271999021, 0.8249993822518999487, 0.8574994969764999642, 0.8899996117012000107, 0.9224997264257999152, 0.9549998411504999618, 0.9874999558750999773, 1.020000070600000086 ),
 .UNSPECIFIED. ) ;
#9943=CARTESIAN_POINT ( 'NONE',  ( -3.462045132322999930, -81.73367725304099451, -0.7738241070029000523 ) ) ;
#9964=CARTESIAN_POINT ( 'NONE',  ( 3.319188267144999926, -79.28328455456849611, 2.165402961309999874 ) ) ;
#9969=CARTESIAN_POINT ( 'NONE',  ( -3.962812355711000212, -78.85171438276199751, -1.662781298490902161E-14 ) ) ;
#9986=B_SPLINE_SURFACE_WITH_KNOTS ( 'NONE', 3, 3, ( 
 ( #44842, #53998, #45148, #4397, #31530, #40410, #39811, #13238, #27109, #44253, #4699, #35972, #48979, #43971, #3522, #39531, #57826, #30940, #8521, #57535, #17094, #53115, #12662, #48691, #8234, #26237, #21809, #17383, #35370, #22094, #53395, #44542, #4096, #8145, #56875 ),
 ( #43883, #12003, #39439, #57446, #25854, #7854, #34702, #16143, #48314, #53016, #38277, #34120, #34415, #3712, #39145, #21138, #30273, #57154, #48036, #12284, #15850, #29982, #6987, #7566, #43299, #7278, #38855, #3429, #25566, #43012, #12569, #3149, #11431, #16719, #26144 ),
 ( #2569, #56297, #20570, #52163, #33838, #30566, #38569, #21431, #20851, #52733, #17005, #44165, #34987, #48599, #51876, #29695, #43586, #29411, #11719, #47464, #24992, #16432, #56583, #47745, #25280, #2854, #52444, #40693, #27967, #14109, #4966, #18262, #36256, #22681, #54277 ),
 ( #14394, #284, #53980, #5258, #41274, #45131, #17964, #46018, #13814, #859, #9400, #36835, #54848, #23266, #18842, #32106, #13519, #45723, #50437, #35652, #31513, #31813, #1144, #36549, #18555, #27678, #54570, #45425, #9690, #13220, #27390, #49855, #32392, #9987, #50148 ),
 ( #5539, #49559, #23549, #4380, #22974, #41563, #53681, #31215, #40984, #4682, #9104, #26797, #49253, #22381, #27093, #576, #8804, #44825, #40392, #58401, #35954, #15278, #51605, #10274, #6128, #10571, #46892, #23839, #48267, #33271, #24434, #46601, #25803, #28842, #28553 ),
 ( #28255, #20297, #11163, #6716, #29136, #41856, #33567, #24724, #47184, #14978, #14683, #16668, #5832, #34649, #30220, #42737, #24134, #52676, #55137, #38289, #32976, #42449, #32681, #51022, #56313, #15572, #12231, #50734, #42153, #51312, #7802, #1434, #43830, #56023, #6420 ),
 ( #2017, #1723, #19714, #2300, #20015, #37998, #19424, #46309, #10871, #37712, #55734, #19131, #37125, #37416, #55435, #18123, #26654, #34933, #4242, #31671, #3659, #49419, #26371, #39388, #22241, #40253, #36118, #31376, #8968, #8371, #21943, #54135, #13674, #57969, #49717 ),
 ( #53248, #49117, #9261, #57673, #145, #17827, #39955, #26953, #44985, #4540, #17229, #12798, #44389, #27246, #58264, #31080, #3941, #17525, #48829, #35514, #8668, #3378, #22542, #8090, #40554, #21372, #44689, #57393, #53543, #16953, #26086, #12515, #52966, #30514, #21662 ),
 ( #35816, #39667, #13378, #48542, #44110, #35219, #13082, #30797, #53843, #28118, #37277, #5694, #55000, #19286, #22832, #36987, #45875, #50882, #42010, #23703, #41716, #1579, #19571, #31965, #37571, #55586, #10428, #32252, #15136, #40844, #5986, #41131, #10142, #438, #725 ),
 ( #55291, #36406, #50296, #36696, #14550, #50009, #33132, #41426, #50589, #14256, #51174, #32542, #54713, #18702, #14839, #46168, #1292, #9554, #13968, #18994, #9848, #27828, #5408, #32835, #28411, #27538, #10729, #46458, #18414, #23994, #45286, #45580, #4834, #23415, #54433 ) ),
 .UNSPECIFIED., .F., .F., .F.,
 ( 4, 1, 1, 1, 1, 1, 1, 4 ),
 ( 4, 1, 1, 1, 1, 1, 1, 1, 1, 1, 1, 1, 1, 1, 1, 1, 1, 1, 1, 1, 1, 1, 1, 1, 1, 1, 1, 1, 1, 1, 1, 1, 4 ),
 ( -0.01000000000000000021, 0.000000000000000000, 0.1000000000000000056, 0.2000000000000000111, 0.2999999999999999889, 0.4000000000000000222, 0.5000000000000000000, 0.5100000000000000089 ),
 ( -0.02000000000000000042, 0.01250000000000000069, 0.04499999999999999833, 0.07749999999999999944, 0.1100000000000000006, 0.1424999999999999878, 0.1749999999999999889, 0.2074999999999999900, 0.2399999999999999911, 0.2725000000000000200, 0.3049999999999999933, 0.3375000000000000222, 0.3699999999999999956, 0.4025000000000000244, 0.4349999999999999978, 0.4675000000000000266, 0.5000000000000000000, 0.5324999999999999734, 0.5649999999999999467, 0.5975000000000000311, 0.6300000000000000044, 0.6624999999999999778, 0.6949999999999999512, 0.7275000000000000355, 0.7600000000000000089, 0.7924999999999999822, 0.8249999999999999556, 0.8575000000000000400, 0.8900000000000000133, 0.9224999999999999867, 0.9549999999999999600, 0.9874999999999000133, 1.020000000000000018 ),
 .UNSPECIFIED. ) ;
#9987=CARTESIAN_POINT ( 'NONE',  ( -3.357614552245999917, -86.32224116883999443, 0.9482802779118000291 ) ) ;
#10029=CARTESIAN_POINT ( 'NONE',  ( -1.060114799228036198, -80.51145833248038741, -3.910610943235043102 ) ) ;
#10056=CARTESIAN_POINT ( 'NONE',  ( 1.353569424327059512, -86.10000000000019327, 3.118950113984905403 ) ) ;
#10061=B_SPLINE_CURVE_WITH_KNOTS ( 'NONE', 3,
 ( #9537, #13658, #44968, #35795, #53825, #22222, #31358, #4523, #41115, #4816, #21926, #40826, #17212, #53232, #22524 ),
 .UNSPECIFIED., .F., .F.,
 ( 4, 1, 1, 1, 1, 1, 1, 1, 1, 1, 1, 1, 4 ),
 ( 0.000000000000000000, 0.08333611588665000569, 0.1666676715620999949, 0.2500039875833999781, 0.3333306964953999807, 0.4166666792817999565, 0.4999999999924999994, 0.5833333197091999933, 0.6666692694150000431, 0.7499959719902999922, 0.8333323089881000678, 0.9166638425153998959, 1.000000000000000000 ),
 .UNSPECIFIED. ) ;
#10092=CARTESIAN_POINT ( 'NONE',  ( 3.103766772394584539, -84.05729167874393681, 1.491608599317842065 ) ) ;
#10107=CARTESIAN_POINT ( 'NONE',  ( 3.979199129784999567, -82.49282046129098944, 0.4013858386831000158 ) ) ;
#10112=CARTESIAN_POINT ( 'NONE',  ( 1.948737297906999899, -85.02368520868098756, -3.014327109634999502 ) ) ;
#10139=CARTESIAN_POINT ( 'NONE',  ( 3.979318866615385364, -82.41927081334193872, -0.5157333616409632837 ) ) ;
#10142=CARTESIAN_POINT ( 'NONE',  ( -3.413772187608999698, -86.04119503318798934, 2.399116304729999705 ) ) ;
#10156=DIRECTION ( 'NONE',  ( 0.000000000000000000, 0.000000000000000000, 1.000000000000000000 ) ) ;
#10169=CARTESIAN_POINT ( 'NONE',  ( -0.3139459252241110221, -82.05312498411764466, -3.417871720250339251 ) ) ;
#10187=CARTESIAN_POINT ( 'NONE',  ( 3.494712293981999895, -79.57543510685839294, 2.279705814203000003 ) ) ;
#10191=CARTESIAN_POINT ( 'NONE',  ( -3.405576000112999768, -81.65107046129099899, 0.9932798323076000857 ) ) ;
#10210=CARTESIAN_POINT ( 'NONE',  ( -3.926978343844999664, -82.86303720588698241, 0.5336957764997000142 ) ) ;
#10218=CARTESIAN_POINT ( 'NONE',  ( 3.999999999999674927, -78.69999999999997442, -4.898587196589014454E-16 ) ) ;
#10231=CARTESIAN_POINT ( 'NONE',  ( 1.666457266735999809, -79.69568553133959199, 3.131212234982999831 ) ) ;
#10252=CARTESIAN_POINT ( 'NONE',  ( -3.037679868588000431, -78.56178455456850429, -2.545324682163999874 ) ) ;
#10274=CARTESIAN_POINT ( 'NONE',  ( -1.578055943689000040, -85.27621544543099219, -3.408973675753000254 ) ) ;
#10283=CARTESIAN_POINT ( 'NONE',  ( 3.992904449609000483, -78.77851881763731967, 0.000000000000000000 ) ) ;
#10294=DIRECTION ( 'NONE',  ( -1.000000000000000000, 0.000000000000000000, 1.400053062821000146E-14 ) ) ;
#10343=CARTESIAN_POINT ( 'NONE',  ( 1.356394222568863217, -86.02148120184399716, 3.125459129808134229 ) ) ;
#10375=CARTESIAN_POINT ( 'NONE',  ( -2.669304356624397467, -83.36354168090352346, -2.174774419161705552 ) ) ;
#10399=CARTESIAN_POINT ( 'NONE',  ( 1.861448431883999888, -85.63651402127000267, 3.016619445684999956 ) ) ;
#10412=CARTESIAN_POINT ( 'NONE',  ( 3.518657424384977084, -85.83735716284299144, -1.566607219110052629 ) ) ;
#10423=CARTESIAN_POINT ( 'NONE',  ( 0.3297891718556331120, -83.59479165932887668, -4.037289259723059409 ) ) ;
#10428=CARTESIAN_POINT ( 'NONE',  ( 3.675204158029000023, -85.31969503318799752, -1.975585186543999949 ) ) ;
#10455=CARTESIAN_POINT ( 'NONE',  ( -2.409906529986267643, -80.01041665875527542, 2.459253724518165818 ) ) ;
#10469=CARTESIAN_POINT ( 'NONE',  ( -3.234946784983960821, -86.07408421428944223, 2.385846890079581062 ) ) ;
#10474=CARTESIAN_POINT ( 'NONE',  ( 3.840130302921999750, -82.41024718738999866, -1.637848040457000165 ) ) ;
#10505=CARTESIAN_POINT ( 'NONE',  ( -3.027399109997999993, -84.54654301962300167, -2.224011006729000428 ) ) ;
#10525=CARTESIAN_POINT ( 'NONE',  ( 0.7884097517636999841, -81.25267555511598516, 3.458752693022000280 ) ) ;
#10549=CARTESIAN_POINT ( 'NONE',  ( 0.6589163185399000700, -81.92492549782599554, -4.077286533258999590 ) ) ;
#10555=CARTESIAN_POINT ( 'NONE',  ( -3.621447497675000182, -78.99318692614357929, -1.519545876029819695E-14 ) ) ;
#10571=CARTESIAN_POINT ( 'NONE',  ( 2.039338779652999811, -85.51671544543098946, -3.154751871486999981 ) ) ;
#10579=CARTESIAN_POINT ( 'NONE',  ( 3.699999999670000150, -79.00321104920828930, 0.000000000000000000 ) ) ;
#10584=CARTESIAN_POINT ( 'NONE',  ( 2.763362037843241303, -78.98488928704560408, -2.600174304222677701 ) ) ;
#10615=CARTESIAN_POINT ( 'NONE',  ( 3.374767226311075952, -81.08958333892509529, 2.240547216630219829 ) ) ;
#10640=CARTESIAN_POINT ( 'NONE',  ( -3.268206247460838210, -85.83735717367099483, 1.381888203335638332 ) ) ;
#10702=CARTESIAN_POINT ( 'NONE',  ( 1.941182638762999790, -82.69930595706300380, 2.968725317687999965 ) ) ;
#10713=CARTESIAN_POINT ( 'NONE',  ( -6.651871862604989083, -85.83735716284299144, -5.470707629659896654 ) ) ;
#10725=CARTESIAN_POINT ( 'NONE',  ( -1.356913547520186114, -85.90729168422163298, 3.776425161692174903 ) ) ;
#10729=CARTESIAN_POINT ( 'NONE',  ( 3.674832906577000013, -85.31342953870898782, -1.975385622428000199 ) ) ;
#10753=ORIENTED_EDGE ( 'NONE', *, *, #28766, .F. ) ;
#10802=CARTESIAN_POINT ( 'NONE',  ( -0.7270104252018999569, -83.22378845168798023, -3.685488592395000040 ) ) ;
#10825=FACE_OUTER_BOUND ( 'NONE', #42513, .T. ) ;
#10850=CARTESIAN_POINT ( 'NONE',  ( -0.05262135556323999791, -79.64017549782629146, 3.589006617443000202 ) ) ;
#10871=CARTESIAN_POINT ( 'NONE',  ( -4.092565674317000024, -83.35607450217399617, 0.5562462044220999324 ) ) ;
#10883=CARTESIAN_POINT ( 'NONE',  ( 1.232169104480089317, -78.93020734066399768, -3.305722366503252019 ) ) ;
#10904=CARTESIAN_POINT ( 'NONE',  ( -0.03204405817075929586, -78.69999999999998863, -3.399848993460456548 ) ) ;
#10907=CARTESIAN_POINT ( 'NONE',  ( 3.325701842495000005, -82.39999999999999147, -0.7068997487804000723 ) ) ;
#10912=CARTESIAN_POINT ( 'NONE',  ( 2.868529044229433111, -82.26510418536243208, -2.805596100957504557 ) ) ;
#10950=CARTESIAN_POINT ( 'NONE',  ( -0.03239434199580018547, -78.54828564506388489, 3.437034971988155441 ) ) ;
#10956=CARTESIAN_POINT ( 'NONE',  ( 3.325193802675403543, -82.33721875853790095, -0.7067914353816346917 ) ) ;
#10992=CARTESIAN_POINT ( 'NONE',  ( 3.133030782380000101, -82.57905554179599505, 1.663082909639999940 ) ) ;
#11018=CARTESIAN_POINT ( 'NONE',  ( 3.723742114431606520, -85.54114584694690393, 1.494555256775147889 ) ) ;
#11069=CARTESIAN_POINT ( 'NONE',  ( 3.837589733631999955, -82.33492937544698975, -1.636764466176000132 ) ) ;
#11098=CARTESIAN_POINT ( 'NONE',  ( -3.696851366990000276, -82.98328762115399115, -1.428033570587000201 ) ) ;
#11119=CARTESIAN_POINT ( 'NONE',  ( -1.757514242320000086, -79.92992088582298038, 3.081509990535999943 ) ) ;
#11144=CARTESIAN_POINT ( 'NONE',  ( -2.147119888857000003, -80.12503455456798918, -3.082407869100999953 ) ) ;
#11149=CARTESIAN_POINT ( 'NONE',  ( -3.992904449609000483, -78.77851881763731967, -1.675407828963362518E-14 ) ) ;
#11163=CARTESIAN_POINT ( 'NONE',  ( 3.962534114458999834, -82.75096544543198718, -0.06234403170014000267 ) ) ;
#11280=CARTESIAN_POINT ( 'NONE',  ( -3.302091768083000201, -84.62331260133198896, 1.295283620051000062 ) ) ;
#11303=CARTESIAN_POINT ( 'NONE',  ( -2.222528567983302228, -85.96510418484399452, 3.340687842950042619 ) ) ;
#11354=CARTESIAN_POINT ( 'NONE',  ( 3.837977427657000007, -82.34119486992599946, -1.636929820955000059 ) ) ;
#11381=CARTESIAN_POINT ( 'NONE',  ( 3.992904449609000483, -78.62148118236265759, -4.889897653514886385E-16 ) ) ;
#11403=CARTESIAN_POINT ( 'NONE',  ( -3.459349611910000011, -81.80899506498398921, -0.7732216137953999979 ) ) ;
#11405=ORIENTED_EDGE ( 'NONE', *, *, #20004, .T. ) ;
#11414=CARTESIAN_POINT ( 'NONE',  ( 2.294679948690146798, -86.17851879815597727, -3.222726853798347779 ) ) ;
#11425=CARTESIAN_POINT ( 'NONE',  ( -3.752701485998999775, -79.88453455456799190, 0.1690965569945000191 ) ) ;
#11431=CARTESIAN_POINT ( 'NONE',  ( -2.902028414455999794, -86.04119503318798934, 2.039475191455999870 ) ) ;
#11448=CARTESIAN_POINT ( 'NONE',  ( 3.106054555984999688, -86.07390000031799104, -1.382904586457999851 ) ) ;
#11459=CARTESIAN_POINT ( 'NONE',  ( 0.6796913841968065251, -78.91095482288170615, -3.420124432299513462 ) ) ;
#11491=CARTESIAN_POINT ( 'NONE',  ( -3.140159956018519161, -81.86041668085154299, -2.498940541498651413 ) ) ;
#11569=CARTESIAN_POINT ( 'NONE',  ( -3.309164444370999991, -83.30682352787700040, -1.278276416343999911 ) ) ;
#11591=FACE_OUTER_BOUND ( 'NONE', #24891, .T. ) ;
#11596=CARTESIAN_POINT ( 'NONE',  ( 3.814358451465653221, -85.36770834507991879, -1.363609372161643796 ) ) ;
#11668=CARTESIAN_POINT ( 'NONE',  ( -4.036611699677500553, -78.62148118236264338, 2.280827005624593617 ) ) ;
#11692=CARTESIAN_POINT ( 'NONE',  ( -3.178381252491000009, -80.36598997120898957, -1.569351427020000189 ) ) ;
#11715=CARTESIAN_POINT ( 'NONE',  ( -3.429377950856999924, -78.32128455456849281, 1.098412442743999851 ) ) ;
#11719=CARTESIAN_POINT ( 'NONE',  ( -0.6678581783745000111, -84.42674735065199343, 3.481225250072000232 ) ) ;
#11739=CARTESIAN_POINT ( 'NONE',  ( -2.666231078231000140, -84.50932768054498467, 3.209013417975999705 ) ) ;
#11744=CARTESIAN_POINT ( 'NONE',  ( 0.8474260888054412355, -78.91675431682378417, -3.388359286580899354 ) ) ;
#11747=SURFACE_STYLE_FILL_AREA ( #52192 ) ;
#11755=CARTESIAN_POINT ( 'NONE',  ( -3.647699726329999947, -86.17851881790099355, 1.624060543896000075 ) ) ;
#11771=CARTESIAN_POINT ( 'NONE',  ( -3.646991572042142860, -81.80260418020685620, -1.672477627614840090 ) ) ;
#11774=CARTESIAN_POINT ( 'NONE',  ( -3.559593837270000005, -80.08782046129100252, 2.176197791817000127 ) ) ;
#11832=CARTESIAN_POINT ( 'NONE',  ( -2.350111744378833301, -86.12609999968211127, 3.172282531658822791 ) ) ;
#11857=CARTESIAN_POINT ( 'NONE',  ( 3.433252676588999908, -83.90807560421097833, -0.8929367438167998827 ) ) ;
#11875=CARTESIAN_POINT ( 'NONE',  ( 3.992904449609001372, -78.62148118236265759, -1.477225460011499791E-15 ) ) ;
#11951=CARTESIAN_POINT ( 'NONE',  ( 2.322889965704379112, -78.69999999999998863, 4.022071092610017828 ) ) ;
#11977=CARTESIAN_POINT ( 'NONE',  ( -3.410021335790000219, -78.72256750329937347, 0.4933396517058999398 ) ) ;
#11991=CARTESIAN_POINT ( 'NONE',  ( 0.4177402061725503657, -86.25171435493597016, -3.969220662749826545 ) ) ;
#12000=CARTESIAN_POINT ( 'NONE',  ( -1.861195093537999945, -79.64403455456849201, 3.263022358706999970 ) ) ;
#12003=CARTESIAN_POINT ( 'NONE',  ( 3.235133317747000081, -82.35352836652198505, -1.192150282569000019 ) ) ;
#12017=CARTESIAN_POINT ( 'NONE',  ( 3.140027144888999810, -85.94828564506399005, -1.398030157551999997 ) ) ;
#12023=CARTESIAN_POINT ( 'NONE',  ( -0.7861846466844000236, -84.38907726527799014, 4.097373424592999136 ) ) ;
#12030=CARTESIAN_POINT ( 'NONE',  ( 3.399999999999725020, -78.69999999999998863, -4.163799117100664307E-16 ) ) ;
#12047=CARTESIAN_POINT ( 'NONE',  ( -0.03561181053916687156, -78.99318692756679638, -3.778384671869483125 ) ) ;
#12058=CARTESIAN_POINT ( 'NONE',  ( -3.197906501122000034, -78.88532046129088826, -2.679581358368999577 ) ) ;
#12156=CARTESIAN_POINT ( 'NONE',  ( 3.992904449609000483, -78.62148118236265759, -2.356505974700060513 ) ) ;
#12231=CARTESIAN_POINT ( 'NONE',  ( 3.490710543544000455, -85.63696544543098810, -1.876411688659999966 ) ) ;
#12234=CARTESIAN_POINT ( 'NONE',  ( 3.999999999999885425, -78.69999999999998863, 2.360693471584177860 ) ) ;
#12257=CARTESIAN_POINT ( 'NONE',  ( 3.263538630792000017, -79.53581372688118734, -1.494342973906999994 ) ) ;
#12271=CARTESIAN_POINT ( 'NONE',  ( -3.079437091258010017, -86.12609999968208285, 1.441203386403802078 ) ) ;
#12277=CARTESIAN_POINT ( 'NONE',  ( -2.360807543337999803, -80.61806754721197876, -3.388967605774999559 ) ) ;
#12280=CARTESIAN_POINT ( 'NONE',  ( -0.9782436348499000678, -81.33525264934799281, 3.407051980398000168 ) ) ;
#12284=CARTESIAN_POINT ( 'NONE',  ( -2.266693762821000213, -84.47794503318799286, 2.728307486420999961 ) ) ;
#12305=CARTESIAN_POINT ( 'NONE',  ( -0.8075256636061000082, -83.54105886393099922, -4.093650542163000061 ) ) ;
#12312=CARTESIAN_POINT ( 'NONE',  ( 0.1735539215762753051, -78.89307393851466088, -3.951712425000363460 ) ) ;
#12331=CARTESIAN_POINT ( 'NONE',  ( -3.850965819624345254, -78.96264283715740362, 0.07259824540930022441 ) ) ;
#12340=CARTESIAN_POINT ( 'NONE',  ( 0.9272595967461000344, -81.28405496681197917, 4.068200085201000071 ) ) ;
#12365=STYLED_ITEM ( 'NONE', ( #41218 ), #57583 ) ;
#12372=CARTESIAN_POINT ( 'NONE',  ( 3.325701842495000005, -82.39999999999999147, -0.7068997487804000723 ) ) ;
#12380=ORIENTED_EDGE ( 'NONE', *, *, #54345, .T. ) ;
#12402=CARTESIAN_POINT ( 'NONE',  ( 4.020839152127012817, -86.31452042059399332, 0.4615274515354030882 ) ) ;
#12424=CARTESIAN_POINT ( 'NONE',  ( -4.013587779334000238, -78.64724969135635035, 0.5806597091830999480 ) ) ;
#12437=CARTESIAN_POINT ( 'NONE',  ( -3.547560735670601595, -85.83735716284299144, 1.500007025275386097 ) ) ;
#12515=CARTESIAN_POINT ( 'NONE',  ( -1.832761557483999937, -85.98999735065198990, 3.751106806215999789 ) ) ;
#12543=CARTESIAN_POINT ( 'NONE',  ( 3.579488350411999864, -79.65606415136248586, 0.2664741063475999927 ) ) ;
#12555=CARTESIAN_POINT ( 'NONE',  ( 3.140027144888942967, -86.25171435493598437, -1.398030157552127895 ) ) ;
#12556=CARTESIAN_POINT ( 'NONE',  ( -2.014760465083978325, -86.03700509404642105, 2.765359799179270883 ) ) ;
#12563=CARTESIAN_POINT ( 'NONE',  ( 3.843843749258000209, -82.73863223182399906, -0.2533585598290000185 ) ) ;
#12567=CARTESIAN_POINT ( 'NONE',  ( 2.358048202871999788, -81.09475264934799554, 2.646615284092999509 ) ) ;
#12569=CARTESIAN_POINT ( 'NONE',  ( 0.1745084697671999974, -85.80069503318799207, 3.542747450414000188 ) ) ;
#12588=CARTESIAN_POINT ( 'NONE',  ( -3.975720615853999274, -86.19283349427999497, 0.4344903803919999974 ) ) ;
#12595=CARTESIAN_POINT ( 'NONE',  ( 3.399999999999690381, -78.72609999968184979, 6.799999999999410072 ) ) ;
#12614=CARTESIAN_POINT ( 'NONE',  ( 2.194290298650410698, -78.99318692756679638, -3.799401814995372995 ) ) ;
#12625=CARTESIAN_POINT ( 'NONE',  ( 0.6660448984561999630, -82.05675264934798463, -4.121397237571000183 ) ) ;
#12662=CARTESIAN_POINT ( 'NONE',  ( -2.859007450852999899, -84.83242953870899328, -2.100149760972999768 ) ) ;
#12685=CARTESIAN_POINT ( 'NONE',  ( 1.412628807274971088, -86.36264282632899381, 3.255037163431034219 ) ) ;
#12703=CARTESIAN_POINT ( 'NONE',  ( 3.934294415302999948, -81.01217470615398497, 1.388482249934000157 ) ) ;
#12718=CARTESIAN_POINT ( 'NONE',  ( 4.515731304085703890, -85.88547955769999476, 0.5183330846481556398 ) ) ;
#12724=CARTESIAN_POINT ( 'NONE',  ( 3.962812355710999768, -78.54828561723799396, -2.338746421483398841 ) ) ;
#12798=CARTESIAN_POINT ( 'NONE',  ( -0.8080452641954999349, -83.58499735065198877, -4.095932448746999910 ) ) ;
#12826=CARTESIAN_POINT ( 'NONE',  ( -3.204937774633000114, -80.37370721702599496, 1.959526568264000179 ) ) ;
#12837=CARTESIAN_POINT ( 'NONE',  ( -3.616440607051700340, -86.17851881763697008, 1.692525710106622894 ) ) ;
#12847=CARTESIAN_POINT ( 'NONE',  ( -2.027398468737999782, -80.44230496681200293, -2.910535655822000134 ) ) ;
#12849=CARTESIAN_POINT ( 'NONE',  ( -4.000000000000000000, -78.69999999915415856, 2.834003763004000336E-08 ) ) ;
#12868=CARTESIAN_POINT ( 'NONE',  ( -3.883990342729000123, -84.62957809581099866, 1.523540054217000117 ) ) ;
#12875=CARTESIAN_POINT ( 'NONE',  ( 3.485499217012001161, -78.91452042059381711, 6.970998434024031631 ) ) ;
#12895=CARTESIAN_POINT ( 'NONE',  ( 3.621447497674998850, -78.99318692614359350, -2.137281964302801374 ) ) ;
#12906=CARTESIAN_POINT ( 'NONE',  ( -3.200023585962000094, -78.81000264934789357, -2.681355300499000283 ) ) ;
#12942=FACE_OUTER_BOUND ( 'NONE', #43615, .T. ) ;
#12965=CARTESIAN_POINT ( 'NONE',  ( 3.618614839418587081, -86.36264283715698298, 2.628308734607720520 ) ) ;
#13004=CARTESIAN_POINT ( 'NONE',  ( -3.547719542586254882, -78.43735717367049176, 0.06688145936885296627 ) ) ;
#13082=CARTESIAN_POINT ( 'NONE',  ( -1.732973334768000084, -82.91469503318799639, 3.795637342627999899 ) ) ;
#13113=CARTESIAN_POINT ( 'NONE',  ( -3.613773621817000237, -78.97078559807879117, 0.5228172038748000183 ) ) ;
#13125=CARTESIAN_POINT ( 'NONE',  ( -3.802013078733825324, -86.17851881763698429, -2.653507570502878998 ) ) ;
#13131=CARTESIAN_POINT ( 'NONE',  ( -3.165913743354999532, -79.05481202895639115, -2.652492535831999731 ) ) ;
#13135=CARTESIAN_POINT ( 'NONE',  ( 0.4740280817681999936, -79.11955496681159161, -3.515234240849999914 ) ) ;
#13157=CARTESIAN_POINT ( 'NONE',  ( -1.734896692008999874, -84.78318437814699848, -3.748152468934999870 ) ) ;
#13164=CARTESIAN_POINT ( 'NONE',  ( -0.4969611113247792145, -78.87321456624501081, -3.919997644563975037 ) ) ;
#13186=CARTESIAN_POINT ( 'NONE',  ( 3.548349909810999847, -78.96264282632948550, -2.094141712711119485 ) ) ;
#13197=CARTESIAN_POINT ( 'NONE',  ( 3.934662594658999257, -81.04355496681199611, 1.388701755431000162 ) ) ;
#13220=CARTESIAN_POINT ( 'NONE',  ( 1.885058010937000095, -85.88132450217399594, 3.054554980983000156 ) ) ;
#13238=CARTESIAN_POINT ( 'NONE',  ( -2.847971885115999857, -83.02867953870898532, 2.115090749172999995 ) ) ;
#13265=CARTESIAN_POINT ( 'NONE',  ( -3.605449341530932106, -86.31452044229999387, 1.524483932634073335 ) ) ;
#13301=CARTESIAN_POINT ( 'NONE',  ( 3.437187628289000152, -78.54828564506388489, -2.028536691635913325 ) ) ;
#13324=( GEOMETRIC_REPRESENTATION_CONTEXT ( 3 ) GLOBAL_UNCERTAINTY_ASSIGNED_CONTEXT ( ( #24256 ) ) GLOBAL_UNIT_ASSIGNED_CONTEXT ( ( #52057, #16036, #7462 ) ) REPRESENTATION_CONTEXT ( 'NONE', 'WORKASPACE' ) );
#13351=CARTESIAN_POINT ( 'NONE',  ( 3.544224594258000405, -82.38975280906599608, -0.05576024114378000385 ) ) ;
#13378=CARTESIAN_POINT ( 'NONE',  ( 4.171964897155000074, -82.43369503318800184, -0.06563908455728000024 ) ) ;
#13400=B_SPLINE_CURVE_WITH_KNOTS ( 'NONE', 3,
 ( #10907, #51347, #51060, #41600, #50768, #28881, #19169, #24470 ),
 .UNSPECIFIED., .F., .F.,
 ( 4, 1, 1, 1, 1, 4 ),
 ( 0.000000000000000000, 0.1999938512431460313, 0.3999979371066214595, 0.6000020229700968599, 0.8000061088335723714, 1.000000000000000000 ),
 .UNSPECIFIED. ) ;
#13410=CARTESIAN_POINT ( 'NONE',  ( -2.689975106962999796, -82.06107264098699261, -2.376505205460000436 ) ) ;
#13420=CARTESIAN_POINT ( 'NONE',  ( -1.661313768260602286, -86.09999999999976694, -3.638686103992718746 ) ) ;
#13421=CARTESIAN_POINT ( 'NONE',  ( 3.626474550257886342, -85.80798832763333905, 1.029710946748257916 ) ) ;
#13428=CARTESIAN_POINT ( 'NONE',  ( -1.492427764749000074, -79.17506245343760440, -3.851117465929000172 ) ) ;
#13432=CARTESIAN_POINT ( 'NONE',  ( 2.184293099093999935, -82.17700264934799748, -2.791770796765000284 ) ) ;
#13457=CARTESIAN_POINT ( 'NONE',  ( -3.905352855690000347, -86.07743221058099437, 1.102748417664999980 ) ) ;
#13486=CARTESIAN_POINT ( 'NONE',  ( -3.999289396771957605, -78.69999999999997442, 0.07539443523754388310 ) ) ;
#13497=CARTESIAN_POINT ( 'NONE',  ( 4.116270392846000270, -80.92330496681199747, -0.6829204583257999506 ) ) ;
#13519=CARTESIAN_POINT ( 'NONE',  ( 2.619126064213000316, -84.31807450217398525, 2.454366755733000005 ) ) ;
#13536=DIRECTION ( 'NONE',  ( 0.000000000000000000, 1.000000000000000000, 0.000000000000000000 ) ) ;
#13560=CARTESIAN_POINT ( 'NONE',  ( -3.210317642309942432, -86.31452042059399332, 1.357411296278473678 ) ) ;
#13594=CARTESIAN_POINT ( 'NONE',  ( 3.437187628289001040, -78.54828564506388489, -1.267161289092433307E-15 ) ) ;
#13606=CARTESIAN_POINT ( 'NONE',  ( 3.851650068367001190, -78.43735716284257364, 2.273141292805247904 ) ) ;
#13649=CARTESIAN_POINT ( 'NONE',  ( 3.130963432471999930, -82.51000322433299061, 1.661985514006000031 ) ) ;
#13658=CARTESIAN_POINT ( 'NONE',  ( 3.106054555984999688, -86.12609999968198338, -1.382904586457999851 ) ) ;
#13674=CARTESIAN_POINT ( 'NONE',  ( -3.379129515849000231, -86.24207450217399185, 2.374770275150999588 ) ) ;
#13706=CARTESIAN_POINT ( 'NONE',  ( 0.8348675186263999626, -81.57621146183899441, 3.662562863923999767 ) ) ;
#13716=CARTESIAN_POINT ( 'NONE',  ( 0.4852795099922571631, -86.17851881763698429, -4.610955397177554538 ) ) ;
#13717=CARTESIAN_POINT ( 'NONE',  ( -0.3587980661367572432, -85.97359605476890465, 3.418821484678626010 ) ) ;
#13724=CARTESIAN_POINT ( 'NONE',  ( -4.096785958912999348, -78.80273445295348722, -0.8034250144825000328 ) ) ;
#13748=CARTESIAN_POINT ( 'NONE',  ( 0.2928406956622999768, -85.03526194493599633, -4.164595335608999527 ) ) ;
#13787=CARTESIAN_POINT ( 'NONE',  ( 3.799029931709000163, -82.16542549782599281, -1.620315315797000055 ) ) ;
#13794=CARTESIAN_POINT ( 'NONE',  ( 3.547276196037999707, -85.47133100267899408, 0.03730513092754000198 ) ) ;
#13814=CARTESIAN_POINT ( 'NONE',  ( -3.556690925232000478, -83.35607450217399617, 0.4834121147714999789 ) ) ;
#13887=CARTESIAN_POINT ( 'NONE',  ( 3.476140009346946336, -85.79678895079199208, 2.524824982687709607 ) ) ;
#13891=CARTESIAN_POINT ( 'NONE',  ( 2.236739703425203896, -78.43735716284257364, -3.872902730369248925 ) ) ;
#13902=CARTESIAN_POINT ( 'NONE',  ( -2.265513599700895053, -78.40681307243320930, 3.757367661055261987 ) ) ;
#13942=CARTESIAN_POINT ( 'NONE',  ( 2.606288821829000124, -83.58068022547898579, -2.467995869495000161 ) ) ;
#13968=CARTESIAN_POINT ( 'NONE',  ( -0.7860676397883000766, -84.35142953870898452, 4.097394633328000246 ) ) ;
#13996=CARTESIAN_POINT ( 'NONE',  ( 3.211401065378436837, -82.36145831624757818, -1.243768903017549832 ) ) ;
#13998=CARTESIAN_POINT ( 'NONE',  ( 3.384788216402000227, -81.21931966961800242, 1.194551770192000095 ) ) ;
#14009=CARTESIAN_POINT ( 'NONE',  ( -4.524698840038064773, -86.31452044229999387, -0.4331261292401809571 ) ) ;
#14010=CARTESIAN_POINT ( 'NONE',  ( 1.150732408062571599, -85.92646434825654467, 3.779866689363247545 ) ) ;
#14015=CARTESIAN_POINT ( 'NONE',  ( -3.128751238076999730, -81.92924548946498930, -2.764149595522999991 ) ) ;
#14046=CARTESIAN_POINT ( 'NONE',  ( -3.863554442403000166, -85.94560505905998582, 1.090945864652000052 ) ) ;
#14088=CARTESIAN_POINT ( 'NONE',  ( -1.334631830339999770, -81.68828455456798565, -3.731588630313000365 ) ) ;
#14109=CARTESIAN_POINT ( 'NONE',  ( 1.861591581734000078, -85.74949735065199263, 3.016529892209999897 ) ) ;
#14114=CARTESIAN_POINT ( 'NONE',  ( -3.106054822367000146, -86.10000002299598520, 1.382903988153999952 ) ) ;
#14146=CARTESIAN_POINT ( 'NONE',  ( -1.999231267869926443, -78.95052081507967046, -3.478840346404192374 ) ) ;
#14173=CARTESIAN_POINT ( 'NONE',  ( 3.380118192975979152, -85.79678895079199208, -1.504925579246046530 ) ) ;
#14176=CARTESIAN_POINT ( 'NONE',  ( 3.699999999670000594, -78.39678895079168797, -1.355252715606880543E-15 ) ) ;
#14229=CARTESIAN_POINT ( 'NONE',  ( -2.308137181837000451, -83.21992897967898273, -2.748863001877999590 ) ) ;
#14242=CARTESIAN_POINT ( 'NONE',  ( -3.620209227049993039, -85.94828561723799965, 1.611820994701015364 ) ) ;
#14256=CARTESIAN_POINT ( 'NONE',  ( -3.891865087805000289, -83.26917953870899680, -1.503306748519000147 ) ) ;
#14284=CARTESIAN_POINT ( 'NONE',  ( -2.780564399470054404, -80.04895832527154198, 2.032809336423852198 ) ) ;
#14297=CARTESIAN_POINT ( 'NONE',  ( 2.344520508141321180, -85.88574262156167549, 3.128943653696025340 ) ) ;
#14303=CARTESIAN_POINT ( 'NONE',  ( 0.5574170278374001031, -79.09443340893348307, -4.135139127346999288 ) ) ;
#14307=CARTESIAN_POINT ( 'NONE',  ( 3.383036395707000210, -82.48655496681199395, 0.3412503010523000313 ) ) ;
#14330=CARTESIAN_POINT ( 'NONE',  ( 1.255787003026999971, -83.46042981021199125, -3.934655318183000183 ) ) ;
#14338=CARTESIAN_POINT ( 'NONE',  ( 3.914500761937001361, -78.91452044229970397, 7.829001523874034696 ) ) ;
#14372=CARTESIAN_POINT ( 'NONE',  ( -2.914365214892999933, -81.32367549782598815, 2.926598508534000054 ) ) ;
#14394=CARTESIAN_POINT ( 'NONE',  ( 2.986994850445999994, -82.51432450217399150, -1.707899905183000167 ) ) ;
#14398=CARTESIAN_POINT ( 'NONE',  ( 3.409064975549345178, -85.48333334097100078, 0.4838537520227722544 ) ) ;
#14433=CARTESIAN_POINT ( 'NONE',  ( -3.851650068366999857, -78.43735716283408976, 2.793213950329999913E-10 ) ) ;
#14437=CARTESIAN_POINT ( 'NONE',  ( -3.990537183407945498, -80.24166666280596871, -0.6977800654927414081 ) ) ;
#14466=CARTESIAN_POINT ( 'NONE',  ( -3.165820273081872305, -85.94828564506399005, 1.338596575002511724 ) ) ;
#14500=CARTESIAN_POINT ( 'NONE',  ( 3.416150720453857481, -83.98020834565045334, 0.4395479122176694786 ) ) ;
#14518=CARTESIAN_POINT ( 'NONE',  ( -3.126658837318000206, -81.89157046129098205, -2.762344429551999880 ) ) ;
#14522=CARTESIAN_POINT ( 'NONE',  ( -1.575900344810000187, -85.74518770028200265, 3.224971915196999994 ) ) ;
#14534=CARTESIAN_POINT ( 'NONE',  ( -3.140027144888994037, -85.94828564506399005, 1.398030157552013319 ) ) ;
#14550=CARTESIAN_POINT ( 'NONE',  ( 2.283273990875999804, -82.66792953870898941, 3.491867166086000118 ) ) ;
#14564=DIRECTION ( 'NONE',  ( 1.000000000000000000, 0.000000000000000000, 0.000000000000000000 ) ) ;
#14576=CARTESIAN_POINT ( 'NONE',  ( 3.177654278060972448, -79.35520832797827495, -1.327594666548604252 ) ) ;
#14591=CARTESIAN_POINT ( 'NONE',  ( 2.336986715456273789, -85.88603725345878104, 3.134951688163078121 ) ) ;
#14596=CARTESIAN_POINT ( 'NONE',  ( -3.126997180111000141, -81.86019317200199907, -2.762599942562999900 ) ) ;
#14600=CARTESIAN_POINT ( 'NONE',  ( 2.112107237196000131, -79.24607046129089838, -2.850184828360999845 ) ) ;
#14624=CARTESIAN_POINT ( 'NONE',  ( 1.224557693228000010, -83.94529094328899532, 3.769144257100999873 ) ) ;
#14631=CARTESIAN_POINT ( 'NONE',  ( 3.914500761937000028, -78.91452044229970397, -4.793880828366022505E-16 ) ) ;
#14641=CARTESIAN_POINT ( 'NONE',  ( 2.185988871226999475, -82.21467895096598966, -2.793952356700000195 ) ) ;
#14662=CARTESIAN_POINT ( 'NONE',  ( 3.909635449501999815, -80.60603455456799793, -0.6486381549911000022 ) ) ;
#14683=CARTESIAN_POINT ( 'NONE',  ( -2.548476486054999768, -83.71296544543099571, -3.035003859434000084 ) ) ;
#14691=CARTESIAN_POINT ( 'NONE',  ( 3.485499217011999828, -78.91452042059380290, 0.000000000000000000 ) ) ;
#14725=CARTESIAN_POINT ( 'NONE',  ( -4.000000000000000000, -78.69999999915415856, 2.834003763004000336E-08 ) ) ;
#14734=CARTESIAN_POINT ( 'NONE',  ( -3.241578942234993654, -85.83735717367099483, 1.443243930775013784 ) ) ;
#14750=CARTESIAN_POINT ( 'NONE',  ( 4.358902656273643039, -85.80681307243297340, 0.5003316865781948231 ) ) ;
#14768=CARTESIAN_POINT ( 'NONE',  ( -3.777881236680218358, -78.40681307243319509, -0.07122001971131411424 ) ) ;
#14789=CARTESIAN_POINT ( 'NONE',  ( -2.832192856027651917, -83.05520834853042800, 1.959254550120464566 ) ) ;
#14807=CARTESIAN_POINT ( 'NONE',  ( 4.046592082650999345, -82.45273712795798815, -0.2667243773544999974 ) ) ;
#14811=CARTESIAN_POINT ( 'NONE',  ( 3.235517445292999561, -82.38490367749800214, -1.192293695388999986 ) ) ;
#14822=CARTESIAN_POINT ( 'NONE',  ( -6.908074975177432187, -86.07389998728979208, -5.681417088837856788 ) ) ;
#14831=EDGE_CURVE ( 'NONE', #521, #36712, #39382, .T. ) ;
#14836=CARTESIAN_POINT ( 'NONE',  ( -1.852268148096546385, -82.93958331894259572, 3.560113889582741997 ) ) ;
#14839=CARTESIAN_POINT ( 'NONE',  ( 4.037760978116000210, -83.87042953870898998, -1.050253016718000199 ) ) ;
#14865=CARTESIAN_POINT ( 'NONE',  ( 1.691954025052836430, -79.70208332662505768, 2.999979231498003163 ) ) ;
#14880=CARTESIAN_POINT ( 'NONE',  ( 1.775602382380404354, -85.90660159999292489, 3.534306991046110014 ) ) ;
#14885=CARTESIAN_POINT ( 'NONE',  ( -4.013993253630999902, -78.65351518583565849, 0.5807183705604999080 ) ) ;
#14889=CARTESIAN_POINT ( 'NONE',  ( 3.345231861902000059, -81.04982046129099160, 1.180667782100000007 ) ) ;
#14914=CARTESIAN_POINT ( 'NONE',  ( -3.724867944340000125, -84.42629260435599292, -0.4865481737740000034 ) ) ;
#14934=CARTESIAN_POINT ( 'NONE',  ( 1.377877372877000184, -80.65768892718899963, -3.268489530280999755 ) ) ;
#14958=CARTESIAN_POINT ( 'NONE',  ( -3.888905289927000020, -78.44153455456849144, -0.7628755026328000177 ) ) ;
#14964=CARTESIAN_POINT ( 'NONE',  ( -4.000000000000000000, -78.69999999915415856, 2.834003763004000336E-08 ) ) ;
#14978=CARTESIAN_POINT ( 'NONE',  ( -3.696868630880000062, -83.59271544543099708, -1.427985666462000092 ) ) ;
#15025=CARTESIAN_POINT ( 'NONE',  ( 2.793917098883578642, -79.25885415185018701, -2.879926396557028312 ) ) ;
#15052=CARTESIAN_POINT ( 'NONE',  ( 3.451879464910978079, -85.80681307243298761, -1.536875756006047533 ) ) ;
#15106=CARTESIAN_POINT ( 'NONE',  ( 3.088334425740999922, -85.58531592346599837, 1.744636951369000100 ) ) ;
#15119=CARTESIAN_POINT ( 'NONE',  ( 3.576074390005976156, -85.88547955769999476, -1.592170899228053438 ) ) ;
#15131=CARTESIAN_POINT ( 'NONE',  ( -3.970500524723944213, -83.24791665559489218, -0.8021306198144204647 ) ) ;
#15136=CARTESIAN_POINT ( 'NONE',  ( 3.633024531674999835, -85.56019503318798058, 2.052118945875000211 ) ) ;
#15163=CARTESIAN_POINT ( 'NONE',  ( 1.047413828337867114, -82.14947915040829685, -3.245710299348970818 ) ) ;
#15178=CARTESIAN_POINT ( 'NONE',  ( 2.094528727916130872, -85.89549859647340213, 3.327249167043359268 ) ) ;
#15212=CARTESIAN_POINT ( 'NONE',  ( -3.504159990688000104, -82.98328762115399115, -1.353600025171000087 ) ) ;
#15232=CARTESIAN_POINT ( 'NONE',  ( 3.345256759276000302, -81.01217470615398497, 1.180600418122999873 ) ) ;
#15259=CARTESIAN_POINT ( 'NONE',  ( -3.276814203403000114, -78.43767549782629089, 1.049547044727999978 ) ) ;
#15278=CARTESIAN_POINT ( 'NONE',  ( -3.724883260595999612, -85.03571544543099492, -0.4864224331464999662 ) ) ;
#15286=CARTESIAN_POINT ( 'NONE',  ( 4.043181936102999252, -84.02832601947699231, 1.029191484053000094 ) ) ;
#15292=CARTESIAN_POINT ( 'NONE',  ( 2.595899973196303723, -78.97680030866433754, -2.796371309837623720 ) ) ;
#15326=CARTESIAN_POINT ( 'NONE',  ( 0.2808874063080823991, -82.09166668342933804, -4.003087784603879484 ) ) ;
#15368=CARTESIAN_POINT ( 'NONE',  ( 3.407095545933004122, -78.62148120184446043, -4.172488654716057829E-16 ) ) ;
#15375=CARTESIAN_POINT ( 'NONE',  ( 3.872097870353349514, -82.21166587810114379, -0.8230394299192180796 ) ) ;
#15409=CARTESIAN_POINT ( 'NONE',  ( -2.847992527146999908, -83.06632269734298291, 2.115064691465000202 ) ) ;
#15432=CARTESIAN_POINT ( 'NONE',  ( -3.296924740810961207, -83.05520832018719091, 2.288194650150326748 ) ) ;
#15510=CARTESIAN_POINT ( 'NONE',  ( 3.840603960130999806, -83.70479011275499204, 0.9776252842081999406 ) ) ;
#15530=CARTESIAN_POINT ( 'NONE',  ( -3.481115695920999897, -78.72741664101050674, -0.6826852699798000579 ) ) ;
#15554=CARTESIAN_POINT ( 'NONE',  ( -3.062422382194999848, -79.88067549782599031, 1.872246422039999914 ) ) ;
#15572=CARTESIAN_POINT ( 'NONE',  ( 2.151480633118999730, -85.51671544543098946, -3.328229532786999734 ) ) ;
#15585=CARTESIAN_POINT ( 'NONE',  ( -3.399999999999706812, -78.71338090247236607, -0.3817310692536478589 ) ) ;
#15593=B_SPLINE_CURVE_WITH_KNOTS ( 'NONE', 3,
 ( #43393, #39242, #2387, #15375, #56113, #56688, #33654, #10956, #7377, #16245 ),
 .UNSPECIFIED., .F., .F.,
 ( 4, 1, 1, 1, 1, 1, 1, 4 ),
 ( 0.000000000000000000, 1.019445619974785175E-05, 0.2000061087224714595, 0.4000020229887432111, 0.5999979372550151568, 0.7999938515212868806, 0.9999897657875587154, 1.000000000000000000 ),
 .UNSPECIFIED. ) ;
#15608=CARTESIAN_POINT ( 'NONE',  ( -2.038544480927432900, -78.72609999968184979, -3.380937442862103737 ) ) ;
#15641=CARTESIAN_POINT ( 'NONE',  ( -3.437217408589642531, -78.70000000000000284, -1.942147800595412255 ) ) ;
#15653=CARTESIAN_POINT ( 'NONE',  ( -3.437217181655296105, -78.67390000031815589, 1.942148107221360220 ) ) ;
#15697=CARTESIAN_POINT ( 'NONE',  ( 1.078481765258000102, -83.66130927919799376, -3.379119232009999418 ) ) ;
#15720=CARTESIAN_POINT ( 'NONE',  ( 3.514163197055722776, -83.82604166181818073, -2.015118541338928981 ) ) ;
#15769=CARTESIAN_POINT ( 'NONE',  ( 0.6656542303264000315, -82.10069402096399926, -4.119090728389999789 ) ) ;
#15783=B_SPLINE_CURVE_WITH_KNOTS ( 'NONE', 3,
 ( #27428, #32143, #45463, #23010, #896, #41021, #54883, #18594, #36584, #14433, #32428, #43066, #24472, #56638, #2902 ),
 .UNSPECIFIED., .F., .F.,
 ( 4, 1, 1, 1, 1, 1, 1, 1, 1, 1, 1, 1, 4 ),
 ( 0.000000000000000000, 0.08333611588665000569, 0.1666676715620999949, 0.2500039875833999781, 0.3333306964953999807, 0.4166666792817999565, 0.4999999999924999994, 0.5833333197091999933, 0.6666692694150000431, 0.7499959719902999922, 0.8333323089881000678, 0.9166638425153998959, 1.000000000000000000 ),
 .UNSPECIFIED. ) ;
#15819=( BOUNDED_SURFACE ( )  B_SPLINE_SURFACE ( 3, 3, ( 
 ( #33311, #19752, #37748, #10904, #46927, #6454, #24469 ),
 ( #56062, #42482, #15608, #48645, #35619, #39186, #16479 ),
 ( #8189, #22046, #17331, #43632, #30028, #4042, #40053 ),
 ( #26468, #47791, #44491, #35320, #30896, #3195, #53062 ),
 ( #30317, #58070, #8471, #7322, #26190, #21185, #56921 ),
 ( #53646, #48358, #25611, #7898, #17630, #13186, #48929 ),
 ( #39763, #25324, #52777, #7611, #53349, #12895, #57201 ),
 ( #43341, #25900, #2898, #21477, #20898, #38901, #34459 ),
 ( #16769, #21758, #52490, #12047, #12614, #48081, #34748 ),
 ( #12331, #43924, #44208, #3471, #17050, #39484, #57486 ),
 ( #35030, #30611, #3758, #57776, #9656, #45981, #45685 ),
 ( #58367, #9365, #19097, #32070, #41527, #36510, #40657 ),
 ( #22344, #50111, #35919, #27931, #1112, #247, #23517 ),
 ( #18231, #53950, #27355, #5225, #40359, #36220, #22647 ),
 ( #13486, #37087, #55105, #22937, #54534, #40949, #540 ) ),
 .UNSPECIFIED., .F., .F., .T. ) 
 B_SPLINE_SURFACE_WITH_KNOTS ( ( 4, 1, 1, 1, 1, 1, 1, 1, 1, 1, 1, 1, 4 ),
 ( 4, 3, 4 ),
 ( 0.009836338020448129327, 0.09153385889397000486, 0.1732268882812000033, 0.2549245844128000260, 0.3366128623372000028, 0.4183102317861999708, 0.5000049915032999115, 0.5816997502458999270, 0.6633970872647999562, 0.7450853589770999319, 0.8267830756728000718, 0.9084760833474000430, 0.9901736249421290159 ),
 ( 0.000000000000000000, 0.5000000000000000000, 1.000000000000000000 ),
 .UNSPECIFIED. ) 
 GEOMETRIC_REPRESENTATION_ITEM ( )  RATIONAL_B_SPLINE_SURFACE ( (
 ( 1.000000000000000000, 0.8025111667134329219, 0.8025111667134329219, 1.000000000000000000, 0.8025111667134329219, 0.8025111667134329219, 1.000000000000000000),
 ( 1.000000000000000000, 0.8025111667134329219, 0.8025111667134329219, 1.000000000000000000, 0.8025111667134329219, 0.8025111667134329219, 1.000000000000000000),
 ( 1.000000000000000000, 0.8025111667134329219, 0.8025111667134329219, 1.000000000000000000, 0.8025111667134329219, 0.8025111667134329219, 1.000000000000000000),
 ( 1.000000000000000000, 0.8025111667134329219, 0.8025111667134329219, 1.000000000000000000, 0.8025111667134329219, 0.8025111667134329219, 1.000000000000000000),
 ( 1.000000000000000000, 0.8025111667134329219, 0.8025111667134329219, 1.000000000000000000, 0.8025111667134329219, 0.8025111667134329219, 1.000000000000000000),
 ( 1.000000000000000000, 0.8025111667134329219, 0.8025111667134329219, 1.000000000000000000, 0.8025111667134329219, 0.8025111667134329219, 1.000000000000000000),
 ( 1.000000000000000000, 0.8025111667134329219, 0.8025111667134329219, 1.000000000000000000, 0.8025111667134329219, 0.8025111667134329219, 1.000000000000000000),
 ( 1.000000000000000000, 0.8025111667134329219, 0.8025111667134329219, 1.000000000000000000, 0.8025111667134329219, 0.8025111667134329219, 1.000000000000000000),
 ( 1.000000000000000000, 0.8025111667134329219, 0.8025111667134329219, 1.000000000000000000, 0.8025111667134329219, 0.8025111667134329219, 1.000000000000000000),
 ( 1.000000000000000000, 0.8025111667134329219, 0.8025111667134329219, 1.000000000000000000, 0.8025111667134329219, 0.8025111667134329219, 1.000000000000000000),
 ( 1.000000000000000000, 0.8025111667134329219, 0.8025111667134329219, 1.000000000000000000, 0.8025111667134329219, 0.8025111667134329219, 1.000000000000000000),
 ( 1.000000000000000000, 0.8025111667134329219, 0.8025111667134329219, 1.000000000000000000, 0.8025111667134329219, 0.8025111667134329219, 1.000000000000000000),
 ( 1.000000000000000000, 0.8025111667134329219, 0.8025111667134329219, 1.000000000000000000, 0.8025111667134329219, 0.8025111667134329219, 1.000000000000000000),
 ( 1.000000000000000000, 0.8025111667134329219, 0.8025111667134329219, 1.000000000000000000, 0.8025111667134329219, 0.8025111667134329219, 1.000000000000000000),
 ( 1.000000000000000000, 0.8025111667134329219, 0.8025111667134329219, 1.000000000000000000, 0.8025111667134329219, 0.8025111667134329219, 1.000000000000000000) ) ) 
 REPRESENTATION_ITEM ( '' )  SURFACE ( )  );
#15821=CARTESIAN_POINT ( 'NONE',  ( -3.218446570455000266, -80.49781712273099288, -1.589134001521000039 ) ) ;
#15834=CARTESIAN_POINT ( 'NONE',  ( -3.237453996416787216, -86.09999999999998010, -2.259489515356280620 ) ) ;
#15845=CARTESIAN_POINT ( 'NONE',  ( -1.265066673746999770, -81.68828455456798565, -3.537086639947999878 ) ) ;
#15850=CARTESIAN_POINT ( 'NONE',  ( -3.302049379960999786, -84.59819503318799150, 1.295388840129999997 ) ) ;
#15855=EDGE_CURVE ( 'NONE', #313, #26598, #20542, .T. ) ;
#15878=CARTESIAN_POINT ( 'NONE',  ( 0.05072268191597268522, -78.88976567714485100, -3.472900191114431490 ) ) ;
#15978=UNCERTAINTY_MEASURE_WITH_UNIT (LENGTH_MEASURE( 1.000000000000000082E-05 ), #33736, 'distance_accuracy_value', 'NONE');
#15990=CARTESIAN_POINT ( 'NONE',  ( -2.280909059783999826, -83.42080844866399048, -2.716435822977000036 ) ) ;
#16014=CARTESIAN_POINT ( 'NONE',  ( 3.915023737200626908, -85.50260417986531536, 0.8776777806838870211 ) ) ;
#16036=( NAMED_UNIT ( * ) PLANE_ANGLE_UNIT ( ) SI_UNIT ( $, .RADIAN. ) );
#16056=CARTESIAN_POINT ( 'NONE',  ( 3.654181830570521594, -86.09999999999978115, -1.626946572303536120 ) ) ;
#16063=APPLICATION_CONTEXT ( 'automotive_design' ) ;
#16069=B_SPLINE_CURVE_WITH_KNOTS ( 'NONE', 3,
 ( #14964, #24711, #11149, #9969, #45999, #32961, #1704, #51006, #10555, #28538, #46586, #6111, #42137, #19999, #56009 ),
 .UNSPECIFIED., .F., .F.,
 ( 4, 1, 1, 1, 1, 1, 1, 1, 1, 1, 1, 1, 4 ),
 ( 0.000000000000000000, 0.08333615652962080012, 0.1666676882018690575, 0.2500040233444769111, 0.3333307240648036851, 0.4166666719153997445, 0.4999999897769762947, 0.5833333086325983574, 0.6666692895637478244, 0.7499959966207713213, 0.8333323107868229052, 0.9166638646071934016, 1.000000000000000000 ),
 .UNSPECIFIED. ) ;
#16091=CARTESIAN_POINT ( 'NONE',  ( -3.999289405514205864, -78.67389998729011324, -0.07539397150087834287 ) ) ;
#16115=CARTESIAN_POINT ( 'NONE',  ( 0.5654955014232999622, -82.16974633842799847, -3.499305150839000067 ) ) ;
#16128=CARTESIAN_POINT ( 'NONE',  ( 3.106054555984424148, -86.12609999968211127, -1.382904586457713858 ) ) ;
#16139=CARTESIAN_POINT ( 'NONE',  ( 3.843843246054999607, -82.12920122123499311, -0.2533605254773000359 ) ) ;
#16143=CARTESIAN_POINT ( 'NONE',  ( -2.847633505915000196, -83.03494503318799502, 2.114839446580000004 ) ) ;
#16165=CARTESIAN_POINT ( 'NONE',  ( -4.134529906664000443, -83.18030761812998719, 0.5619030602642999250 ) ) ;
#16170=CARTESIAN_POINT ( 'NONE',  ( 1.550761107483941137, -78.94176543215372988, -3.175578139143914846 ) ) ;
#16172=EDGE_CURVE ( 'NONE', #313, #35853, #28375, .T. ) ;
#16186=ADVANCED_FACE ( 'NONE', ( #48624 ), #19506, .T. ) ;
#16200=CARTESIAN_POINT ( 'NONE',  ( -3.300976773589475499, -81.55208334408089854, 2.347730810921812239 ) ) ;
#16203=CARTESIAN_POINT ( 'NONE',  ( -2.943945732315000008, -81.53082046129100036, 2.956303192671000168 ) ) ;
#16237=CARTESIAN_POINT ( 'NONE',  ( -3.406490280106461377, -78.62148120184446043, -0.06421861612271693998 ) ) ;
#16245=CARTESIAN_POINT ( 'NONE',  ( 3.325701842495000005, -82.39999999999999147, -0.7068997487804000723 ) ) ;
#16263=CARTESIAN_POINT ( 'NONE',  ( 3.106054555984939736, -86.09999999999998010, -1.382904586457970986 ) ) ;
#16307=CARTESIAN_POINT ( 'NONE',  ( -2.398287624620491609, -78.67389998729009903, -3.977573462190680420 ) ) ;
#16310=CARTESIAN_POINT ( 'NONE',  ( 3.541116439658829496, -85.32916667799834443, -1.969010436737064662 ) ) ;
#16379=CARTESIAN_POINT ( 'NONE',  ( 3.999999999999884537, -78.69999999999998863, -4.898587196589271820E-16 ) ) ;
#16404=CARTESIAN_POINT ( 'NONE',  ( -0.9781931330616999709, -81.44824379153999416, 3.407067580805999807 ) ) ;
#16418=CARTESIAN_POINT ( 'NONE',  ( 2.289901096215520404, -86.12609999968211127, -3.216015270247588820 ) ) ;
#16428=CARTESIAN_POINT ( 'NONE',  ( -3.205004355390999926, -79.76428455456799327, 1.959415517562000053 ) ) ;
#16432=CARTESIAN_POINT ( 'NONE',  ( -3.514866375491000117, -84.78749735065200355, -0.4589968959933000137 ) ) ;
#16453=CARTESIAN_POINT ( 'NONE',  ( -3.413555124258999651, -86.07258307901300043, 2.398694242656000064 ) ) ;
#16459=CARTESIAN_POINT ( 'NONE',  ( -3.399999999999725020, -78.69999999999998863, -1.426627331148077631E-14 ) ) ;
#16460=VERTEX_POINT ( 'NONE', #41414 ) ;
#16479=CARTESIAN_POINT ( 'NONE',  ( 3.399999999999690381, -78.72609999968184979, -1.260385025514398905E-15 ) ) ;
#16527=CARTESIAN_POINT ( 'NONE',  ( 3.548349909811000291, -78.43735717367049176, 0.000000000000000000 ) ) ;
#16548=CARTESIAN_POINT ( 'NONE',  ( 3.922208058606298842, -86.12609999968211127, 0.4502061935811673132 ) ) ;
#16588=CARTESIAN_POINT ( 'NONE',  ( 2.322889840689294161, -78.67389998729009903, -4.022071228304369583 ) ) ;
#16613=SURFACE_STYLE_USAGE ( .BOTH. , #21319 ) ;
#16640=CARTESIAN_POINT ( 'NONE',  ( 0.000000000000000000, -78.69999999999998863, 0.000000000000000000 ) ) ;
#16668=CARTESIAN_POINT ( 'NONE',  ( -0.7670514813460999060, -83.83321544543098014, -3.888137449123000078 ) ) ;
#16695=CARTESIAN_POINT ( 'NONE',  ( 2.184286877926000070, -82.28999676290898435, -2.791777007933000210 ) ) ;
#16707=CARTESIAN_POINT ( 'NONE',  ( 0.4132205903735213237, -86.12609999968209706, -3.926276861430695320 ) ) ;
#16717=CARTESIAN_POINT ( 'NONE',  ( -0.05196629067518999945, -79.77200264934798213, 3.544328326796999828 ) ) ;
#16719=CARTESIAN_POINT ( 'NONE',  ( -3.318006187736000090, -86.12136169985498668, 0.9370938149272999285 ) ) ;
#16741=CARTESIAN_POINT ( 'NONE',  ( 2.191142140121999926, -85.70556633873299290, 3.550913296835999766 ) ) ;
#16749=CARTESIAN_POINT ( 'NONE',  ( 3.621447497675000182, -78.99318692614357929, -4.434994086307880463E-16 ) ) ;
#16763=CARTESIAN_POINT ( 'NONE',  ( -3.106054822367000146, -86.12610002267798848, 1.382903988153999952 ) ) ;
#16769=CARTESIAN_POINT ( 'NONE',  ( -3.777881228421892335, -78.99318692756679638, 0.07122045777464609817 ) ) ;
#16778=CARTESIAN_POINT ( 'NONE',  ( -0.06120470443819999579, -79.77200264934798213, 4.174428554646000045 ) ) ;
#16836=PRODUCT_DEFINITION_CONTEXT ( 'detailed design', #16063, 'design' ) ;
#16838=CARTESIAN_POINT ( 'NONE',  ( -2.452652587122145178, -86.36264282632899381, 3.310696598561635451 ) ) ;
#16858=CARTESIAN_POINT ( 'NONE',  ( 3.275019288765999903, -80.77167385719099002, -2.584725161986999975 ) ) ;
#16953=CARTESIAN_POINT ( 'NONE',  ( 2.192539838120000084, -85.74949735065199263, 3.552799672304999934 ) ) ;
#16978=CARTESIAN_POINT ( 'NONE',  ( -3.399999999999999911, -78.69999997992952956, 5.715921273723000819E-07 ) ) ;
#16981=CARTESIAN_POINT ( 'NONE',  ( -2.051686749538000232, -80.61806754721197876, -2.945220990589999754 ) ) ;
#16994=CARTESIAN_POINT ( 'NONE',  ( 2.289901096216106158, -86.09999999999999432, -3.216015270247992497 ) ) ;
#16995=CARTESIAN_POINT ( 'NONE',  ( -2.951654015434272971, -86.08669351303142037, 1.729693878444511501 ) ) ;
#17000=CARTESIAN_POINT ( 'NONE',  ( 2.636414666285999964, -81.45596103735698534, 2.958936952162999567 ) ) ;
#17003=CARTESIAN_POINT ( 'NONE',  ( -1.757416575686000071, -79.96130496681199418, 3.081079248453999941 ) ) ;
#17005=CARTESIAN_POINT ( 'NONE',  ( -2.279442914376999862, -83.46474735065199013, -2.714609328494999474 ) ) ;
#17024=CARTESIAN_POINT ( 'NONE',  ( 3.687576869571000060, -82.51000322433299061, 1.957448392864999720 ) ) ;
#17041=CARTESIAN_POINT ( 'NONE',  ( -3.241578944612999891, -86.36264282653499436, 1.443243925434000152 ) ) ;
#17050=CARTESIAN_POINT ( 'NONE',  ( 2.236739703425203896, -78.96264283715740362, -3.872902730369248925 ) ) ;
#17059=CARTESIAN_POINT ( 'NONE',  ( -4.074332639539999690, -81.69600264934798872, -0.9107214065898999733 ) ) ;
#17094=CARTESIAN_POINT ( 'NONE',  ( -3.302441756588000210, -84.59192953870899601, 1.295542768871000172 ) ) ;
#17118=CARTESIAN_POINT ( 'NONE',  ( 1.504274447196719100, -86.39318692756698681, 3.466210801031044397 ) ) ;
#17139=CARTESIAN_POINT ( 'NONE',  ( 4.160603301095000539, -79.44891918789778629, 0.3097350621069000498 ) ) ;
#17152=CARTESIAN_POINT ( 'NONE',  ( 4.571463104798920263, -85.94828561723799965, 0.5247301960423848000 ) ) ;
#17157=CARTESIAN_POINT ( 'NONE',  ( -3.999289396771888327, -78.67389998729011324, 0.07539443523754257859 ) ) ;
#17212=CARTESIAN_POINT ( 'NONE',  ( 3.647699722741000183, -86.17851881763699851, -1.624060551956000076 ) ) ;
#17229=CARTESIAN_POINT ( 'NONE',  ( -2.684675547274000262, -83.46474735065199013, -3.197204561977000203 ) ) ;
#17256=CARTESIAN_POINT ( 'NONE',  ( 0.1493788696755103118, -79.08541666236438061, -3.407719317120471825 ) ) ;
#17259=CARTESIAN_POINT ( 'NONE',  ( -3.037813758603999936, -79.17120297221410397, -2.545166726939000146 ) ) ;
#17271=CARTESIAN_POINT ( 'NONE',  ( -1.658366784370784108, -86.17851881763698429, -3.632231483840216768 ) ) ;
#17272=CARTESIAN_POINT ( 'NONE',  ( 3.401880147206532978, -85.81571308423876587, 1.208734972710103328 ) ) ;
#17278=CARTESIAN_POINT ( 'NONE',  ( 4.118797911448999649, -79.65606415136248586, 0.3066228704314999942 ) ) ;
#17281=CARTESIAN_POINT ( 'NONE',  ( 3.423421051771000201, -82.28567549782599144, 0.3453239421332999770 ) ) ;
#17307=CARTESIAN_POINT ( 'NONE',  ( -3.902769136194000232, -86.15275002252400327, 1.102018856806000091 ) ) ;
#17313=CARTESIAN_POINT ( 'NONE',  ( -3.621447497675031268, -78.99318692614360771, 7.242894995350018128 ) ) ;
#17331=CARTESIAN_POINT ( 'NONE',  ( -2.042798770927879648, -78.77851879815550262, -3.387993206663126866 ) ) ;
#17343=CARTESIAN_POINT ( 'NONE',  ( -3.973290944682999370, -78.47775883115959061, 0.5746058003935000658 ) ) ;
#17383=CARTESIAN_POINT ( 'NONE',  ( 3.547276804185000021, -85.43367953870898646, 0.03714848770851999354 ) ) ;
#17408=CARTESIAN_POINT ( 'NONE',  ( -2.503178322334999262, -86.39318692614398287, 3.378898422409667202 ) ) ;
#17440=CARTESIAN_POINT ( 'NONE',  ( -2.705739474708930281, -85.88547955769999476, 3.652324231546577149 ) ) ;
#17445=CARTESIAN_POINT ( 'NONE',  ( -3.620804144604786057, -78.40681307385639798, 0.06825924720741134710 ) ) ;
#17525=CARTESIAN_POINT ( 'NONE',  ( 1.290108009600000161, -84.30649735065199479, 3.970544182317999660 ) ) ;
#17551=CARTESIAN_POINT ( 'NONE',  ( -1.699346936231083793, -78.95052082955746187, -2.957013875707059647 ) ) ;
#17555=CARTESIAN_POINT ( 'NONE',  ( 2.314800267987999760, -82.53821485768798993, -2.958588558779999822 ) ) ;
#17568=CARTESIAN_POINT ( 'NONE',  ( -3.622867166186050536, -86.12610001270962812, 1.695533395769002638 ) ) ;
#17579=CARTESIAN_POINT ( 'NONE',  ( 3.110929027860000140, -81.09520976391398506, -2.455221122833000091 ) ) ;
#17582=CARTESIAN_POINT ( 'NONE',  ( 3.260489991048999947, -82.29725264934799611, -1.390623913068999906 ) ) ;
#17602=CARTESIAN_POINT ( 'NONE',  ( -1.813335989237000234, -85.74518770028200265, 3.710867668353999616 ) ) ;
#17610=CARTESIAN_POINT ( 'NONE',  ( -3.399999999999689937, -78.72609999968184979, -1.426627331148062801E-14 ) ) ;
#17630=CARTESIAN_POINT ( 'NONE',  ( 2.060606489177889689, -78.96264282632948550, -3.567929020052158950 ) ) ;
#17640=CARTESIAN_POINT ( 'NONE',  ( 1.960173199283000267, -79.72080496681199691, 3.683447210608000066 ) ) ;
#17647=CARTESIAN_POINT ( 'NONE',  ( -1.490122748909000094, -84.99032934161199648, -3.219331321608999819 ) ) ;
#17669=CARTESIAN_POINT ( 'NONE',  ( 0.000000000000000000, -86.09999999999999432, 0.000000000000000000 ) ) ;
#17689=ORIENTED_EDGE ( 'NONE', *, *, #6, .F. ) ;
#17712=CARTESIAN_POINT ( 'NONE',  ( 3.112536659741847345, -86.17851879815597727, -1.385790604991341546 ) ) ;
#17743=CARTESIAN_POINT ( 'NONE',  ( 3.723051508230033502, -85.94828561723799965, 2.704164226566601492 ) ) ;
#17747=CARTESIAN_POINT ( 'NONE',  ( -3.436577009133267691, -78.54828564506388489, 0.06478620501008579280 ) ) ;
#17776=CARTESIAN_POINT ( 'NONE',  ( 3.123036614452256110, -82.55416668342336095, 1.451080448598909944 ) ) ;
#17827=CARTESIAN_POINT ( 'NONE',  ( 0.3144812618505000157, -82.86349735065198274, 4.163017894414998921 ) ) ;
#17858=CARTESIAN_POINT ( 'NONE',  ( 2.817594599424999569, -80.97881882065600223, -2.223714431971000050 ) ) ;
#17871=CARTESIAN_POINT ( 'NONE',  ( -4.580541315389114132, -86.25171438276197478, -0.4384716419589351766 ) ) ;
#17877=CARTESIAN_POINT ( 'NONE',  ( 0.8807763160617000375, -81.57621146183899441, 3.863964706566999752 ) ) ;
#17881=CARTESIAN_POINT ( 'NONE',  ( -1.280698150711000238, -78.93025264934789220, -3.305257395273999865 ) ) ;
#17904=CARTESIAN_POINT ( 'NONE',  ( 3.766997394601000249, -82.17775871403298993, -1.388144962921000092 ) ) ;
#17911=EDGE_LOOP ( 'NONE', ( #40050, #32934, #9003, #56193 ) ) ;
#17940=CARTESIAN_POINT ( 'NONE',  ( -3.811312777322000134, -78.56950264934789629, 1.220744239273999998 ) ) ;
#17964=CARTESIAN_POINT ( 'NONE',  ( -1.490776890111999986, -83.11557450217399889, 3.265167628442000147 ) ) ;
#18004=CARTESIAN_POINT ( 'NONE',  ( -2.409209601448000893, -86.31452042059399332, 3.252055376540964104 ) ) ;
#18035=CARTESIAN_POINT ( 'NONE',  ( -0.5677917205626995534, -85.94828561723799965, 4.566314625519897419 ) ) ;
#18040=CARTESIAN_POINT ( 'NONE',  ( 3.407095545933004122, -78.62148120184446043, -2.010777145231036567 ) ) ;
#18054=CARTESIAN_POINT ( 'NONE',  ( 3.914500761937000028, -78.48547955770030171, 2.310234098304058126 ) ) ;
#18061=( BOUNDED_SURFACE ( )  B_SPLINE_SURFACE ( 3, 3, ( 
 ( #38841, #16994, #51861, #2839, #15834, #47730, #42704 ),
 ( #16128, #16418, #16707, #2271, #34400, #48300, #12271 ),
 ( #52431, #11414, #20268, #25841, #34105, #34689, #56568 ),
 ( #12555, #30260, #11991, #57142, #3417, #52719, #7265 ),
 ( #43868, #29395, #21416, #30553, #48585, #20556, #53004 ),
 ( #34974, #47445, #8130, #33821, #25552, #2555, #29969 ),
 ( #48020, #7554, #21125, #20835, #6973, #24975, #42998 ),
 ( #52147, #29680, #25266, #53889, #44432, #26132, #26995 ),
 ( #45031, #48872, #9300, #191, #44152, #9011, #26702 ),
 ( #3985, #18166, #36159, #3699, #58009, #35560, #21702 ),
 ( #49159, #54179, #21987, #39707, #22874, #14009, #39996 ),
 ( #475, #4582, #35261, #27290, #44733, #17871, #26411 ),
 ( #4284, #22281, #13716, #17271, #13125, #53291, #12837 ),
 ( #45327, #40299, #31711, #36444, #58309, #35861, #17568 ),
 ( #54474, #57714, #30838, #13420, #22583, #31421, #31120 ) ),
 .UNSPECIFIED., .F., .F., .F. ) 
 B_SPLINE_SURFACE_WITH_KNOTS ( ( 4, 1, 1, 1, 1, 1, 1, 1, 1, 1, 1, 1, 4 ),
 ( 4, 3, 4 ),
 ( 0.009836358961777999163, 0.09153385889397000486, 0.1732268882812000033, 0.2549245844128000260, 0.3366128623372000028, 0.4183102317861999708, 0.5000049915032999115, 0.5816997502458999270, 0.6633970872647999562, 0.7450853589770999319, 0.8267830756728000718, 0.9084760833474000430, 0.9901736252444659492 ),
 ( 0.000000000000000000, 0.5000000000000000000, 1.000000000000000000 ),
 .UNSPECIFIED. ) 
 GEOMETRIC_REPRESENTATION_ITEM ( )  RATIONAL_B_SPLINE_SURFACE ( (
 ( 1.000000000000000000, 0.8025111795252390934, 0.8025111795252390934, 1.000000000000000000, 0.8025111795252390934, 0.8025111795252390934, 1.000000000000000000),
 ( 1.000000000000000000, 0.8025111795252390934, 0.8025111795252390934, 1.000000000000000000, 0.8025111795252390934, 0.8025111795252390934, 1.000000000000000000),
 ( 1.000000000000000000, 0.8025111795252390934, 0.8025111795252390934, 1.000000000000000000, 0.8025111795252390934, 0.8025111795252390934, 1.000000000000000000),
 ( 1.000000000000000000, 0.8025111795252390934, 0.8025111795252390934, 1.000000000000000000, 0.8025111795252390934, 0.8025111795252390934, 1.000000000000000000),
 ( 1.000000000000000000, 0.8025111795252390934, 0.8025111795252390934, 1.000000000000000000, 0.8025111795252390934, 0.8025111795252390934, 1.000000000000000000),
 ( 1.000000000000000000, 0.8025111795252390934, 0.8025111795252390934, 1.000000000000000000, 0.8025111795252390934, 0.8025111795252390934, 1.000000000000000000),
 ( 1.000000000000000000, 0.8025111795252390934, 0.8025111795252390934, 1.000000000000000000, 0.8025111795252390934, 0.8025111795252390934, 1.000000000000000000),
 ( 1.000000000000000000, 0.8025111795252390934, 0.8025111795252390934, 1.000000000000000000, 0.8025111795252390934, 0.8025111795252390934, 1.000000000000000000),
 ( 1.000000000000000000, 0.8025111795252390934, 0.8025111795252390934, 1.000000000000000000, 0.8025111795252390934, 0.8025111795252390934, 1.000000000000000000),
 ( 1.000000000000000000, 0.8025111795252390934, 0.8025111795252390934, 1.000000000000000000, 0.8025111795252390934, 0.8025111795252390934, 1.000000000000000000),
 ( 1.000000000000000000, 0.8025111795252390934, 0.8025111795252390934, 1.000000000000000000, 0.8025111795252390934, 0.8025111795252390934, 1.000000000000000000),
 ( 1.000000000000000000, 0.8025111795252390934, 0.8025111795252390934, 1.000000000000000000, 0.8025111795252390934, 0.8025111795252390934, 1.000000000000000000),
 ( 1.000000000000000000, 0.8025111795252390934, 0.8025111795252390934, 1.000000000000000000, 0.8025111795252390934, 0.8025111795252390934, 1.000000000000000000),
 ( 1.000000000000000000, 0.8025111795252390934, 0.8025111795252390934, 1.000000000000000000, 0.8025111795252390934, 0.8025111795252390934, 1.000000000000000000),
 ( 1.000000000000000000, 0.8025111795252390934, 0.8025111795252390934, 1.000000000000000000, 0.8025111795252390934, 0.8025111795252390934, 1.000000000000000000) ) ) 
 REPRESENTATION_ITEM ( '' )  SURFACE ( )  );
#18095=CARTESIAN_POINT ( 'NONE',  ( 3.161638919850000118, -85.14393562394799631, -1.699348249670000088 ) ) ;
#18123=CARTESIAN_POINT ( 'NONE',  ( 4.002578937700000949, -84.19782450217398662, 1.018756769644999949 ) ) ;
#18155=CARTESIAN_POINT ( 'NONE',  ( -0.3927644566776000157, -80.85470891495099011, -3.735921117030000183 ) ) ;
#18166=CARTESIAN_POINT ( 'NONE',  ( 2.594087562880047493, -86.36264283715696877, -3.643225128093495968 ) ) ;
#18174=CARTESIAN_POINT ( 'NONE',  ( -3.523754135837000145, -80.25731627376899269, 2.154453638336999877 ) ) ;
#18178=CARTESIAN_POINT ( 'NONE',  ( 0.4740844096781999806, -79.12582046129089974, -3.515651949852999891 ) ) ;
#18204=CARTESIAN_POINT ( 'NONE',  ( -3.415814973257000453, -85.99726526706999152, 2.400282231302999669 ) ) ;
#18227=B_SPLINE_SURFACE_WITH_KNOTS ( 'NONE', 3, 3, ( 
 ( #42745, #28562, #33857, #2307, #1441, #20304, #28849, #56322, #46609, #7010, #37425, #1730, #19723, #37720, #55741, #15286, #46901, #44186, #12023, #11739, #12868, #2875, #30871, #26442, #39740, #3169, #48906, #52183, #35293, #43319, #25301, #30295, #16453, #17307, #12588 ),
 ( #21159, #20873, #53323, #30587, #8447, #29716, #7299, #7873, #16165, #39459, #39165, #12305, #38876, #44464, #52464, #57175, #57750, #53041, #56896, #4015, #8165, #3732, #3446, #25875, #57463, #48334, #48618, #43902, #34435, #16741, #21733, #22021, #40029, #34143, #47764 ),
 ( #34721, #30003, #35008, #17024, #48057, #7588, #25587, #43609, #52751, #21452, #26167, #54213, #9921, #45362, #8744, #45067, #26735, #27617, #53619, #40630, #32327, #18778, #36480, #53925, #13748, #45657, #9044, #45949, #225, #35893, #44766, #5200, #18204, #13457, #27903 ),
 ( #4619, #17904, #23201, #41206, #27030, #40332, #5480, #36195, #796, #31748, #36770, #54788, #14330, #50374, #54509, #31453, #9629, #22618, #23486, #49793, #35591, #22315, #58341, #13157, #58042, #9339, #49495, #27328, #40923, #4911, #22910, #17602, #31154, #14046, #32040 ),
 ( #511, #49192, #50085, #18487, #4315, #41792, #37059, #51541, #10210, #11098, #6650, #37936, #32909, #29078, #1084, #15510, #50668, #14624, #24071, #5770, #55959, #28783, #47123, #19071, #32616, #1657, #41499, #46829, #28488, #19647, #28189, #24663, #37353, #6061, #42671 ),
 ( #33203, #51251, #1364, #23777, #55663, #46539, #42088, #37649, #46242, #15212, #1955, #10802, #6355, #19360, #24372, #55077, #42384, #55369, #19948, #50953, #2239, #14914, #10505, #33505, #50559, #117, #18387, #49391, #46142, #31938, #5666, #23096, #44958, #22806, #4513 ),
 ( #32515, #50270, #54404, #22514, #698, #31644, #41401, #45257, #40817, #28093, #14229, #5098, #36378, #13942, #408, #49981, #41107, #23676, #23389, #40524, #984, #5382, #18680, #41690, #9525, #10112, #18095, #36090, #53815, #18968, #54108, #14522, #1268, #35785, #36672 ),
 ( #36960, #27511, #13351, #13649, #49687, #8939, #31350, #45552, #9233, #54688, #32228, #9818, #27802, #54973, #26927, #45848, #27218, #4805, #33691, #1552, #32807, #43154, #28975, #7128, #20138, #29548, #24556, #28679, #51147, #10399, #38124, #5961, #37541, #47017, #51440 ),
 ( #33402, #19543, #19258, #10992, #10702, #19842, #2136, #6547, #37837, #24847, #15990, #56148, #15697, #33977, #51730, #55557, #50855, #37251, #42571, #25129, #11280, #47604, #29259, #46731, #6250, #28384, #47306, #23964, #15106, #6835, #42862, #2420, #33103, #20423, #55856 ),
 ( #52014, #14811, #46432, #38417, #55263, #56436, #24265, #15409, #41983, #11569, #42281, #1849, #27074, #40377, #11857, #4666, #53966, #49542, #49238, #53664, #44810, #58087, #58384, #17647, #7417, #48173, #9088, #13794, #31794, #266, #34266, #44509, #25421, #27373, #43434 ) ),
 .UNSPECIFIED., .F., .F., .F.,
 ( 4, 1, 1, 1, 1, 1, 1, 4 ),
 ( 4, 1, 1, 1, 1, 1, 1, 1, 1, 1, 1, 1, 1, 1, 1, 1, 1, 1, 1, 1, 1, 1, 1, 1, 1, 1, 1, 1, 1, 1, 1, 1, 4 ),
 ( 0.4899999999999999911, 0.5000000000000000000, 0.5999999999999999778, 0.6999999999999999556, 0.8000000000000000444, 0.9000000000000000222, 1.000000000000000000, 1.010000000000000009 ),
 ( -0.02000006906724000055, 0.01250004316702999982, 0.04500015540130000019, 0.07750026763557001097, 0.1100003798698000052, 0.1425004921040999850, 0.1750006043384000065, 0.2075007165727000003, 0.2400008288068999907, 0.2725009410411999844, 0.3050010532755000336, 0.3375011655096999963, 0.3700012777439999900, 0.4025013899782999838, 0.4350015022125000019, 0.4675016144467999957, 0.5000017266810999894, 0.5325018389153999276, 0.5650019511495999458, 0.5975020633838999951, 0.6300021756182000443, 0.6625022878524000625, 0.6950024000867000007, 0.7275025123210000499, 0.7600026245552999882, 0.7925027367895000063, 0.8250028490237999446, 0.8575029612580999938, 0.8900030734923000120, 0.9225031857265999502, 0.9550032979608999995, 0.9875034101951999377, 1.020003522429000054 ),
 .UNSPECIFIED. ) ;
#18231=CARTESIAN_POINT ( 'NONE',  ( -3.999289396772098382, -78.72610001270986402, 0.07539443523754654763 ) ) ;
#18243=CARTESIAN_POINT ( 'NONE',  ( -2.796443448903999762, -81.20728455456799111, 2.808181755991999928 ) ) ;
#18262=CARTESIAN_POINT ( 'NONE',  ( -1.556119267444000087, -85.98999735065198990, 3.184903978129999924 ) ) ;
#18267=CARTESIAN_POINT ( 'NONE',  ( -3.201827619569314720, -84.78958334313092848, -1.266442718568655534 ) ) ;
#18303=CARTESIAN_POINT ( 'NONE',  ( 4.035839202124311242, -79.47083332087994734, 0.3584785459293593490 ) ) ;
#18313=EDGE_CURVE ( 'NONE', #3531, #9865, #31803, .T. ) ;
#18331=CARTESIAN_POINT ( 'NONE',  ( 3.229228496052769071, -85.94828564506400426, 2.345485728341623943 ) ) ;
#18335=CARTESIAN_POINT ( 'NONE',  ( 3.778552491321001128, -78.40681307243319509, -1.395910297075086959E-15 ) ) ;
#18347=CARTESIAN_POINT ( 'NONE',  ( -0.03413092954076433344, -78.40681307385639798, 3.621286657814484666 ) ) ;
#18387=CARTESIAN_POINT ( 'NONE',  ( 3.308840272069000221, -85.02754468068998506, -1.778467455431999911 ) ) ;
#18410=CARTESIAN_POINT ( 'NONE',  ( 2.678834687796258773, -82.65052081583097277, 2.987155636024215521 ) ) ;
#18414=CARTESIAN_POINT ( 'NONE',  ( 3.632657541006000024, -85.55392953870899930, 2.051911650686999877 ) ) ;
#18443=CARTESIAN_POINT ( 'NONE',  ( -3.407263062984217772, -80.16458332482034166, 0.5042877003416306181 ) ) ;
#18445=CARTESIAN_POINT ( 'NONE',  ( 3.603299446323999788, -79.65220467013898542, -1.649916185975000227 ) ) ;
#18455=CARTESIAN_POINT ( 'NONE',  ( 3.542904717112961954, -85.81974682883925709, 1.393669458272039696 ) ) ;
#18462=CARTESIAN_POINT ( 'NONE',  ( -4.170640425553999719, -80.24573954672798948, 0.1880654775389999922 ) ) ;
#18466=CARTESIAN_POINT ( 'NONE',  ( -2.027639380875000175, -80.44857046129098421, -2.910881509572999626 ) ) ;
#18487=CARTESIAN_POINT ( 'NONE',  ( 3.500498580606000054, -82.26178512955299027, 1.858143047098000045 ) ) ;
#18489=CARTESIAN_POINT ( 'NONE',  ( 4.000000000000000000, -78.69999999999998863, 0.000000000000000000 ) ) ;
#18495=CARTESIAN_POINT ( 'NONE',  ( -3.914500761937032447, -78.91452044229970397, 7.829001523874018709 ) ) ;
#18532=CARTESIAN_POINT ( 'NONE',  ( -2.046340481354000040, -79.76042549782599167, 3.587616777720000094 ) ) ;
#18555=CARTESIAN_POINT ( 'NONE',  ( 0.2516332205413999712, -85.28007450217398855, -3.580561164506000260 ) ) ;
#18560=CARTESIAN_POINT ( 'NONE',  ( -2.882630883240388631, -86.06145833917183552, 1.884276930884437595 ) ) ;
#18594=CARTESIAN_POINT ( 'NONE',  ( -3.699999999670000150, -78.39678895077818765, 3.845529056692000202E-10 ) ) ;
#18598=CARTESIAN_POINT ( 'NONE',  ( -3.999588488232725059, -78.71927081250180436, -0.3228834954761045095 ) ) ;
#18609=CARTESIAN_POINT ( 'NONE',  ( -3.451879464910993622, -85.80681307243298761, 1.536875756006014671 ) ) ;
#18624=CARTESIAN_POINT ( 'NONE',  ( -0.5413909687624368638, -85.80681307243297340, 4.353993567106648754 ) ) ;
#18628=CARTESIAN_POINT ( 'NONE',  ( -3.850965819624345254, -78.43735716284258785, 0.07259824540930022441 ) ) ;
#18640=CARTESIAN_POINT ( 'NONE',  ( 3.699999999670001039, -78.39678895079168797, 2.183641461020670693 ) ) ;
#18680=CARTESIAN_POINT ( 'NONE',  ( -2.892718313690000098, -84.66293396287998974, -2.125070773710000527 ) ) ;
#18689=CARTESIAN_POINT ( 'NONE',  ( 3.654181830570425671, -86.09999999999999432, -1.626946572303649807 ) ) ;
#18702=CARTESIAN_POINT ( 'NONE',  ( 3.029351209061000194, -83.75017953870899134, -2.868723822119999767 ) ) ;
#18731=CARTESIAN_POINT ( 'NONE',  ( -1.553970433762575931, -81.43645831985729444, 3.072459199874610025 ) ) ;
#18743=CARTESIAN_POINT ( 'NONE',  ( 2.664092970791406056, -85.87263560081200353, 2.844305389928088790 ) ) ;
#18748=CARTESIAN_POINT ( 'NONE',  ( 0.9273277571154000531, -81.25894104959499487, 4.068185826040000563 ) ) ;
#18778=CARTESIAN_POINT ( 'NONE',  ( -4.139711922552000267, -84.67451069913499850, -0.5407357538481999404 ) ) ;
#18820=CARTESIAN_POINT ( 'NONE',  ( -3.381245366627000148, -79.76428455456799327, 2.067162445164999696 ) ) ;
#18842=CARTESIAN_POINT ( 'NONE',  ( 3.473803517655999595, -84.07757450217398798, -0.9035632974999000533 ) ) ;
#18847=CARTESIAN_POINT ( 'NONE',  ( 1.522508719054618709, -85.71458334025085435, 3.052348956963513160 ) ) ;
#18880=CARTESIAN_POINT ( 'NONE',  ( -2.835184365519229477, -80.01041666022817367, 2.893239195999958824 ) ) ;
#18892=CARTESIAN_POINT ( 'NONE',  ( -3.654181830570668144, -86.07389998728979208, 1.626946572303400451 ) ) ;
#18908=CARTESIAN_POINT ( 'NONE',  ( -2.350111744379241863, -86.10000000000017906, 3.172282531658992877 ) ) ;
#18924=CARTESIAN_POINT ( 'NONE',  ( -0.03344200926162519544, -78.43735717367049176, 3.548192316444005456 ) ) ;
#18944=CARTESIAN_POINT ( 'NONE',  ( -1.594109084609295790, -82.93958334889045148, 3.052517646826329312 ) ) ;
#18968=CARTESIAN_POINT ( 'NONE',  ( 1.884913056600999948, -85.50468686974798516, 3.054645663329999650 ) ) ;
#18981=CARTESIAN_POINT ( 'NONE',  ( 3.140027144888978938, -85.94828564506399005, -1.398030157552047070 ) ) ;
#18991=CARTESIAN_POINT ( 'NONE',  ( 3.123304715064033843, -82.61197914874944104, 2.518555082941037249 ) ) ;
#18994=CARTESIAN_POINT ( 'NONE',  ( -2.666133258262000094, -84.47167953870898316, 3.209093106279000018 ) ) ;
#19022=EDGE_CURVE ( 'NONE', #34390, #9865, #10061, .T. ) ;
#19023=CARTESIAN_POINT ( 'NONE',  ( -2.805830205465538629, -81.55208331940609412, 1.995571323810327424 ) ) ;
#19043=CARTESIAN_POINT ( 'NONE',  ( -3.561876371173000155, -80.12548912224700359, 2.177761901471999995 ) ) ;
#19047=CARTESIAN_POINT ( 'NONE',  ( -3.543875382632000193, -80.20807046129100115, 0.1596868623460999947 ) ) ;
#19071=CARTESIAN_POINT ( 'NONE',  ( -1.664698873050999950, -84.66679343488898724, -3.596493796894000283 ) ) ;
#19090=CARTESIAN_POINT ( 'NONE',  ( -0.05186576338884000409, -79.81593595582098999, 3.546671651303999973 ) ) ;
#19097=CARTESIAN_POINT ( 'NONE',  ( -2.375990957848951091, -78.85171438276198330, -3.940594315429740480 ) ) ;
#19111=CARTESIAN_POINT ( 'NONE',  ( -3.703301542149999737, -80.12117549782598758, -1.828677444530000251 ) ) ;
#19131=CARTESIAN_POINT ( 'NONE',  ( -0.7993968753929999727, -83.71682450217399207, -4.052094290298000168 ) ) ;
#19140=CARTESIAN_POINT ( 'NONE',  ( 3.851650068366999857, -78.96264283715740362, 0.000000000000000000 ) ) ;
#19169=CARTESIAN_POINT ( 'NONE',  ( 3.911991157192746815, -82.46277140582677134, -0.8315225724521397854 ) ) ;
#19175=CARTESIAN_POINT ( 'NONE',  ( -3.271252402253135294, -80.04895832732434258, 2.391540143840818811 ) ) ;
#19184=CARTESIAN_POINT ( 'NONE',  ( -3.620209227049993039, -85.94828561723799965, 1.611820994701015364 ) ) ;
#19202=CARTESIAN_POINT ( 'NONE',  ( 3.106054555984665289, -86.10000000000019327, -1.382904586457952556 ) ) ;
#19217=CARTESIAN_POINT ( 'NONE',  ( -0.03487126055828242838, -78.39678895079168797, 3.699835671046090901 ) ) ;
#19234=CARTESIAN_POINT ( 'NONE',  ( 2.277009439587376338, -82.65052084978994174, 2.539082304559017178 ) ) ;
#19251=CARTESIAN_POINT ( 'NONE',  ( 2.484010139066000100, -79.24607046129089838, -3.352049501643000085 ) ) ;
#19258=CARTESIAN_POINT ( 'NONE',  ( 3.546564817179000073, -82.45880512652999528, -0.05579705918139000326 ) ) ;
#19271=CARTESIAN_POINT ( 'NONE',  ( -3.184161977317994108, -85.88547957940599531, 1.417680250971013356 ) ) ;
#19282=CARTESIAN_POINT ( 'NONE',  ( -0.9444306527324454192, -82.88177081832023418, 3.899503811090379024 ) ) ;
#19286=CARTESIAN_POINT ( 'NONE',  ( 3.029657250468000385, -83.75644503318798684, -2.869013636082000218 ) ) ;
#19315=CARTESIAN_POINT ( 'NONE',  ( 1.769645564550136996, -80.70416665604813033, -2.954788210828755091 ) ) ;
#19332=CARTESIAN_POINT ( 'NONE',  ( -2.386348275546000153, -80.48624039569099864, -3.425631633863999603 ) ) ;
#19336=CARTESIAN_POINT ( 'NONE',  ( 1.378124299131000097, -80.68907046129099569, -3.268841696656000106 ) ) ;
#19360=CARTESIAN_POINT ( 'NONE',  ( 2.727633873738000148, -83.46428928222098875, -2.582902200820999639 ) ) ;
#19380=CARTESIAN_POINT ( 'NONE',  ( -2.027483865207000413, -80.41718807822699944, -2.910477459209999562 ) ) ;
#19402=CARTESIAN_POINT ( 'NONE',  ( -3.553457639398999834, -80.00478455456800475, -1.754685045573999957 ) ) ;
#19424=CARTESIAN_POINT ( 'NONE',  ( -1.715387267769999946, -83.11557450217399889, 3.757119535535999866 ) ) ;
#19463=CARTESIAN_POINT ( 'NONE',  ( -0.4747412272618017348, -79.04687498282052616, -4.009948279880011235 ) ) ;
#19472=CARTESIAN_POINT ( 'NONE',  ( -3.380118192975993807, -85.79678895079199208, 1.504925579246014111 ) ) ;
#19488=CARTESIAN_POINT ( 'NONE',  ( 3.402340145821319606, -85.80681307385597734, 2.471221923361610173 ) ) ;
#19506=( BOUNDED_SURFACE ( )  B_SPLINE_SURFACE ( 3, 3, ( 
 ( #12030, #7595, #8171, #16459 ),
 ( #3452, #12595, #25594, #17610 ),
 ( #39466, #35599, #53329, #43614 ),
 ( #26449, #53626, #21741, #26174 ),
 ( #30593, #12875, #57756, #57182 ),
 ( #44773, #22324, #40340, #34440 ),
 ( #16749, #34728, #17313, #52757 ),
 ( #48341, #25880, #43907, #35300 ),
 ( #45665, #55084, #46250, #50382 ),
 ( #45958, #45370, #36777, #32623 ),
 ( #14631, #14338, #18495, #45075 ),
 ( #54516, #5488, #54797, #58348 ),
 ( #9929, #40931, #519, #22917 ),
 ( #23493, #5778, #41506, #1092 ),
 ( #10218, #31460, #4626, #23785 ) ),
 .UNSPECIFIED., .F., .F., .F. ) 
 B_SPLINE_SURFACE_WITH_KNOTS ( ( 4, 1, 1, 1, 1, 1, 1, 1, 1, 1, 1, 1, 4 ),
 ( 4, 4 ),
 ( 0.009836338020448129327, 0.09153385889397000486, 0.1732268882812000033, 0.2549245844128000260, 0.3366128623372000028, 0.4183102317861999708, 0.5000049915032999115, 0.5816997502458999270, 0.6633970872647999562, 0.7450853589770999319, 0.8267830756728000718, 0.9084760833474000430, 0.9901736249421290159 ),
 ( 0.000000000000000000, 1.000000000000000000 ),
 .UNSPECIFIED. ) 
 GEOMETRIC_REPRESENTATION_ITEM ( )  RATIONAL_B_SPLINE_SURFACE ( (
 ( 1.000000000000000000, 0.3333333333333318715, 0.3333333333333318715, 1.000000000000000000),
 ( 1.000000000000000000, 0.3333333333333318715, 0.3333333333333318715, 1.000000000000000000),
 ( 1.000000000000000000, 0.3333333333333318715, 0.3333333333333318715, 1.000000000000000000),
 ( 1.000000000000000000, 0.3333333333333318715, 0.3333333333333318715, 1.000000000000000000),
 ( 1.000000000000000000, 0.3333333333333318715, 0.3333333333333318715, 1.000000000000000000),
 ( 1.000000000000000000, 0.3333333333333318715, 0.3333333333333318715, 1.000000000000000000),
 ( 1.000000000000000000, 0.3333333333333318715, 0.3333333333333318715, 1.000000000000000000),
 ( 1.000000000000000000, 0.3333333333333318715, 0.3333333333333318715, 1.000000000000000000),
 ( 1.000000000000000000, 0.3333333333333318715, 0.3333333333333318715, 1.000000000000000000),
 ( 1.000000000000000000, 0.3333333333333318715, 0.3333333333333318715, 1.000000000000000000),
 ( 1.000000000000000000, 0.3333333333333318715, 0.3333333333333318715, 1.000000000000000000),
 ( 1.000000000000000000, 0.3333333333333318715, 0.3333333333333318715, 1.000000000000000000),
 ( 1.000000000000000000, 0.3333333333333318715, 0.3333333333333318715, 1.000000000000000000),
 ( 1.000000000000000000, 0.3333333333333318715, 0.3333333333333318715, 1.000000000000000000),
 ( 1.000000000000000000, 0.3333333333333318715, 0.3333333333333318715, 1.000000000000000000) ) ) 
 REPRESENTATION_ITEM ( '' )  SURFACE ( )  );
#19543=CARTESIAN_POINT ( 'NONE',  ( 3.235133020217000333, -82.37863818301799768, -1.192152034091999990 ) ) ;
#19555=CARTESIAN_POINT ( 'NONE',  ( -3.654181830570668144, -86.07389998728979208, 1.626946572303400229 ) ) ;
#19568=CARTESIAN_POINT ( 'NONE',  ( -3.787130605393867810, -83.28645832267650917, -1.440612511541762064 ) ) ;
#19571=CARTESIAN_POINT ( 'NONE',  ( -3.362765314666999572, -84.83869503318800298, -2.470196700500999487 ) ) ;
#19599=CARTESIAN_POINT ( 'NONE',  ( 2.262828338668485983, -82.24583331669903430, -2.595881390529711119 ) ) ;
#19614=CARTESIAN_POINT ( 'NONE',  ( 3.615006554704453201, -85.81033527783026216, 1.103425733751174587 ) ) ;
#19618=CARTESIAN_POINT ( 'NONE',  ( 0.9278479323973001236, -81.32799336705899407, 4.070467834415999242 ) ) ;
#19647=CARTESIAN_POINT ( 'NONE',  ( 2.081147779020000144, -85.38829592649000233, 3.372659028315000196 ) ) ;
#19660=ORIENTED_EDGE ( 'NONE', *, *, #57590, .T. ) ;
#19668=CARTESIAN_POINT ( 'NONE',  ( 1.666655288874999918, -79.68942003686028386, 3.131584311337999971 ) ) ;
#19693=CARTESIAN_POINT ( 'NONE',  ( 3.263605101345000037, -79.15917549782629692, -1.494195225221999879 ) ) ;
#19714=CARTESIAN_POINT ( 'NONE',  ( 4.129628149831999551, -82.63457450217399014, -0.06497298467246999387 ) ) ;
#19723=CARTESIAN_POINT ( 'NONE',  ( 1.268533116358999902, -83.66757477367698925, -3.974591678799999972 ) ) ;
#19730=CARTESIAN_POINT ( 'NONE',  ( 2.622076063046486993, -78.97800812098877543, -2.767894580093630985 ) ) ;
#19752=CARTESIAN_POINT ( 'NONE',  ( -3.437217408589384515, -78.69999999999998863, -1.942147800595266816 ) ) ;
#19759=CARTESIAN_POINT ( 'NONE',  ( -0.3693480770463897778, -82.05312501633302702, -4.021025545053856121 ) ) ;
#19787=EDGE_LOOP ( 'NONE', ( #24734, #55684, #30173, #42602 ) ) ;
#19801=CARTESIAN_POINT ( 'NONE',  ( -2.060840846990595221, -78.54828564506389910, 3.417916694071717387 ) ) ;
#19842=CARTESIAN_POINT ( 'NONE',  ( 0.2671681181389000126, -82.81955637232998413, 3.536976524314999981 ) ) ;
#19867=CARTESIAN_POINT ( 'NONE',  ( -1.587910676672080967, -83.47916665808423886, -3.726481291835321841 ) ) ;
#19948=CARTESIAN_POINT ( 'NONE',  ( -0.7078687434456000238, -84.06554135855498089, 3.689212947271000242 ) ) ;
#19970=CARTESIAN_POINT ( 'NONE',  ( -3.412678419678000008, -78.64724969135635035, 0.4937240612773000636 ) ) ;
#19993=CARTESIAN_POINT ( 'NONE',  ( 0.8348061542621000308, -80.96678455456799384, 3.662575701359999769 ) ) ;
#19999=CARTESIAN_POINT ( 'NONE',  ( -3.399999999999689937, -78.72609999968184979, -1.426627331148062801E-14 ) ) ;
#20004=EDGE_CURVE ( 'NONE', #313, #26598, #55340, .T. ) ;
#20015=CARTESIAN_POINT ( 'NONE',  ( 2.260331847164999797, -82.87507450217398741, 3.456781180494999717 ) ) ;
#20028=CARTESIAN_POINT ( 'NONE',  ( -3.116622985464775564, -78.75135162752194162, -1.413773745829535411 ) ) ;
#20060=CARTESIAN_POINT ( 'NONE',  ( -4.014515848897613814, -81.66770834536960422, 0.5407614939776936858 ) ) ;
#20094=CARTESIAN_POINT ( 'NONE',  ( 3.399999999999981704, -78.70000000000000284, 2.006589450846597789 ) ) ;
#20100=CARTESIAN_POINT ( 'NONE',  ( -3.654181822837000215, -86.09999999943198645, 1.626946589673999854 ) ) ;
#20111=ORIENTED_EDGE ( 'NONE', *, *, #41247, .F. ) ;
#20138=CARTESIAN_POINT ( 'NONE',  ( 0.2486384805219999938, -85.03526194493599633, -3.535979362066000498 ) ) ;
#20161=CARTESIAN_POINT ( 'NONE',  ( -3.887390283284898551, -83.13229165435031121, 1.138840507441416516 ) ) ;
#20214=EDGE_CURVE ( 'NONE', #16460, #521, #15593, .T. ) ;
#20232=CARTESIAN_POINT ( 'NONE',  ( -2.398287285836949501, -78.67389998729011324, 3.977573602256665009 ) ) ;
#20256=CARTESIAN_POINT ( 'NONE',  ( -2.027724787492000136, -80.41092258374798973, -2.910823306046000258 ) ) ;
#20268=CARTESIAN_POINT ( 'NONE',  ( 0.4140829508681878046, -86.17851879815596305, -3.934470707847995907 ) ) ;
#20278=CARTESIAN_POINT ( 'NONE',  ( -3.585753949159999898, -80.00092549782598894, 0.1615739086348000064 ) ) ;
#20297=CARTESIAN_POINT ( 'NONE',  ( 3.614576546944999969, -82.67079877876498983, -1.331975541213999970 ) ) ;
#20298=CARTESIAN_POINT ( 'NONE',  ( 3.647699722741000183, -86.02148118236299013, -1.624060551956000076 ) ) ;
#20304=CARTESIAN_POINT ( 'NONE',  ( 0.3142488045808999875, -82.82582186680899383, 4.160266772619999109 ) ) ;
#20339=CARTESIAN_POINT ( 'NONE',  ( -0.06116421237667998834, -79.84732046129099103, 4.171666818936000887 ) ) ;
#20364=ORIENTED_EDGE ( 'NONE', *, *, #20214, .F. ) ;
#20402=CARTESIAN_POINT ( 'NONE',  ( 3.922208058606934333, -86.09999999999998010, 0.4502061935814848925 ) ) ;
#20423=CARTESIAN_POINT ( 'NONE',  ( -3.318057126862000050, -86.14648452804499357, 0.9369146352647000908 ) ) ;
#20447=CARTESIAN_POINT ( 'NONE',  ( -3.470841151267981317, -83.07447915372796388, 2.013464203440571421 ) ) ;
#20468=( NAMED_UNIT ( * ) PLANE_ANGLE_UNIT ( ) SI_UNIT ( $, .RADIAN. ) );
#20519=CARTESIAN_POINT ( 'NONE',  ( -0.03769866006636925920, -78.69999999999998863, 3.999822347433480640 ) ) ;
#20542=CIRCLE ( 'NONE', #54473, 3.399999999999999911 ) ;
#20544=CARTESIAN_POINT ( 'NONE',  ( -3.235964442481000347, -78.68248402847228817, 1.036662180689999824 ) ) ;
#20556=CARTESIAN_POINT ( 'NONE',  ( -4.028823909683901583, -86.31452042059395069, -0.3856585746546848936 ) ) ;
#20565=CARTESIAN_POINT ( 'NONE',  ( 3.579475725212000192, -79.27942549782629555, 0.2666292237523999464 ) ) ;
#20570=CARTESIAN_POINT ( 'NONE',  ( 3.544223523194999892, -82.50274735065200105, -0.05576259466792000269 ) ) ;
#20598=CARTESIAN_POINT ( 'NONE',  ( -1.937220121396670214, -78.81741337217214038, -2.837945647007499961 ) ) ;
#20625=CARTESIAN_POINT ( 'NONE',  ( 1.232251595443166980, -82.14947918407371219, -3.818482668381804501 ) ) ;
#20627=CARTESIAN_POINT ( 'NONE',  ( -4.167886093573000217, -80.20807046129100115, 0.1878047563862999814 ) ) ;
#20734=CARTESIAN_POINT ( 'NONE',  ( 4.019001026802343723, -83.98020833014430764, 0.5171148167050576561 ) ) ;
#20771=CARTESIAN_POINT ( 'NONE',  ( 1.592434616855211038, -86.12610001270965654, 3.669353075276090781 ) ) ;
#20824=CARTESIAN_POINT ( 'NONE',  ( 2.185729144939000168, -82.22094444544498515, -2.793620395780000099 ) ) ;
#20835=CARTESIAN_POINT ( 'NONE',  ( -1.504090147229564911, -86.39318692614398287, -3.294327671531883439 ) ) ;
#20844=MECHANICAL_DESIGN_GEOMETRIC_PRESENTATION_REPRESENTATION('',(#12365),#3850);
#20847=CARTESIAN_POINT ( 'NONE',  ( -0.05507133005142999388, -79.52378455456849338, 3.756105593829000000 ) ) ;
#20851=CARTESIAN_POINT ( 'NONE',  ( -3.512414921358999909, -83.22424735065199286, 0.4773942860886000172 ) ) ;
#20862=AXIS2_PLACEMENT_3D ( 'NONE', #42019, #24001, #55595 ) ;
#20873=CARTESIAN_POINT ( 'NONE',  ( 3.805616469024999837, -82.37863818301799768, -1.402376157695000014 ) ) ;
#20879=CARTESIAN_POINT ( 'NONE',  ( -2.382488120207371107, -78.79697025342967720, -2.465198065420734164 ) ) ;
#20898=CARTESIAN_POINT ( 'NONE',  ( 2.148673102446170713, -79.00321104920828930, -3.720415885850087534 ) ) ;
#20907=CARTESIAN_POINT ( 'NONE',  ( -3.989720889280234051, -81.72552084601404943, -0.4276727937140968883 ) ) ;
#20970=CARTESIAN_POINT ( 'NONE',  ( -0.4871519710311427165, -86.09999999999998010, 3.917790784212549227 ) ) ;
#21012=CARTESIAN_POINT ( 'NONE',  ( -2.347024683480479545, -78.48547955770027329, -3.892553587101836410 ) ) ;
#21031=PRODUCT_DEFINITION_SHAPE ( 'NONE', 'NONE',  #54603 ) ;
#21037=ORIENTED_EDGE ( 'NONE', *, *, #53131, .T. ) ;
#21057=CARTESIAN_POINT ( 'NONE',  ( 4.614362421890539245, -86.09999999999978115, 0.5296543453899439369 ) ) ;
#21114=CARTESIAN_POINT ( 'NONE',  ( 1.665357644511999968, -79.76473784880299434, 3.129146085054999471 ) ) ;
#21125=CARTESIAN_POINT ( 'NONE',  ( 0.4401343155876301094, -86.39318692614396866, -4.182001622060982804 ) ) ;
#21133=CARTESIAN_POINT ( 'NONE',  ( 3.301590336738000175, -82.16542549782599281, -1.408153524787000066 ) ) ;
#21138=CARTESIAN_POINT ( 'NONE',  ( 3.437452679404000122, -83.99694503318799832, 0.8749179571431999758 ) ) ;
#21159=CARTESIAN_POINT ( 'NONE',  ( 3.472269588435000109, -82.33855471126298653, -1.985374575346000370 ) ) ;
#21165=CARTESIAN_POINT ( 'NONE',  ( -3.926077803139174982, -78.72584796626247794, -0.8615687731491100676 ) ) ;
#21185=CARTESIAN_POINT ( 'NONE',  ( 3.485499217011998940, -78.91452042059378869, -2.057048905967550745 ) ) ;
#21195=FACE_OUTER_BOUND ( 'NONE', #57199, .T. ) ;
#21233=CARTESIAN_POINT ( 'NONE',  ( 3.407095545933000569, -78.62148120184447464, 0.000000000000000000 ) ) ;
#21319=SURFACE_SIDE_STYLE ('',( #24889 ) ) ;
#21372=CARTESIAN_POINT ( 'NONE',  ( 2.266462915304999992, -85.26849735065199809, -3.506101190763999842 ) ) ;
#21403=CARTESIAN_POINT ( 'NONE',  ( -3.062358763434999798, -80.25731627376899269, 1.872352532395999969 ) ) ;
#21416=CARTESIAN_POINT ( 'NONE',  ( 0.4236117777057033518, -86.31452042059397911, -4.025010272438366954 ) ) ;
#21425=CARTESIAN_POINT ( 'NONE',  ( 0.6322386839596000341, -82.41796443320698984, -3.912314205455000415 ) ) ;
#21428=CARTESIAN_POINT ( 'NONE',  ( 3.537250157901000058, -79.48030496681158752, 0.2634839111148000179 ) ) ;
#21431=CARTESIAN_POINT ( 'NONE',  ( -2.845754477180000297, -83.10399735065199422, 2.113443956577000016 ) ) ;
#21444=CARTESIAN_POINT ( 'NONE',  ( 3.451879464910999840, -85.80681307243298761, -1.536875756006000016 ) ) ;
#21452=CARTESIAN_POINT ( 'NONE',  ( -3.894423402048999616, -83.23150571593399150, -1.504352435119000075 ) ) ;
#21459=CARTESIAN_POINT ( 'NONE',  ( -3.065563091283566521, -78.78445349890496630, -2.577180195798276063 ) ) ;
#21477=CARTESIAN_POINT ( 'NONE',  ( -0.03487147506507188438, -79.00321104920828930, -3.699835669024340579 ) ) ;
#21486=CARTESIAN_POINT ( 'NONE',  ( -3.743366236640000455, -80.25300264934799088, -1.848461251573999986 ) ) ;
#21548=CARTESIAN_POINT ( 'NONE',  ( -0.4881686207923673915, -86.17851879815599148, 3.925966920820173733 ) ) ;
#21567=CARTESIAN_POINT ( 'NONE',  ( 0.5573607202496000390, -79.08816791445418914, -4.134721415477000228 ) ) ;
#21582=CARTESIAN_POINT ( 'NONE',  ( 1.592434616855533891, -86.09999999999999432, 3.669353075276593046 ) ) ;
#21629=CARTESIAN_POINT ( 'NONE',  ( 3.757989199629302668, -86.12610001270964233, 2.729540522067530173 ) ) ;
#21662=CARTESIAN_POINT ( 'NONE',  ( -3.978328889313999639, -86.23049735065200139, 0.4349952100312000081 ) ) ;
#21688=CARTESIAN_POINT ( 'NONE',  ( -1.756145855908000097, -80.00523869776598929, 3.079110751715000038 ) ) ;
#21702=CARTESIAN_POINT ( 'NONE',  ( -3.488504142081042314, -86.36264283715695456, 1.632650329933101885 ) ) ;
#21703=CARTESIAN_POINT ( 'NONE',  ( 3.281627333226164289, -85.82424546584941538, 1.435836378473854591 ) ) ;
#21709=CARTESIAN_POINT ( 'NONE',  ( 0.6588992274324999565, -82.30157348994899280, -4.077290543664999767 ) ) ;
#21712=CARTESIAN_POINT ( 'NONE',  ( -1.756256933393999908, -79.89225264934799497, 3.079046179090000113 ) ) ;
#21733=CARTESIAN_POINT ( 'NONE',  ( 0.2050755927455000238, -85.82581675399998744, 4.167486983637000542 ) ) ;
#21741=CARTESIAN_POINT ( 'NONE',  ( -3.437187628289029018, -78.85171435493609238, 6.874375256578015403 ) ) ;
#21758=CARTESIAN_POINT ( 'NONE',  ( -3.819913647775994292, -78.99318692756679638, -2.158384532486305574 ) ) ;
#21769=CARTESIAN_POINT ( 'NONE',  ( 1.621859418500000150, -80.61375264934798679, -3.846969171540000065 ) ) ;
#21809=CARTESIAN_POINT ( 'NONE',  ( 3.124641504234999534, -85.31342953870898782, -1.679633349223000005 ) ) ;
#21830=CARTESIAN_POINT ( 'NONE',  ( -0.4924802140953842278, -86.25171435493598437, 3.960641768741265611 ) ) ;
#21864=CARTESIAN_POINT ( 'NONE',  ( 3.654181830570652156, -86.07389998728979208, -1.626946572303435534 ) ) ;
#21926=CARTESIAN_POINT ( 'NONE',  ( 3.576074390006000137, -86.31452044229999387, -1.592170899227999925 ) ) ;
#21943=CARTESIAN_POINT ( 'NONE',  ( 0.2031981210172000007, -86.00157450217399457, 4.125184445905999198 ) ) ;
#21974=CARTESIAN_POINT ( 'NONE',  ( 0.5726238964369999573, -82.30157348994899280, -3.543415898539000075 ) ) ;
#21987=CARTESIAN_POINT ( 'NONE',  ( 0.4757506811368034660, -86.31452044229999387, -4.520415813425825213 ) ) ;
#21988=CARTESIAN_POINT ( 'NONE',  ( -1.469278768180998673, -86.01430711258555561, 3.096351707814453125 ) ) ;
#21997=CARTESIAN_POINT ( 'NONE',  ( 0.5726387496589999682, -81.92492549782599554, -3.543412413248999915 ) ) ;
#22021=CARTESIAN_POINT ( 'NONE',  ( -1.831926221770999952, -85.94606716926699619, 3.748911303548999818 ) ) ;
#22027=CARTESIAN_POINT ( 'NONE',  ( -2.821716789433580619, -78.79507810614309449, -2.832896129789050921 ) ) ;
#22046=CARTESIAN_POINT ( 'NONE',  ( -3.444390624473297358, -78.77851879815550262, -1.946200917927129570 ) ) ;
#22056=CARTESIAN_POINT ( 'NONE',  ( -2.068479106922999744, -79.89225264934799497, 3.626429920131999829 ) ) ;
#22094=CARTESIAN_POINT ( 'NONE',  ( 1.863042131308999982, -85.67417953870899794, 3.018880368111999779 ) ) ;
#22122=CARTESIAN_POINT ( 'NONE',  ( 3.274617103212424940, -86.31452042059399332, 2.378452838117018242 ) ) ;
#22157=CARTESIAN_POINT ( 'NONE',  ( 1.577629893833666808, -85.94828561723799965, 3.635239426043249011 ) ) ;
#22163=CARTESIAN_POINT ( 'NONE',  ( -0.03413113949348758891, -78.40681307385639798, -3.621286655835656898 ) ) ;
#22174=CARTESIAN_POINT ( 'NONE',  ( -2.375990622215050418, -78.54828561723800817, 3.940594454193545371 ) ) ;
#22222=CARTESIAN_POINT ( 'NONE',  ( 3.241578942234999872, -86.36264282632899381, -1.443243930775000239 ) ) ;
#22230=EDGE_CURVE ( 'NONE', #521, #16460, #13400, .T. ) ;
#22241=CARTESIAN_POINT ( 'NONE',  ( 0.2895459579014000306, -85.28007450217398855, -4.120032362860000852 ) ) ;
#22270=CARTESIAN_POINT ( 'NONE',  ( -3.752697076307999868, -80.49395764150798982, 0.1692192794638000264 ) ) ;
#22281=CARTESIAN_POINT ( 'NONE',  ( 2.689222434189590061, -86.17851881763698429, -3.776835788994612475 ) ) ;
#22282=CARTESIAN_POINT ( 'NONE',  ( 2.452186592920638120, -85.87062192719187692, 2.534882777327113867 ) ) ;
#22291=CARTESIAN_POINT ( 'NONE',  ( 3.894762958177000023, -81.21931966961800242, 1.374530897864000067 ) ) ;
#22294=CARTESIAN_POINT ( 'NONE',  ( -1.208787279847999940, -81.80467549782599690, -3.379731224302000125 ) ) ;
#22315=CARTESIAN_POINT ( 'NONE',  ( -4.095405198877999808, -84.54268354761398996, -0.5349483391501999030 ) ) ;
#22324=CARTESIAN_POINT ( 'NONE',  ( 3.548349909811001179, -78.96264282632948550, 7.096699819622030780 ) ) ;
#22344=CARTESIAN_POINT ( 'NONE',  ( -3.992195106911536673, -78.77851881763731967, 0.07526069398394277798 ) ) ;
#22357=CARTESIAN_POINT ( 'NONE',  ( 3.277247998812000240, -80.73400264934798543, -2.586357541886000089 ) ) ;
#22381=CARTESIAN_POINT ( 'NONE',  ( 2.727581927295000153, -84.07371544543099162, -2.582955461952999965 ) ) ;
#22421=CARTESIAN_POINT ( 'NONE',  ( 1.356394222569207386, -86.17851879815597727, 3.125459129807984571 ) ) ;
#22459=CARTESIAN_POINT ( 'NONE',  ( 3.778552491320999795, -78.40681307243319509, -2.230001151765018008 ) ) ;
#22514=CARTESIAN_POINT ( 'NONE',  ( 3.170431021627999613, -82.37817607281098731, 1.682935794284000197 ) ) ;
#22524=CARTESIAN_POINT ( 'NONE',  ( 3.654181830570000233, -86.09999999999999432, -1.626946572303000105 ) ) ;
#22542=CARTESIAN_POINT ( 'NONE',  ( -3.364651624423000253, -84.90774735065198797, -2.471582332770999813 ) ) ;
#22572=CARTESIAN_POINT ( 'NONE',  ( 3.423420673917999757, -82.66232476339300206, 0.3453276880145999539 ) ) ;
#22583=CARTESIAN_POINT ( 'NONE',  ( -3.808769407549206232, -86.09999999999979536, -2.658222959242663386 ) ) ;
#22584=CARTESIAN_POINT ( 'NONE',  ( 3.243587544365338360, -85.82689775056601889, 1.505994140326985198 ) ) ;
#22589=CARTESIAN_POINT ( 'NONE',  ( 1.940427222861999867, -79.89656500032499764, 3.645991759044000080 ) ) ;
#22618=CARTESIAN_POINT ( 'NONE',  ( 1.276195428221999828, -84.06168188654598339, 3.928083336394000202 ) ) ;
#22623=ORIENTED_EDGE ( 'NONE', *, *, #8089, .F. ) ;
#22647=CARTESIAN_POINT ( 'NONE',  ( 3.999999999999816147, -78.72610001270986402, -1.484001723589534194E-15 ) ) ;
#22660=CARTESIAN_POINT ( 'NONE',  ( -1.151506974306000020, -81.40430496681199202, 4.010497975643999347 ) ) ;
#22681=CARTESIAN_POINT ( 'NONE',  ( -3.315816780652000251, -86.19041401731898588, 0.9364754677271999173 ) ) ;
#22718=CARTESIAN_POINT ( 'NONE',  ( 4.177667811529521380, -86.39318692614398287, 0.4795288509365496221 ) ) ;
#22721=CARTESIAN_POINT ( 'NONE',  ( 3.404852354755926847, -79.58645832216895144, 2.196520115241515470 ) ) ;
#22751=CARTESIAN_POINT ( 'NONE',  ( 3.407095545933005010, -78.62148120184446043, -1.253608761936364502E-15 ) ) ;
#22763=CARTESIAN_POINT ( 'NONE',  ( 3.851650068366999857, -78.43735716284258785, -4.716910927661330529E-16 ) ) ;
#22783=CARTESIAN_POINT ( 'NONE',  ( 2.843708761399523777, -82.59270834996989663, 1.941616614676821229 ) ) ;
#22806=CARTESIAN_POINT ( 'NONE',  ( -3.513994194679999961, -85.82921411580198878, 0.9922410806546999584 ) ) ;
#22829=CARTESIAN_POINT ( 'NONE',  ( 3.761670435195240358, -82.53489581458633495, 1.396303704899410691 ) ) ;
#22832=CARTESIAN_POINT ( 'NONE',  ( 4.038168894520000052, -83.87669503318799968, -1.050359118944999892 ) ) ;
#22862=CARTESIAN_POINT ( 'NONE',  ( 3.142447459108117513, -81.05104165469458621, 1.410275201556511870 ) ) ;
#22865=CARTESIAN_POINT ( 'NONE',  ( -3.666049313226999562, -82.05721315976299479, -0.8194224013866000522 ) ) ;
#22874=CARTESIAN_POINT ( 'NONE',  ( -3.727357686973370221, -86.31452044229999387, -2.601403949838035246 ) ) ;
#22880=CARTESIAN_POINT ( 'NONE',  ( -1.508573806804000217, -79.04323530191599900, -3.892781328016000408 ) ) ;
#22885=CARTESIAN_POINT ( 'NONE',  ( 3.263030560321000362, -82.37257046129099081, -1.391707485291000079 ) ) ;
#22910=CARTESIAN_POINT ( 'NONE',  ( 0.2029945029552999991, -85.62493728501499390, 4.125195677802000027 ) ) ;
#22917=CARTESIAN_POINT ( 'NONE',  ( -3.992904449609000483, -78.77851881763731967, -1.675407828963362202E-14 ) ) ;
#22937=CARTESIAN_POINT ( 'NONE',  ( -0.03769889196559914751, -78.69999999999997442, -3.999822345247594502 ) ) ;
#22953=CARTESIAN_POINT ( 'NONE',  ( -3.959059990207000723, -79.88453455456799190, 0.1783950617379000125 ) ) ;
#22974=CARTESIAN_POINT ( 'NONE',  ( 2.055825304754000271, -82.99146544543100390, 3.144024286863999595 ) ) ;
#22979=CARTESIAN_POINT ( 'NONE',  ( 0.3254755831213840822, -85.09791667550392447, -3.428796880094302946 ) ) ;
#23010=CARTESIAN_POINT ( 'NONE',  ( -3.437187628289000152, -78.54828564256808932, 7.107975105357999081E-08 ) ) ;
#23013=CARTESIAN_POINT ( 'NONE',  ( -1.107038077825813316, -79.00833331572410145, -3.857210535151066821 ) ) ;
#23038=CARTESIAN_POINT ( 'NONE',  ( -0.4994022981160649577, -85.88547957940600952, 4.016310797290806534 ) ) ;
#23042=CARTESIAN_POINT ( 'NONE',  ( -0.03561181053916687156, -78.40681307243319509, -3.778384671869483125 ) ) ;
#23053=CARTESIAN_POINT ( 'NONE',  ( -0.03284966253593384761, -78.48547957940618858, 3.485344415041724098 ) ) ;
#23096=CARTESIAN_POINT ( 'NONE',  ( -1.649271994007999842, -85.62879675702399140, 3.375121960417999833 ) ) ;
#23109=CARTESIAN_POINT ( 'NONE',  ( -6.525630976922989213, -85.80681307243297340, -5.366883173815897301 ) ) ;
#23120=CARTESIAN_POINT ( 'NONE',  ( 2.428549115787052237, -82.66979164937175995, 3.194813371584084294 ) ) ;
#23152=CARTESIAN_POINT ( 'NONE',  ( -0.9876844338732081452, -79.89479165920646153, 3.298423224253481223 ) ) ;
#23154=CARTESIAN_POINT ( 'NONE',  ( -3.812492577196000099, -78.97078559807879117, 0.5515665665854999622 ) ) ;
#23173=CARTESIAN_POINT ( 'NONE',  ( 3.275350148889000224, -80.77793935167099448, -2.584986284871999551 ) ) ;
#23181=DIRECTION ( 'NONE',  ( 0.000000000000000000, 1.000000000000000000, 0.000000000000000000 ) ) ;
#23201=CARTESIAN_POINT ( 'NONE',  ( 4.129629397805000046, -82.25792565754399277, -0.06497024241327999106 ) ) ;
#23243=CARTESIAN_POINT ( 'NONE',  ( 4.005932268072999847, -82.24559216449299015, -0.2640443533972999801 ) ) ;
#23266=CARTESIAN_POINT ( 'NONE',  ( 2.606239186342999670, -83.95732450217400356, -2.468046761181999837 ) ) ;
#23271=CARTESIAN_POINT ( 'NONE',  ( -1.634254835633885516, -84.44270834421041627, 3.031084325246120592 ) ) ;
#23307=CARTESIAN_POINT ( 'NONE',  ( 0.7784319255180548458, -79.77916665765043547, 3.975193877679629839 ) ) ;
#23334=CARTESIAN_POINT ( 'NONE',  ( -3.131568623105716043, -86.07390000031791999, 1.324114027860883613 ) ) ;
#23337=CARTESIAN_POINT ( 'NONE',  ( 2.060606489177889689, -78.43735717367049176, -3.567929020052158950 ) ) ;
#23348=CARTESIAN_POINT ( 'NONE',  ( 2.273238635161466181, -78.48547955770030171, 3.936100089146787884 ) ) ;
#23367=CARTESIAN_POINT ( 'NONE',  ( 2.987038927812020184, -83.82604167946361429, -1.712850616285394922 ) ) ;
#23389=CARTESIAN_POINT ( 'NONE',  ( -0.6763775780641000379, -84.18193230181299214, 3.525089843763999919 ) ) ;
#23402=CARTESIAN_POINT ( 'NONE',  ( -3.106054555984679055, -86.07390000031791999, 1.382904586457439189 ) ) ;
#23415=CARTESIAN_POINT ( 'NONE',  ( -3.902709220513999711, -86.11509620537599119, 1.102229611723000158 ) ) ;
#23442=CARTESIAN_POINT ( 'NONE',  ( 2.158813089671214769, -79.66354166010867743, 2.682229611206861541 ) ) ;
#23453=CARTESIAN_POINT ( 'NONE',  ( 2.936513971769209252, -85.86020212823702025, 2.544426056595365804 ) ) ;
#23458=CARTESIAN_POINT ( 'NONE',  ( -4.072058394011000004, -81.73994274751999001, -0.9101721179166000208 ) ) ;
#23463=CARTESIAN_POINT ( 'NONE',  ( 0.7882581348285999656, -81.28405496681197917, 3.458353866083999861 ) ) ;
#23486=CARTESIAN_POINT ( 'NONE',  ( -0.7782851299293001013, -84.18193230181299214, 4.056203363392000050 ) ) ;
#23493=CARTESIAN_POINT ( 'NONE',  ( 3.999999999999815259, -78.72610001270986402, -4.898587196589186031E-16 ) ) ;
#23517=CARTESIAN_POINT ( 'NONE',  ( 3.992904449609001372, -78.77851881763731967, -1.477225460011499791E-15 ) ) ;
#23529=CARTESIAN_POINT ( 'NONE',  ( 2.747530502382999895, -80.96292549782599224, 3.083760634012000068 ) ) ;
#23547=ORIENTED_EDGE ( 'NONE', *, *, #54345, .F. ) ;
#23549=CARTESIAN_POINT ( 'NONE',  ( 3.755994528103999919, -82.75096544543198718, -0.05909446711668000368 ) ) ;
#23591=CARTESIAN_POINT ( 'NONE',  ( 3.219568491329446669, -79.29739581894648381, -2.394182203109038731 ) ) ;
#23617=CARTESIAN_POINT ( 'NONE',  ( 3.194290819685191796, -86.10000000000017906, 2.320109443757543133 ) ) ;
#23635=CARTESIAN_POINT ( 'NONE',  ( 3.699999999670000150, -78.39678895079168797, -4.531193156441073745E-16 ) ) ;
#23653=CARTESIAN_POINT ( 'NONE',  ( -1.349723918382976784, -83.47916668054376998, -3.167509171181071448 ) ) ;
#23676=CARTESIAN_POINT ( 'NONE',  ( 1.109092207577000000, -84.06168188654598339, 3.413745671519000435 ) ) ;
#23689=CARTESIAN_POINT ( 'NONE',  ( 3.308356911591977756, -85.80681307385599155, -1.472975398279049442 ) ) ;
#23700=CARTESIAN_POINT ( 'NONE',  ( 0.01844432583040244572, -82.82395831769791528, 4.013020696622482397 ) ) ;
#23703=CARTESIAN_POINT ( 'NONE',  ( -2.666402605432000250, -84.47794503318799286, 3.209417306183000029 ) ) ;
#23733=CARTESIAN_POINT ( 'NONE',  ( 2.868552210033068928, -81.08958332121085277, 1.904464906000009838 ) ) ;
#23750=CARTESIAN_POINT ( 'NONE',  ( -2.944205202882999917, -81.49944189855800403, 2.956641395289000052 ) ) ;
#23754=CARTESIAN_POINT ( 'NONE',  ( -0.9788895612340001717, -81.40430496681199202, 3.409301629348000073 ) ) ;
#23777=CARTESIAN_POINT ( 'NONE',  ( 3.318041721436999936, -82.26178512955299027, 1.761290859772999928 ) ) ;
#23785=CARTESIAN_POINT ( 'NONE',  ( -3.999999999999674927, -78.69999999999997442, -1.678385095468326031E-14 ) ) ;
#23796=CARTESIAN_POINT ( 'NONE',  ( -3.543450156475999702, -80.17668722926399028, 0.1597837688739999762 ) ) ;
#23818=CARTESIAN_POINT ( 'NONE',  ( -1.431853854392999947, -78.68203455456848872, -3.695363765894000174 ) ) ;
#23839=CARTESIAN_POINT ( 'NONE',  ( 3.756303339431999788, -85.75721544543100094, 0.03933749637742999655 ) ) ;
#23880=CARTESIAN_POINT ( 'NONE',  ( 4.571463104798961119, -86.25171438276198899, 0.5247301960419221700 ) ) ;
#23883=CARTESIAN_POINT ( 'NONE',  ( -3.389161288344675782, -78.83489581379073741, -2.147886495578234189 ) ) ;
#23908=CARTESIAN_POINT ( 'NONE',  ( 4.093343120888095932, -85.83735717367099483, 0.4698497371742681450 ) ) ;
#23964=CARTESIAN_POINT ( 'NONE',  ( 3.546854729627999969, -85.46506550819998438, 0.03730069855218000330 ) ) ;
#23990=EDGE_CURVE ( 'NONE', #16460, #3531, #27301, .T. ) ;
#23991=CARTESIAN_POINT ( 'NONE',  ( 3.797598824419751384, -83.86458332889966982, -1.413738007671073271 ) ) ;
#23994=CARTESIAN_POINT ( 'NONE',  ( 2.191089288545000180, -85.67417953870899794, 3.550449196403000052 ) ) ;
#24001=DIRECTION ( 'NONE',  ( 0.000000000000000000, 1.000000000000000000, 0.000000000000000000 ) ) ;
#24023=CARTESIAN_POINT ( 'NONE',  ( -3.233969914661031897, -81.78333331850373611, -1.182064197856841803 ) ) ;
#24037=CARTESIAN_POINT ( 'NONE',  ( -1.418579035640199937, -86.00469764872917722, 3.738292511752264513 ) ) ;
#24042=CARTESIAN_POINT ( 'NONE',  ( -4.016244863222999228, -78.72256750329937347, 0.5810441187545000163 ) ) ;
#24071=CARTESIAN_POINT ( 'NONE',  ( -0.7467939645478000044, -84.06554135855498089, 3.892080259883999638 ) ) ;
#24091=CARTESIAN_POINT ( 'NONE',  ( 0.7883160775726999470, -81.25894104959499487, 3.458341744451999933 ) ) ;
#24115=CARTESIAN_POINT ( 'NONE',  ( 3.643490196435000161, -82.12920122123499311, -0.2401545879082000179 ) ) ;
#24134=CARTESIAN_POINT ( 'NONE',  ( 2.891798309966000069, -84.43446544543100174, 2.709886222448000037 ) ) ;
#24143=CARTESIAN_POINT ( 'NONE',  ( 3.399999999999999911, -78.69999999999998863, 0.000000000000000000 ) ) ;
#24150=CARTESIAN_POINT ( 'NONE',  ( 2.655560623658488328, -78.97957698290076678, -2.730538163075394209 ) ) ;
#24207=CARTESIAN_POINT ( 'NONE',  ( -3.210317642310111186, -85.88547957940599531, 1.357411296278074442 ) ) ;
#24256=UNCERTAINTY_MEASURE_WITH_UNIT (LENGTH_MEASURE( 1.000000000000000082E-05 ), #52057, 'distance_accuracy_value', 'NONE');
#24265=CARTESIAN_POINT ( 'NONE',  ( -1.473390922089000021, -82.94607228207600258, 3.227022943217999984 ) ) ;
#24277=CARTESIAN_POINT ( 'NONE',  ( -3.654181830570442990, -86.09999999999999432, 1.626946572303610283 ) ) ;
#24290=CARTESIAN_POINT ( 'NONE',  ( 3.056131291857314469, -85.61822918110996739, 2.599642428790069015 ) ) ;
#24372=CARTESIAN_POINT ( 'NONE',  ( 3.635560235662999684, -83.58453969748799750, -0.9455538594405999975 ) ) ;
#24391=CARTESIAN_POINT ( 'NONE',  ( 2.970835140755999859, -79.57543510685839294, 1.937965009331999999 ) ) ;
#24414=CARTESIAN_POINT ( 'NONE',  ( 1.764731964946999909, -79.40353455456848053, 3.316185037183999818 ) ) ;
#24434=CARTESIAN_POINT ( 'NONE',  ( 0.1848134996591999923, -86.11796544543098264, 3.751952874225000123 ) ) ;
#24447=CARTESIAN_POINT ( 'NONE',  ( 2.432155020134764811, -78.96932498430172132, -2.971370035328440462 ) ) ;
#24469=CARTESIAN_POINT ( 'NONE',  ( 3.399999999999725464, -78.69999999999998863, -1.260385025514398905E-15 ) ) ;
#24470=CARTESIAN_POINT ( 'NONE',  ( 3.912590402935000267, -82.39999999999999147, -0.8316467632710000668 ) ) ;
#24472=CARTESIAN_POINT ( 'NONE',  ( -3.992904449609000483, -78.62148118275521824, -1.315241435988999952E-08 ) ) ;
#24512=CARTESIAN_POINT ( 'NONE',  ( -3.474811874272821566, -78.54828564506389910, 1.963390425425277641 ) ) ;
#24538=CARTESIAN_POINT ( 'NONE',  ( -3.138103972814393572, -86.17851879815597727, 1.326877354892202376 ) ) ;
#24556=CARTESIAN_POINT ( 'NONE',  ( 3.122280780499000485, -85.27576277546900485, -1.678193656463999872 ) ) ;
#24582=CARTESIAN_POINT ( 'NONE',  ( -3.140358198060591466, -83.36354165683960105, -2.558558009700006686 ) ) ;
#24631=CARTESIAN_POINT ( 'NONE',  ( -3.559519890270999909, -80.05017131030399469, 2.176321128746000255 ) ) ;
#24663=CARTESIAN_POINT ( 'NONE',  ( -1.739964340038000046, -85.62879675702399140, 3.560717623133999865 ) ) ;
#24680=CARTESIAN_POINT ( 'NONE',  ( 3.537682960765999862, -79.44891918789778629, 0.2633619146721000170 ) ) ;
#24696=EDGE_CURVE ( 'NONE', #3531, #36712, #57625, .T. ) ;
#24704=CARTESIAN_POINT ( 'NONE',  ( -2.815196241353000506, -81.56803455456798702, -2.487173068765999862 ) ) ;
#24711=CARTESIAN_POINT ( 'NONE',  ( -3.999999999999815259, -78.72610001270986402, -1.678385095468384722E-14 ) ) ;
#24724=CARTESIAN_POINT ( 'NONE',  ( -3.181627547869000150, -83.35221544543098560, 2.362885332182999676 ) ) ;
#24734=ORIENTED_EDGE ( 'NONE', *, *, #18313, .T. ) ;
#24736=CARTESIAN_POINT ( 'NONE',  ( 2.984579200595963488, -79.00013989958746663, -2.163174824610843316 ) ) ;
#24847=CARTESIAN_POINT ( 'NONE',  ( -3.308771268993000003, -83.30055803339699594, -1.278124539089000145 ) ) ;
#24870=CARTESIAN_POINT ( 'NONE',  ( -3.107766917196799206, -84.86666667301983580, -2.600398495668877263 ) ) ;
#24889=SURFACE_STYLE_FILL_AREA ( #56191 ) ;
#24891=EDGE_LOOP ( 'NONE', ( #33678, #11405, #26033, #27270 ) ) ;
#24964=CARTESIAN_POINT ( 'NONE',  ( 3.262642887984999795, -82.34119486992599946, -1.391544775636999853 ) ) ;
#24975=CARTESIAN_POINT ( 'NONE',  ( -4.185964006270539883, -86.39318692614395445, -0.4007007872290511696 ) ) ;
#24987=CARTESIAN_POINT ( 'NONE',  ( 1.459331535918999778, -80.36553455456798645, -3.461461188124999921 ) ) ;
#24992=CARTESIAN_POINT ( 'NONE',  ( -3.299870502076000189, -84.66724735065199070, 1.294534069721999803 ) ) ;
#25007=CARTESIAN_POINT ( 'NONE',  ( 3.241578942234999872, -85.83735717367099483, -1.443243930775000239 ) ) ;
#25018=CARTESIAN_POINT ( 'NONE',  ( 0.8528862836333073183, -78.91694510676077812, -3.387194058658217877 ) ) ;
#25032=CARTESIAN_POINT ( 'NONE',  ( -3.380118193142000127, -86.40321104922298900, 1.504925578873999914 ) ) ;
#25047=CARTESIAN_POINT ( 'NONE',  ( -1.907247829674572071, -81.95677084859232764, -3.530101888956680423 ) ) ;
#25129=CARTESIAN_POINT ( 'NONE',  ( -2.266776927424000387, -84.50306218606498021, 2.728239737002000176 ) ) ;
#25153=CARTESIAN_POINT ( 'NONE',  ( -1.922652541418499839, -84.44270833512283048, 3.565982039631133471 ) ) ;
#25195=CARTESIAN_POINT ( 'NONE',  ( 4.606177061618105917, -86.17851881763701272, 0.5287147981155758680 ) ) ;
#25228=CARTESIAN_POINT ( 'NONE',  ( 2.301294264262669476, -78.54828561723800817, 3.984678255335871278 ) ) ;
#25254=CARTESIAN_POINT ( 'NONE',  ( -3.541111988782999820, -80.24573954672798948, 0.1596783345572000135 ) ) ;
#25266=CARTESIAN_POINT ( 'NONE',  ( 0.4496812306607233523, -86.40321104920798234, -4.272713054705454816 ) ) ;
#25275=CARTESIAN_POINT ( 'NONE',  ( -1.036694699304999912, -81.08703455456799247, 3.610626844383000300 ) ) ;
#25280=CARTESIAN_POINT ( 'NONE',  ( 0.2485007264108999858, -85.14824735065198524, -3.535988008354999934 ) ) ;
#25301=CARTESIAN_POINT ( 'NONE',  ( 0.2050548769952000028, -85.83208224847899714, 4.167066004140999702 ) ) ;
#25306=CARTESIAN_POINT ( 'NONE',  ( 2.627793897904080023, -78.98480243775595966, -2.477488290611707278 ) ) ;
#25324=CARTESIAN_POINT ( 'NONE',  ( -3.661088936265289195, -78.99318692614359350, -2.068643027229794651 ) ) ;
#25332=CARTESIAN_POINT ( 'NONE',  ( 3.912590402935000267, -82.39999999999999147, -0.8316467632710000668 ) ) ;
#25334=CARTESIAN_POINT ( 'NONE',  ( -4.014024930567999583, -78.67863830014491100, 0.5804966311653999567 ) ) ;
#25345=CARTESIAN_POINT ( 'NONE',  ( 3.106054555984999688, -86.09999999999999432, -1.382904586457999851 ) ) ;
#25421=CARTESIAN_POINT ( 'NONE',  ( -2.902481905820999852, -86.07258307901300043, 2.039564730455999619 ) ) ;
#25439=CARTESIAN_POINT ( 'NONE',  ( 3.914500761937000028, -78.48547955770028750, -1.429791614965258972E-15 ) ) ;
#25505=EDGE_CURVE ( 'NONE', #26598, #50685, #42059, .T. ) ;
#25515=CARTESIAN_POINT ( 'NONE',  ( -0.03763178688082682161, -78.62148118236265759, 3.992727112178280358 ) ) ;
#25539=ORIENTED_EDGE ( 'NONE', *, *, #6, .T. ) ;
#25540=CARTESIAN_POINT ( 'NONE',  ( -3.024236528099000232, -80.12548912224700359, 1.849044269261000073 ) ) ;
#25552=CARTESIAN_POINT ( 'NONE',  ( -3.378711645942461317, -86.36264282632897960, -2.358076299421792754 ) ) ;
#25563=CARTESIAN_POINT ( 'NONE',  ( 2.111856289087000071, -79.23980496681159025, -2.849846186231000278 ) ) ;
#25566=CARTESIAN_POINT ( 'NONE',  ( 3.088413591160000138, -85.56019503318798058, 1.744494700727000192 ) ) ;
#25587=CARTESIAN_POINT ( 'NONE',  ( -1.733974900253999918, -82.87075447013299367, 3.797754351674999640 ) ) ;
#25594=CARTESIAN_POINT ( 'NONE',  ( -3.399999999999718359, -78.72609999968184979, 6.799999999999395861 ) ) ;
#25611=CARTESIAN_POINT ( 'NONE',  ( -2.127490919130949454, -78.96264282632948550, -3.528455608958080525 ) ) ;
#25623=CARTESIAN_POINT ( 'NONE',  ( -2.067110633960000055, -79.96757046129098967, 3.624030731625000001 ) ) ;
#25657=CARTESIAN_POINT ( 'NONE',  ( 3.992904449609000483, -78.62148118236265759, 0.000000000000000000 ) ) ;
#25778=DIRECTION ( 'NONE',  ( -1.000000000000000000, 0.000000000000000000, 0.000000000000000000 ) ) ;
#25803=CARTESIAN_POINT ( 'NONE',  ( -3.073398260277000027, -86.35846544543099412, 2.159909763142000116 ) ) ;
#25829=CARTESIAN_POINT ( 'NONE',  ( 0.4795136812456999853, -79.29531287791878924, -3.557221409453999783 ) ) ;
#25841=CARTESIAN_POINT ( 'NONE',  ( -1.415063685059226417, -86.17851879815596305, -3.099337804490793324 ) ) ;
#25842=CARTESIAN_POINT ( 'NONE',  ( 3.223004389858187047, -85.82829189952225590, 1.542474583517786879 ) ) ;
#25848=CARTESIAN_POINT ( 'NONE',  ( 4.074485157876000407, -81.09906924513698812, -0.6760801638114999346 ) ) ;
#25852=CARTESIAN_POINT ( 'NONE',  ( -2.718796855976000071, -78.87905496681159434, -2.278127071542000337 ) ) ;
#25854=CARTESIAN_POINT ( 'NONE',  ( 1.941194386247999892, -82.67419503318798490, 2.968716399090999936 ) ) ;
#25875=CARTESIAN_POINT ( 'NONE',  ( -1.752682768676000036, -84.98406384713199202, -3.786578346095999859 ) ) ;
#25880=CARTESIAN_POINT ( 'NONE',  ( 3.699999999670001039, -79.00321104920828930, 7.399999999340033163 ) ) ;
#25900=CARTESIAN_POINT ( 'NONE',  ( -3.740501297249256396, -79.00321104920828930, -2.113513782812399544 ) ) ;
#25910=CARTESIAN_POINT ( 'NONE',  ( -4.016276557929000290, -78.60958598268121023, 0.5808222549768999876 ) ) ;
#25947=CARTESIAN_POINT ( 'NONE',  ( 3.399999999999999911, -78.67390000031814168, 0.000000000000000000 ) ) ;
#25968=CARTESIAN_POINT ( 'NONE',  ( 3.333665159394799016, -86.36264282632899381, 2.421341216326561074 ) ) ;
#25987=CARTESIAN_POINT ( 'NONE',  ( 3.793360466995999936, -79.32866876341660145, -1.736943300707000093 ) ) ;
#26002=CARTESIAN_POINT ( 'NONE',  ( -2.764837346328655965, -86.10000000000000853, 3.732097096069709963 ) ) ;
#26007=CARTESIAN_POINT ( 'NONE',  ( -3.992195106911536673, -78.62148118236265759, 0.07526069398394277798 ) ) ;
#26033=ORIENTED_EDGE ( 'NONE', *, *, #25505, .T. ) ;
#26086=CARTESIAN_POINT ( 'NONE',  ( 0.2053964487923000126, -85.86974735065199127, 4.169813340600000195 ) ) ;
#26117=CARTESIAN_POINT ( 'NONE',  ( -3.461633792564999812, -81.73994274751999001, -0.7737321657921999440 ) ) ;
#26132=CARTESIAN_POINT ( 'NONE',  ( -4.276761386645500984, -86.40321104920798234, -0.4093923530758877827 ) ) ;
#26138=CARTESIAN_POINT ( 'NONE',  ( -3.095264676899999845, -82.06107264098699261, -2.734565311734000304 ) ) ;
#26141=CARTESIAN_POINT ( 'NONE',  ( -3.543454320287000137, -80.20180496681199145, 0.1596678892961000129 ) ) ;
#26144=CARTESIAN_POINT ( 'NONE',  ( -3.380058860739000082, -86.16144503318800218, 0.3695796539080999921 ) ) ;
#26146=CARTESIAN_POINT ( 'NONE',  ( 3.399999999999999911, -78.69999999999998863, 0.000000000000000000 ) ) ;
#26167=CARTESIAN_POINT ( 'NONE',  ( -2.684629700338999836, -83.35175613119999127, -3.197244650393999965 ) ) ;
#26174=CARTESIAN_POINT ( 'NONE',  ( -3.437187628289000152, -78.85171435493609238, -1.442231121412212840E-14 ) ) ;
#26190=CARTESIAN_POINT ( 'NONE',  ( 2.024107680232116291, -78.91452042059378869, -3.504731529255688649 ) ) ;
#26195=ADVANCED_FACE ( 'NONE', ( #41864 ), #18227, .T. ) ;
#26200=CARTESIAN_POINT ( 'NONE',  ( -2.945894689509000131, -81.45550264934799145, 2.958260330776999680 ) ) ;
#26237=CARTESIAN_POINT ( 'NONE',  ( 1.925855953377999974, -85.19317953870898918, -2.979199794438999849 ) ) ;
#26261=CARTESIAN_POINT ( 'NONE',  ( 4.093343120888133235, -86.36264282632899381, 0.4698497371738549200 ) ) ;
#26280=CARTESIAN_POINT ( 'NONE',  ( -4.167881196010999822, -80.17042173478499478, 0.1879410564025000008 ) ) ;
#26295=CARTESIAN_POINT ( 'NONE',  ( 3.618614839418320184, -85.83735716284300565, 2.628308734608108654 ) ) ;
#26300=CARTESIAN_POINT ( 'NONE',  ( -2.398287624620659475, -78.69999999999998863, -3.977573462190958420 ) ) ;
#26371=CARTESIAN_POINT ( 'NONE',  ( -3.328640256345000381, -85.03957450217399128, -2.445129353070000011 ) ) ;
#26383=ORIENTED_EDGE ( 'NONE', *, *, #171, .T. ) ;
#26399=CARTESIAN_POINT ( 'NONE',  ( 2.236424164684999827, -79.53195424565778637, -3.018240402847999881 ) ) ;
#26411=CARTESIAN_POINT ( 'NONE',  ( -3.589185692315953524, -86.25171438276197478, 1.679770172568654685 ) ) ;
#26418=CARTESIAN_POINT ( 'NONE',  ( -2.914327657214999867, -81.70032136754298335, 2.926637648191000363 ) ) ;
#26421=CARTESIAN_POINT ( 'NONE',  ( 2.784408088275000193, -80.80305496681198463, -2.197415289112000014 ) ) ;
#26442=CARTESIAN_POINT ( 'NONE',  ( -1.752505721091000002, -84.99032934161199648, -3.786195844160000323 ) ) ;
#26449=CARTESIAN_POINT ( 'NONE',  ( 3.437187628289000152, -78.85171435493609238, -4.209340827053006789E-16 ) ) ;
#26468=CARTESIAN_POINT ( 'NONE',  ( -3.436577009133267691, -78.85171435493609238, 0.06478620501008579280 ) ) ;
#26478=CARTESIAN_POINT ( 'NONE',  ( -2.944243145599999778, -81.52455496681199065, 2.956601854374000027 ) ) ;
#26503=CARTESIAN_POINT ( 'NONE',  ( -0.03499679800989389383, -84.32708334457048238, 3.443595259721679902 ) ) ;
#26514=CARTESIAN_POINT ( 'NONE',  ( 3.851650068366999857, -78.43735716284258785, 0.000000000000000000 ) ) ;
#26540=CARTESIAN_POINT ( 'NONE',  ( -0.5608696358174141139, -86.31452044230000809, 4.510645591149716971 ) ) ;
#26571=CARTESIAN_POINT ( 'NONE',  ( 1.589609816837670220, -86.02148118236289065, 3.662844055364274265 ) ) ;
#26575=CARTESIAN_POINT ( 'NONE',  ( 2.024107680232116291, -78.48547957940618858, -3.504731529255688649 ) ) ;
#26587=CARTESIAN_POINT ( 'NONE',  ( -4.043784919594221705, -78.69999999999998863, 2.284880126142637913 ) ) ;
#26598=VERTEX_POINT ( 'NONE', #26146 ) ;
#26654=CARTESIAN_POINT ( 'NONE',  ( 3.013741045381999939, -84.31807450217398525, 2.824158001876999613 ) ) ;
#26686=CARTESIAN_POINT ( 'NONE',  ( 2.917534638751946741, -79.31666666146197997, -1.828613902223640286 ) ) ;
#26689=CARTESIAN_POINT ( 'NONE',  ( 3.146268143924999983, -79.89270551910098561, 2.052405227492000162 ) ) ;
#26702=CARTESIAN_POINT ( 'NONE',  ( -3.422298439130150971, -86.39318692756695839, 1.601665484175957443 ) ) ;
#26703=CARTESIAN_POINT ( 'NONE',  ( 2.692109722253454240, -85.85905354011360657, 2.287895808997782332 ) ) ;
#26709=CARTESIAN_POINT ( 'NONE',  ( 1.604404035714000143, -80.85856839617498792, -3.805837802621000243 ) ) ;
#26712=CARTESIAN_POINT ( 'NONE',  ( 2.968793402029999751, -79.53150264934789959, 1.936809095135999748 ) ) ;
#26735=CARTESIAN_POINT ( 'NONE',  ( 3.046275090675000019, -84.07325862280099216, 2.854788613758000082 ) ) ;
#26742=CARTESIAN_POINT ( 'NONE',  ( 0.5495870423892605938, -78.90418355198266909, -3.893366406191818729 ) ) ;
#26747=( LENGTH_UNIT ( ) NAMED_UNIT ( * ) SI_UNIT ( .MILLI., .METRE. ) );
#26774=CARTESIAN_POINT ( 'NONE',  ( 4.118579373781999564, -80.85425264934799827, -0.6833035357645000918 ) ) ;
#26797=CARTESIAN_POINT ( 'NONE',  ( -0.7270703755450000916, -83.83321544543098014, -3.685475648053000430 ) ) ;
#26801=CARTESIAN_POINT ( 'NONE',  ( 2.209590870513934657, -85.65677084043076661, 2.597958555648024248 ) ) ;
#26839=CARTESIAN_POINT ( 'NONE',  ( -3.649946715412064613, -86.25171438276198899, 1.543298655876290448 ) ) ;
#26880=CARTESIAN_POINT ( 'NONE',  ( -0.03211093172565320647, -78.62148120184446043, -3.406944224254372600 ) ) ;
#26927=CARTESIAN_POINT ( 'NONE',  ( 3.430579573749999778, -83.83275779226799784, -0.8922415104712000389 ) ) ;
#26949=CARTESIAN_POINT ( 'NONE',  ( -2.886976430161214413, -83.01666665310567339, 2.786905270152955083 ) ) ;
#26953=CARTESIAN_POINT ( 'NONE',  ( -3.351664308082999977, -83.10399735065199422, 2.489165784748999855 ) ) ;
#26984=CARTESIAN_POINT ( 'NONE',  ( -2.879473469535999808, -79.17120297221410397, -2.412504731407000058 ) ) ;
#26995=CARTESIAN_POINT ( 'NONE',  ( -3.351152128423308785, -86.40321104920796813, 1.568368390946520918 ) ) ;
#26996=CARTESIAN_POINT ( 'NONE',  ( 3.148955979375664960, -85.83315908744809519, 1.668297098845500592 ) ) ;
#27005=CARTESIAN_POINT ( 'NONE',  ( -2.970023312147000105, -82.17746358424498965, -2.623918653887999941 ) ) ;
#27009=CARTESIAN_POINT ( 'NONE',  ( 3.383438395877000016, -82.49282046129098944, 0.3412908512157999952 ) ) ;
#27030=CARTESIAN_POINT ( 'NONE',  ( 2.260318168362000169, -82.49842648807799605, 3.456791565332999916 ) ) ;
#27052=ORIENTED_EDGE ( 'NONE', *, *, #50958, .T. ) ;
#27068=CARTESIAN_POINT ( 'NONE',  ( 0.9277797337941999789, -81.21500264934797997, 4.070482101575999323 ) ) ;
#27074=CARTESIAN_POINT ( 'NONE',  ( 1.078609919318999966, -83.66757477367698925, -3.379520766710000235 ) ) ;
#27093=CARTESIAN_POINT ( 'NONE',  ( 3.635538803723000090, -84.19396544543099026, -0.9456319026059999411 ) ) ;
#27098=CARTESIAN_POINT ( 'NONE',  ( -3.423353336519171286, -84.67395834349072459, 0.3700115578796988047 ) ) ;
#27109=CARTESIAN_POINT ( 'NONE',  ( -3.515151790187000191, -83.14892953870898396, 0.4777662710532999957 ) ) ;
#27131=CARTESIAN_POINT ( 'NONE',  ( -0.5188809666114609920, -86.39318692614398287, 4.172962832911258246 ) ) ;
#27164=CARTESIAN_POINT ( 'NONE',  ( -3.699342691684420537, -78.39678895079168797, 0.06973985258851372881 ) ) ;
#27176=CARTESIAN_POINT ( 'NONE',  ( -3.819913395574868531, -78.40681307243320930, 2.158384873251588232 ) ) ;
#27218=CARTESIAN_POINT ( 'NONE',  ( 2.586461584802999703, -84.07325862280099216, 2.423878626333000330 ) ) ;
#27246=CARTESIAN_POINT ( 'NONE',  ( 3.031356706570000448, -83.82549735065198604, -2.870622980746000419 ) ) ;
#27270=ORIENTED_EDGE ( 'NONE', *, *, #57438, .F. ) ;
#27280=CARTESIAN_POINT ( 'NONE',  ( -3.606241821240999901, -81.93696273528199470, 1.051851009248000013 ) ) ;
#27290=CARTESIAN_POINT ( 'NONE',  ( -1.645868681893847718, -86.25171438276198899, -3.604857562864015375 ) ) ;
#27291=CARTESIAN_POINT ( 'NONE',  ( -2.687989892693834815, -86.04954200792612085, 2.984330770045349635 ) ) ;
#27298=CARTESIAN_POINT ( 'NONE',  ( 4.118565555109999998, -80.96724209361498481, -0.6833944332293000468 ) ) ;
#27301=B_SPLINE_CURVE_WITH_KNOTS ( 'NONE', 3,
 ( #36402, #10139, #5124, #4537, #4830, #22829, #40549, #8964, #18991, #18410, #23120, #28114, #46165, #5690, #23700, #1289, #19282, #37272, #14836, #32832, #50005, #26949, #15432, #20447, #20161, #38150, #15131, #19568, #24582, #55882, #19867, #51463, #10423, #37861, #6862, #33426, #15720, #23991, #51753, #20734, #42306, #34003, #38443, #33129, #28703, #28408, #25153, #29284, #29572, #2734, #2160, #47628, #38731, #24870, #43179, #56461, #1873, #56172, #56750, #46755, #7151, #16310, #11596, #47333, #6273, #47041, #16014, #11018, #50877, #29002, #24290, #37568, #52039, #6571, #42598, #46455, #42888, #5983, #33718, #10725, #42006, #11303, #2445, #1574, #55583, #51171, #43463 ),
 .UNSPECIFIED., .F., .F.,
 ( 4, 2, 2, 2, 2, 2, 1, 2, 2, 2, 2, 2, 2, 2, 2, 2, 2, 2, 2, 2, 2, 2, 1, 2, 2, 2, 2, 2, 2, 2, 2, 2, 2, 2, 2, 2, 2, 2, 1, 2, 2, 2, 2, 2, 4 ),
 ( 0.000000000000000000, 0.01562500000000004510, 0.03125000000000009021, 0.04687500000000014572, 0.06250000000000019429, 0.07812500000000024980, 0.09375000000000030531, 0.1093750000000003608, 0.1250000000000004163, 0.1406250000000004718, 0.1562500000000004996, 0.1718750000000005551, 0.1875000000000006106, 0.2187500000000006384, 0.2500000000000006661, 0.2812500000000007216, 0.3125000000000007216, 0.3437500000000007216, 0.3750000000000006661, 0.4062500000000007216, 0.4375000000000007772, 0.4687500000000007216, 0.5000000000000006661, 0.5312500000000007772, 0.5625000000000007772, 0.5937500000000006661, 0.6250000000000006661, 0.6562500000000006661, 0.6875000000000006661, 0.7187500000000006661, 0.7500000000000005551, 0.7812500000000005551, 0.8125000000000005551, 0.8281250000000005551, 0.8437500000000004441, 0.8593750000000003331, 0.8750000000000003331, 0.8906250000000002220, 0.9062500000000002220, 0.9218750000000002220, 0.9375000000000002220, 0.9531250000000002220, 0.9687500000000001110, 0.9843750000000001110, 1.000000000000000000 ),
 .UNSPECIFIED. ) ;
#27304=CARTESIAN_POINT ( 'NONE',  ( -1.281696068931000188, -79.00557046129088690, -3.307832847245999464 ) ) ;
#27328=CARTESIAN_POINT ( 'NONE',  ( 4.129966972622000299, -85.26418603921399608, 0.04343303146570000328 ) ) ;
#27355=CARTESIAN_POINT ( 'NONE',  ( -2.398287624620617287, -78.72610001270986402, -3.977573462190889586 ) ) ;
#27368=CARTESIAN_POINT ( 'NONE',  ( -1.963540946778999929, -79.64403455456849201, 3.442453740513999882 ) ) ;
#27373=CARTESIAN_POINT ( 'NONE',  ( -3.318451405660999942, -86.15275002252400327, 0.9370259671568000881 ) ) ;
#27390=CARTESIAN_POINT ( 'NONE',  ( 0.1765916470397999871, -86.00157450217399457, 3.585038641099000056 ) ) ;
#27394=CARTESIAN_POINT ( 'NONE',  ( -1.116640241144032153, -84.40416667766366743, 3.258149010649826316 ) ) ;
#27428=CARTESIAN_POINT ( 'NONE',  ( -3.399999999999999911, -78.69999997992952956, 5.715921273723000819E-07 ) ) ;
#27455=CARTESIAN_POINT ( 'NONE',  ( 1.473002020459392547, -85.79678895079199208, 3.394151594327925014 ) ) ;
#27456=ORIENTED_EDGE ( 'NONE', *, *, #48114, .F. ) ;
#27459=CARTESIAN_POINT ( 'NONE',  ( 3.851650068367000745, -78.43735716284258785, -1.429791614965258972E-15 ) ) ;
#27472=CARTESIAN_POINT ( 'NONE',  ( -3.962108367559339595, -78.54828561723799396, -0.07469304045245830914 ) ) ;
#27511=CARTESIAN_POINT ( 'NONE',  ( 3.232998297510000008, -82.30958586555499323, -1.191365385135000121 ) ) ;
#27523=CARTESIAN_POINT ( 'NONE',  ( 0.3995786188288962815, -86.02148118236289065, -8.919459997437842347 ) ) ;
#27538=CARTESIAN_POINT ( 'NONE',  ( 2.264963459394000012, -85.19317953870898918, -3.503781609835999955 ) ) ;
#27568=CARTESIAN_POINT ( 'NONE',  ( 1.459243437995999981, -80.97495933943199020, -3.461499544958999586 ) ) ;
#27586=CARTESIAN_POINT ( 'NONE',  ( 1.960320388553999926, -79.69568553133959199, 3.683370289565999656 ) ) ;
#27591=CARTESIAN_POINT ( 'NONE',  ( 2.784738954513000131, -80.80932046129099433, -2.197676404043999998 ) ) ;
#27617=CARTESIAN_POINT ( 'NONE',  ( 1.290002129988000235, -84.19350903806798669, 3.970579864698999817 ) ) ;
#27627=( NAMED_UNIT ( * ) SI_UNIT ( $, .STERADIAN. ) SOLID_ANGLE_UNIT ( ) );
#27657=CARTESIAN_POINT ( 'NONE',  ( 4.118783384051000418, -79.27942549782629555, 0.3068013588580000284 ) ) ;
#27678=CARTESIAN_POINT ( 'NONE',  ( 1.948614114418999899, -85.40032450217400140, -3.014405495351000219 ) ) ;
#27719=CARTESIAN_POINT ( 'NONE',  ( 2.539779680857219279, -79.66354165636154505, 3.155564599645395596 ) ) ;
#27744=CARTESIAN_POINT ( 'NONE',  ( 3.308356911591979088, -85.80681307385599155, -1.472975398279045667 ) ) ;
#27750=CARTESIAN_POINT ( 'NONE',  ( 3.621447497675000182, -78.40681307385639798, -1.355252715606880543E-15 ) ) ;
#27763=CARTESIAN_POINT ( 'NONE',  ( -3.484880022881380768, -78.48547957940618858, -0.06569640715844060619 ) ) ;
#27780=CARTESIAN_POINT ( 'NONE',  ( -0.8140818358313716141, -83.51770834709049041, -3.346713179724626563 ) ) ;
#27802=CARTESIAN_POINT ( 'NONE',  ( 1.077770122336999981, -83.59225696173399456, -3.376889499103000070 ) ) ;
#27813=CARTESIAN_POINT ( 'NONE',  ( 0.3402453830697489967, -86.07390000031791999, -7.595013698426734017 ) ) ;
#27828=CARTESIAN_POINT ( 'NONE',  ( -4.136990165604000680, -84.71217953870899464, -0.5402383595598000410 ) ) ;
#27855=CARTESIAN_POINT ( 'NONE',  ( -1.621160707165126613, -81.95677081782697826, -3.000586557583472480 ) ) ;
#27867=CARTESIAN_POINT ( 'NONE',  ( 2.372446516949769268, -85.88464632347285033, 3.106461528215548107 ) ) ;
#27875=CARTESIAN_POINT ( 'NONE',  ( -1.151447527804999815, -81.37919147407698972, 4.010516339146000142 ) ) ;
#27879=CARTESIAN_POINT ( 'NONE',  ( 2.185995097243000007, -82.25232046129099217, -2.793946140691999869 ) ) ;
#27885=EDGE_LOOP ( 'NONE', ( #27456, #19660, #30712, #35718 ) ) ;
#27903=CARTESIAN_POINT ( 'NONE',  ( -3.978352630842000082, -86.11751568233700027, 0.4347780226346000254 ) ) ;
#27923=CARTESIAN_POINT ( 'NONE',  ( 3.383438022436999759, -82.45517979992798985, 0.3412945533484999516 ) ) ;
#27931=CARTESIAN_POINT ( 'NONE',  ( -0.03763201836869552869, -78.77851881763731967, -3.992727109996482060 ) ) ;
#27945=CARTESIAN_POINT ( 'NONE',  ( 4.074498828648000170, -80.72242549782599497, -0.6759902392087999701 ) ) ;
#27967=CARTESIAN_POINT ( 'NONE',  ( 3.086375682183999825, -85.62924735065199400, 1.743343585014999864 ) ) ;
#28010=CARTESIAN_POINT ( 'NONE',  ( 3.813617437220001793, -79.37447915313912006, -1.247836695960566900 ) ) ;
#28038=CARTESIAN_POINT ( 'NONE',  ( -0.5301359684281606865, -85.79678895079199208, 4.263478205968141310 ) ) ;
#28053=CARTESIAN_POINT ( 'NONE',  ( 2.194290416744271610, -78.40681307243320930, 3.799401686813050905 ) ) ;
#28070=CARTESIAN_POINT ( 'NONE',  ( 2.818472100349270981, -84.09583334529067145, 1.979553588263253783 ) ) ;
#28093=CARTESIAN_POINT ( 'NONE',  ( -3.348269392590999871, -83.09967856441200240, -1.293382021977999896 ) ) ;
#28104=CARTESIAN_POINT ( 'NONE',  ( 0.3624061150339111803, -85.80681307385599155, -8.089689221462933233 ) ) ;
#28114=CARTESIAN_POINT ( 'NONE',  ( 1.884805892303897945, -82.70833331645327746, 3.542755432913997193 ) ) ;
#28118=CARTESIAN_POINT ( 'NONE',  ( -3.892258265018999630, -83.27544503318799229, -1.503458620679999802 ) ) ;
#28143=CARTESIAN_POINT ( 'NONE',  ( 1.808130592854080065, -82.20729165018273932, -2.930395587151967796 ) ) ;
#28165=CARTESIAN_POINT ( 'NONE',  ( -1.405983071794000061, -82.04949591394598940, -3.931009852230000323 ) ) ;
#28169=CARTESIAN_POINT ( 'NONE',  ( 3.344834401207000152, -81.04355496681199611, 1.180527502125999773 ) ) ;
#28189=CARTESIAN_POINT ( 'NONE',  ( 0.1947808891803000098, -85.50854634175698266, 3.958280990209000372 ) ) ;
#28209=CARTESIAN_POINT ( 'NONE',  ( 0.4739133679264000421, -79.08816791445418914, -3.515676078802999704 ) ) ;
#28236=CARTESIAN_POINT ( 'NONE',  ( 3.242172098794999791, -80.60217549782598212, -2.558676140119000131 ) ) ;
#28255=CARTESIAN_POINT ( 'NONE',  ( 3.297965217643000102, -82.63071544543198854, -1.885706124222999991 ) ) ;
#28264=CARTESIAN_POINT ( 'NONE',  ( 3.399999999999999911, -78.72609999968186401, 0.000000000000000000 ) ) ;
#28297=CARTESIAN_POINT ( 'NONE',  ( -2.531415867984625034, -78.91197914798334523, -3.112890062190800222 ) ) ;
#28322=CARTESIAN_POINT ( 'NONE',  ( -2.355016251977294583, -86.02148120184399716, 3.178902848251809576 ) ) ;
#28375=B_SPLINE_CURVE_WITH_KNOTS ( 'NONE', 3,
 ( #38305, #15585, #51620, #20028, #29151, #56327, #20879, #20598, #37727, #38598, #2601, #15878, #51326, #51902, #38882, #11459, #29436, #47490, #47198, #56612, #11744, #25018, #10883, #16170, #2028, #34148, #6728, #42168, #52188, #28856, #56037, #29722, #47772, #1736, #7305, #25306, #43325, #2883, #24736, #56902, #32991, #51036, #38013, #10584, #46615, #6142, #24150, #19730, #55748, #15292, #6433, #33286, #46907, #24447, #42462, #49200, #44471, #31162, #39170, #57469, #30009, #4323, #48912, #8752, #4022, #7878, #3739, #26742, #12312, #13164, #30878, #35014, #3175, #39746, #30300, #22027, #21459, #8453, #48064, #21165, #44192, #40035 ),
 .UNSPECIFIED., .F., .F.,
 ( 4, 2, 2, 2, 2, 2, 2, 2, 1, 1, 1, 2, 2, 2, 2, 2, 1, 1, 1, 2, 2, 2, 2, 2, 2, 2, 1, 1, 1, 1, 2, 2, 2, 2, 2, 1, 1, 1, 1, 2, 2, 2, 2, 2, 2, 2, 2, 4 ),
 ( 0.000000000000000000, 0.01562499999999716893, 0.03124999999999433786, 0.04687499999999150679, 0.06249999999998866185, 0.09374999999998295808, 0.1093749999999800993, 0.1171874999999786837, 0.1210937499999779760, 0.1230468749999776290, 0.1240234374999774764, 0.1245117187499773931, 0.1249999999999773237, 0.1874999999999681088, 0.2187499999999635014, 0.2343749999999611144, 0.2421874999999600042, 0.2460937499999593936, 0.2480468749999591160, 0.2490234374999589773, 0.2499999999999588662, 0.3749999999999662492, 0.4999999999999736877, 0.6249999999999811262, 0.6874999999999849010, 0.7187499999999867883, 0.7343749999999877875, 0.7421874999999883427, 0.7460937499999885647, 0.7480468749999886757, 0.7490234374999887867, 0.7499999999999887867, 0.8124999999999883427, 0.8437499999999881206, 0.8593749999999880096, 0.8671874999999881206, 0.8710937499999880096, 0.8730468749999880096, 0.8740234374999881206, 0.8745117187499881206, 0.8749999999999881206, 0.9062499999999911182, 0.9218749999999925615, 0.9374999999999941158, 0.9531249999999955591, 0.9687499999999971134, 0.9843749999999985567, 1.000000000000000000 ),
 .UNSPECIFIED. ) ;
#28380=CARTESIAN_POINT ( 'NONE',  ( -4.094030986447999787, -78.76507046129088963, -0.8031144277722999103 ) ) ;
#28384=CARTESIAN_POINT ( 'NONE',  ( 1.925748864890999945, -85.22456467766599530, -2.978768362480000320 ) ) ;
#28397=CARTESIAN_POINT ( 'NONE',  ( -3.308356911591993743, -85.80681307385599155, 1.472975398279013692 ) ) ;
#28408=CARTESIAN_POINT ( 'NONE',  ( -1.313693873217006924, -84.40416666804125612, 3.833116371664651023 ) ) ;
#28411=CARTESIAN_POINT ( 'NONE',  ( 0.2924848206110000071, -85.07292953870899055, -4.161850282066000162 ) ) ;
#28442=CARTESIAN_POINT ( 'NONE',  ( 2.942028868608097536, -80.81979165559693001, -1.791020663990882111 ) ) ;
#28455=CARTESIAN_POINT ( 'NONE',  ( 3.440052570659030806, -85.82990816067768947, 1.702406959663651076 ) ) ;
#28460=CARTESIAN_POINT ( 'NONE',  ( -4.074342574665000605, -81.80899506498398921, -0.9106826699133000469 ) ) ;
#28488=CARTESIAN_POINT ( 'NONE',  ( 3.450559865080999877, -85.26804551122299358, 1.949262422280000129 ) ) ;
#28508=CARTESIAN_POINT ( 'NONE',  ( 3.499206421942000045, -80.89818977615198037, -0.5806240443371000204 ) ) ;
#28532=CARTESIAN_POINT ( 'NONE',  ( 3.952128152273000516, -79.16303455456849747, 0.2943874864100000099 ) ) ;
#28538=CARTESIAN_POINT ( 'NONE',  ( -3.548349909811000291, -78.96264282632948550, -1.488874400533411562E-14 ) ) ;
#28553=CARTESIAN_POINT ( 'NONE',  ( -3.579657239220000342, -86.47871544543099276, 0.3914039778855000207 ) ) ;
#28562=CARTESIAN_POINT ( 'NONE',  ( 3.805232043948999721, -82.38490367749800214, -1.402234496399000108 ) ) ;
#28596=CARTESIAN_POINT ( 'NONE',  ( 1.828892197797149732, -82.18802085116996636, -3.571177028183664337 ) ) ;
#28622=CARTESIAN_POINT ( 'NONE',  ( -2.375816180258422339, -85.94828564506400426, 3.206979491545860039 ) ) ;
#28638=CARTESIAN_POINT ( 'NONE',  ( 1.974456470848842127, -78.67390000031815589, 3.418760428718723432 ) ) ;
#28679=CARTESIAN_POINT ( 'NONE',  ( 3.544514315405999927, -85.39601319073598518, 0.03727608545351999980 ) ) ;
#28691=CARTESIAN_POINT ( 'NONE',  ( -3.451879464910993622, -85.80681307243298761, 1.536875756006014448 ) ) ;
#28703=CARTESIAN_POINT ( 'NONE',  ( -0.04117230827835093726, -84.32708333387819266, 4.051288899054856785 ) ) ;
#28735=CARTESIAN_POINT ( 'NONE',  ( -0.8546198232617973067, -82.01458331760134968, -3.302194718003578888 ) ) ;
#28752=CARTESIAN_POINT ( 'NONE',  ( 4.046592612395000010, -82.41509632510098982, -0.2667223080253999790 ) ) ;
#28766=EDGE_CURVE ( 'NONE', #36712, #3531, #33491, .T. ) ;
#28783=CARTESIAN_POINT ( 'NONE',  ( -3.929695901009000458, -84.42629260435599292, -0.5133031271695001063 ) ) ;
#28801=CARTESIAN_POINT ( 'NONE',  ( 2.971188159787999883, -79.56916961237898533, 1.938195294252000211 ) ) ;
#28823=CARTESIAN_POINT ( 'NONE',  ( 2.236565090990000115, -78.92253455456848599, -3.018134580346000018 ) ) ;
#28842=CARTESIAN_POINT ( 'NONE',  ( -3.513940247509999892, -86.43863211209799147, 0.9924308411892999171 ) ) ;
#28849=CARTESIAN_POINT ( 'NONE',  ( -1.732827729967000074, -82.94607228207600258, 3.795241817643000282 ) ) ;
#28856=CARTESIAN_POINT ( 'NONE',  ( 2.366083363358619351, -78.97374669511339107, -2.683407710015649261 ) ) ;
#28881=CARTESIAN_POINT ( 'NONE',  ( 3.872094496555182008, -82.58831665197764949, -0.8230422429851939059 ) ) ;
#28889=CARTESIAN_POINT ( 'NONE',  ( 1.943390883608510533, -81.20520834021384360, 3.554109968293325483 ) ) ;
#28931=CARTESIAN_POINT ( 'NONE',  ( -2.038544192961597279, -78.70000000000000284, 3.380937561918479606 ) ) ;
#28975=CARTESIAN_POINT ( 'NONE',  ( -2.856707873099999961, -84.79476111440199304, -2.098616509398999685 ) ) ;
#29002=CARTESIAN_POINT ( 'NONE',  ( 3.257100396869151204, -85.59895834756915178, 2.343891278707987968 ) ) ;
#29050=CARTESIAN_POINT ( 'NONE',  ( -3.808723190200999920, -78.60716621652929348, 1.220149157440000076 ) ) ;
#29078=CARTESIAN_POINT ( 'NONE',  ( 2.877624606631000059, -83.46428928222098875, -2.724934237387000024 ) ) ;
#29096=CARTESIAN_POINT ( 'NONE',  ( 2.784687482942999726, -80.77167385719099002, -2.197743332419999973 ) ) ;
#29118=CARTESIAN_POINT ( 'NONE',  ( -3.368240389584999939, -80.00478455456800475, -1.663225410646000046 ) ) ;
#29136=CARTESIAN_POINT ( 'NONE',  ( 2.168873741030000080, -82.99146544543100390, 3.316912045576999812 ) ) ;
#29151=CARTESIAN_POINT ( 'NONE',  ( -2.960776533348827844, -78.76333549854666671, -1.715155014509248899 ) ) ;
#29259=CARTESIAN_POINT ( 'NONE',  ( -2.858594134272999909, -84.86381343186599224, -2.100002208958999805 ) ) ;
#29284=CARTESIAN_POINT ( 'NONE',  ( -2.947487654899788367, -84.51979166928597920, 2.780664221283836390 ) ) ;
#29382=CARTESIAN_POINT ( 'NONE',  ( -3.585749735645000325, -80.37756669824999278, 0.1616911715135000149 ) ) ;
#29395=CARTESIAN_POINT ( 'NONE',  ( 2.347484846439459094, -86.31452042059399332, -3.296887854808300045 ) ) ;
#29405=CARTESIAN_POINT ( 'NONE',  ( -2.751252219471000071, -78.67817549782625974, -2.305321983890999959 ) ) ;
#29411=CARTESIAN_POINT ( 'NONE',  ( 1.095375403649999857, -84.30649735065199479, 3.371218846835000171 ) ) ;
#29436=CARTESIAN_POINT ( 'NONE',  ( 0.7347525963730557885, -78.91284375429691522, -3.410767982593458925 ) ) ;
#29464=CARTESIAN_POINT ( 'NONE',  ( -2.698602497352579732, -81.89895834794788243, -2.969860844161505753 ) ) ;
#29466=CARTESIAN_POINT ( 'NONE',  ( -2.384669060246999983, -80.44857046129098421, -3.423433742407000047 ) ) ;
#29548=CARTESIAN_POINT ( 'NONE',  ( 1.924478147487999946, -85.15551236020199610, -2.976802803591999780 ) ) ;
#29572=CARTESIAN_POINT ( 'NONE',  ( -3.361724651403247499, -84.55833333636749671, 2.260551657038760709 ) ) ;
#29588=FILL_AREA_STYLE_COLOUR ( '', #46362 ) ;
#29642=CARTESIAN_POINT ( 'NONE',  ( -3.992195115638344838, -78.62148118236265759, -0.07526023106989525313 ) ) ;
#29668=CARTESIAN_POINT ( 'NONE',  ( -3.453006609811000160, -78.85439465482099308, 0.4995584808644000230 ) ) ;
#29680=CARTESIAN_POINT ( 'NONE',  ( 2.491951192718460106, -86.40321104920799655, -3.499781323192636684 ) ) ;
#29692=CARTESIAN_POINT ( 'NONE',  ( -0.3926621439294999960, -80.24528455456798781, -3.735930744721999819 ) ) ;
#29695=CARTESIAN_POINT ( 'NONE',  ( 3.435184454807999721, -84.06599735065199752, 0.8743406370706999775 ) ) ;
#29711=CARTESIAN_POINT ( 'NONE',  ( 3.620209227050000145, -85.94828561723799965, -1.611820994701000043 ) ) ;
#29716=CARTESIAN_POINT ( 'NONE',  ( 0.3142805516909999430, -82.81955637232998413, 4.160687065221000402 ) ) ;
#29722=CARTESIAN_POINT ( 'NONE',  ( 2.420934736278871569, -78.97605044823936282, -2.640979877710285972 ) ) ;
#29734=CARTESIAN_POINT ( 'NONE',  ( -3.654181822837000215, -86.12610001214198974, 1.626946589673999854 ) ) ;
#29746=CARTESIAN_POINT ( 'NONE',  ( 3.457929002525866213, -82.32291668600672097, -2.035687669133669164 ) ) ;
#29748=CARTESIAN_POINT ( 'NONE',  ( -1.507378969381000022, -79.00557046129088690, -3.890280846631000156 ) ) ;
#29853=CARTESIAN_POINT ( 'NONE',  ( -4.036611966185642331, -78.62148118236265759, -2.280826645528176488 ) ) ;
#29955=CARTESIAN_POINT ( 'NONE',  ( 2.968874816653999993, -79.64448742432209372, 1.936686231029999927 ) ) ;
#29969=CARTESIAN_POINT ( 'NONE',  ( -3.213800095599238293, -86.36264282632896538, 1.504086442990089534 ) ) ;
#29978=CARTESIAN_POINT ( 'NONE',  ( 0.4796867442264000081, -78.91867549782628544, -3.557196995368999914 ) ) ;
#29982=CARTESIAN_POINT ( 'NONE',  ( -3.517187213417000358, -84.71844503318800434, -0.4592999679426000292 ) ) ;
#30003=CARTESIAN_POINT ( 'NONE',  ( 3.807751191731999718, -82.30958586555499323, -1.403162806651999883 ) ) ;
#30009=CARTESIAN_POINT ( 'NONE',  ( 1.034427849767293406, -78.91950550033550371, -3.765568750399868492 ) ) ;
#30028=CARTESIAN_POINT ( 'NONE',  ( 1.978576907476573332, -78.77851879815550262, -3.425895241845610339 ) ) ;
#30059=EDGE_LOOP ( 'NONE', ( #51553, #17689, #37371, #56989 ) ) ;
#30173=ORIENTED_EDGE ( 'NONE', *, *, #57590, .F. ) ;
#30220=CARTESIAN_POINT ( 'NONE',  ( 3.835454611662000080, -84.19396544543099026, -0.9976315582358001866 ) ) ;
#30249=CARTESIAN_POINT ( 'NONE',  ( -0.05248490571276999417, -80.01681542480598353, 3.589009686742000493 ) ) ;
#30260=CARTESIAN_POINT ( 'NONE',  ( 2.314946975858551248, -86.25171435493599859, -3.251190558613353598 ) ) ;
#30267=CARTESIAN_POINT ( 'NONE',  ( -3.553512937130000271, -80.61420806598900413, -1.754575727644000160 ) ) ;
#30270=CARTESIAN_POINT ( 'NONE',  ( 0.5655101697426998530, -82.05675264934798463, -3.499301708937000210 ) ) ;
#30273=CARTESIAN_POINT ( 'NONE',  ( 2.588229337315999690, -84.11719503318798274, 2.425413624993999928 ) ) ;
#30295=CARTESIAN_POINT ( 'NONE',  ( -1.831741169393000135, -85.95233266374599168, 3.748532606556000069 ) ) ;
#30300=CARTESIAN_POINT ( 'NONE',  ( -2.309105416988717074, -78.81515588160679897, -3.255121060972665514 ) ) ;
#30306=( GEOMETRIC_REPRESENTATION_CONTEXT ( 3 ) GLOBAL_UNCERTAINTY_ASSIGNED_CONTEXT ( ( #15978 ) ) GLOBAL_UNIT_ASSIGNED_CONTEXT ( ( #33736, #20468, #47644 ) ) REPRESENTATION_CONTEXT ( 'NONE', 'WORKASPACE' ) );
#30317=CARTESIAN_POINT ( 'NONE',  ( -3.484880015263546404, -78.91452042059380290, 0.06569681124688563079 ) ) ;
#30328=CARTESIAN_POINT ( 'NONE',  ( 4.049271016118000333, -82.37741931601499346, -0.2669009547921000203 ) ) ;
#30365=CARTESIAN_POINT ( 'NONE',  ( 3.621447497675000182, -78.40681307385639798, 0.000000000000000000 ) ) ;
#30393=CARTESIAN_POINT ( 'NONE',  ( 3.380118192975835711, -86.40321104920799655, -1.504925579246371159 ) ) ;
#30413=CARTESIAN_POINT ( 'NONE',  ( -1.151331214113000101, -81.37292597959698526, 4.010111216070000317 ) ) ;
#30514=CARTESIAN_POINT ( 'NONE',  ( -3.905292900344000007, -86.19041401731898588, 1.102959312106999823 ) ) ;
#30538=CARTESIAN_POINT ( 'NONE',  ( -0.9409828818170595799, -79.00833332933186171, -3.278629126855026499 ) ) ;
#30542=CARTESIAN_POINT ( 'NONE',  ( -0.3752914285551999796, -80.73831797169299307, -3.569720093411000050 ) ) ;
#30553=CARTESIAN_POINT ( 'NONE',  ( -1.447626959621158838, -86.31452042059397911, -3.170659391604351285 ) ) ;
#30554=CARTESIAN_POINT ( 'NONE',  ( 2.115553404172148433, -85.88479124992733205, 2.777125045544115434 ) ) ;
#30555=ADVANCED_FACE ( 'NONE', ( #21195 ), #5024, .T. ) ;
#30561=CARTESIAN_POINT ( 'NONE',  ( -4.052938665471999435, -78.93456160447509262, -0.7948260755284000112 ) ) ;
#30564=CARTESIAN_POINT ( 'NONE',  ( -3.459341176421000252, -81.69600264934798872, -0.7732545034468999434 ) ) ;
#30566=CARTESIAN_POINT ( 'NONE',  ( 0.2670125575351000036, -82.86349735065198274, 3.534640024372999623 ) ) ;
#30587=CARTESIAN_POINT ( 'NONE',  ( 3.685509519663000333, -82.57905554179599505, 1.956350997232000122 ) ) ;
#30590=ORIENTED_EDGE ( 'NONE', *, *, #22230, .F. ) ;
#30593=CARTESIAN_POINT ( 'NONE',  ( 3.485499217011999828, -78.91452042059380290, -4.268505459544351420E-16 ) ) ;
#30611=CARTESIAN_POINT ( 'NONE',  ( -3.957350048490399175, -78.91452044229970397, -2.236040895654427985 ) ) ;
#30621=CARTESIAN_POINT ( 'NONE',  ( 2.571168007570000302, -82.24605496681199668, -3.286240184565999645 ) ) ;
#30677=CARTESIAN_POINT ( 'NONE',  ( 1.387607402548411528, -86.31452042059399332, 3.197381817703935702 ) ) ;
#30712=ORIENTED_EDGE ( 'NONE', *, *, #19022, .T. ) ;
#30716=CARTESIAN_POINT ( 'NONE',  ( -3.913805347717917105, -78.48547955770028750, 0.07378289354579982418 ) ) ;
#30743=ORIENTED_EDGE ( 'NONE', *, *, #171, .F. ) ;
#30797=CARTESIAN_POINT ( 'NONE',  ( -3.349785279347999634, -83.03494503318799502, 2.487770294745999866 ) ) ;
#30823=CARTESIAN_POINT ( 'NONE',  ( -1.454554856007286512, -78.96979166281558093, -3.085434141896665317 ) ) ;
#30826=CARTESIAN_POINT ( 'NONE',  ( -2.147210328137000079, -80.73445849046999001, -3.082346235878000051 ) ) ;
#30838=CARTESIAN_POINT ( 'NONE',  ( 0.4861418710280006605, -86.09999999999979536, -4.619149248742774994 ) ) ;
#30846=CARTESIAN_POINT ( 'NONE',  ( 3.342627291359000274, -80.97450264934799691, 1.179748523689000184 ) ) ;
#30871=CARTESIAN_POINT ( 'NONE',  ( -3.362339023590000142, -84.87007892634498774, -2.470067118709999843 ) ) ;
#30878=CARTESIAN_POINT ( 'NONE',  ( -0.7377377962817491808, -78.86606320632056111, -3.889143611529064515 ) ) ;
#30889=CARTESIAN_POINT ( 'NONE',  ( -3.112536536121000008, -86.17851878748298589, 1.385790882648999967 ) ) ;
#30896=CARTESIAN_POINT ( 'NONE',  ( 1.996052055574059514, -78.85171435493610659, -3.456153366506571789 ) ) ;
#30904=CARTESIAN_POINT ( 'NONE',  ( 3.840130277397999947, -82.29725264934799611, -1.637844927514000126 ) ) ;
#30940=CARTESIAN_POINT ( 'NONE',  ( 1.096228918643000094, -84.23117953870900010, 3.373845695877999873 ) ) ;
#30964=CARTESIAN_POINT ( 'NONE',  ( 4.443227334435309039, -86.36264283715698298, 0.5100107989077657944 ) ) ;
#30998=FACE_OUTER_BOUND ( 'NONE', #19787, .T. ) ;
#31003=CARTESIAN_POINT ( 'NONE',  ( -3.484880015263546404, -78.48547957940618858, 0.06569681124688563079 ) ) ;
#31015=CARTESIAN_POINT ( 'NONE',  ( 2.318769420003345072, -78.62148118236264338, 4.014936390581685721 ) ) ;
#31080=CARTESIAN_POINT ( 'NONE',  ( 4.045881407263999918, -84.06599735065199752, 1.029778334665000017 ) ) ;
#31107=CARTESIAN_POINT ( 'NONE',  ( -3.888947658978999744, -79.05095254773289071, -0.7626656263158999582 ) ) ;
#31120=CARTESIAN_POINT ( 'NONE',  ( -3.622867166186615417, -86.09999999999976694, 1.695533395769283080 ) ) ;
#31121=CARTESIAN_POINT ( 'NONE',  ( 2.038851226788696458, -85.88796493201749627, 2.830303225609521078 ) ) ;
#31127=CARTESIAN_POINT ( 'NONE',  ( 3.459248248861000352, -79.77631457584399755, 2.256571552193000318 ) ) ;
#31130=CARTESIAN_POINT ( 'NONE',  ( 0.4737152913811000232, -79.05050264934789084, -3.512914691605000250 ) ) ;
#31154=CARTESIAN_POINT ( 'NONE',  ( -3.379256011433000140, -85.86543811554798822, 2.374592366029999901 ) ) ;
#31162=CARTESIAN_POINT ( 'NONE',  ( 1.358304078313203656, -78.93004670938226752, -3.649112436916695401 ) ) ;
#31192=CARTESIAN_POINT ( 'NONE',  ( -2.067319464631000248, -79.96130496681199418, 3.624396850766999911 ) ) ;
#31215=CARTESIAN_POINT ( 'NONE',  ( -3.015791237393999680, -83.35221544543098560, 2.239724409143000194 ) ) ;
#31256=CARTESIAN_POINT ( 'NONE',  ( 1.558396630254053949, -86.31452044229999387, 3.590921352246257747 ) ) ;
#31293=CARTESIAN_POINT ( 'NONE',  ( -3.444390624473300910, -78.62148120184446043, -1.946200917927131790 ) ) ;
#31350=CARTESIAN_POINT ( 'NONE',  ( -1.472243751803000045, -82.87075447013299367, 3.224510409186000182 ) ) ;
#31358=CARTESIAN_POINT ( 'NONE',  ( 3.308356911591999960, -86.39318692614399708, -1.472975398278999926 ) ) ;
#31376=CARTESIAN_POINT ( 'NONE',  ( 4.129967680665999730, -85.64082450217398446, 0.04325065736083000267 ) ) ;
#31410=CARTESIAN_POINT ( 'NONE',  ( 3.415484286716000017, -79.65220467013898542, -1.563917429438999918 ) ) ;
#31421=CARTESIAN_POINT ( 'NONE',  ( -4.623525823813485758, -86.09999999999976694, -0.4425863276891531251 ) ) ;
#31429=CARTESIAN_POINT ( 'NONE',  ( -2.265283964738999956, -80.73445849046999001, -3.251842360486000061 ) ) ;
#31433=CARTESIAN_POINT ( 'NONE',  ( 3.481401174418000011, -82.24559216449299015, -0.2294707599881000148 ) ) ;
#31453=CARTESIAN_POINT ( 'NONE',  ( 4.002556386389000131, -83.82118105601298907, 1.018850255173999964 ) ) ;
#31460=CARTESIAN_POINT ( 'NONE',  ( 3.999999999999675371, -78.70000000000000284, 7.999999999999384492 ) ) ;
#31469=ORIENTED_EDGE ( 'NONE', *, *, #24696, .T. ) ;
#31489=CARTESIAN_POINT ( 'NONE',  ( 3.795949068449000041, -79.29100264934788811, -1.737921346834000014 ) ) ;
#31513=CARTESIAN_POINT ( 'NONE',  ( -3.341467261686000167, -84.79907450217399401, 1.310852413871999911 ) ) ;
#31530=CARTESIAN_POINT ( 'NONE',  ( 1.941425054909000192, -82.66792953870898941, 2.969069166356000267 ) ) ;
#31552=CARTESIAN_POINT ( 'NONE',  ( -3.268206247460667235, -86.36264282632899381, 1.381888203336044896 ) ) ;
#31584=CARTESIAN_POINT ( 'NONE',  ( -2.662296488502435832, -85.83735716284300565, 3.593683008806336066 ) ) ;
#31590=CARTESIAN_POINT ( 'NONE',  ( -0.03204405817076288326, -78.67390000031814168, -3.399848993460840685 ) ) ;
#31602=CARTESIAN_POINT ( 'NONE',  ( 3.621447497675000626, -78.40681307385641219, 2.137281866361618654 ) ) ;
#31644=CARTESIAN_POINT ( 'NONE',  ( 0.2703574106265999588, -82.61867690334500480, 3.579198825151999941 ) ) ;
#31671=CARTESIAN_POINT ( 'NONE',  ( -2.639344177053999818, -84.67882450217399537, 3.176848410495999975 ) ) ;
#31701=CARTESIAN_POINT ( 'NONE',  ( -3.686243627255000099, -79.05095254773289071, -0.7229131249021999439 ) ) ;
#31711=CARTESIAN_POINT ( 'NONE',  ( 0.4861418710279412081, -86.12610001270962812, -4.619149248742044911 ) ) ;
#31712=CARTESIAN_POINT ( 'NONE',  ( 3.180025244547568519, -85.83115353646098811, 1.616841368705626891 ) ) ;
#31720=CARTESIAN_POINT ( 'NONE',  ( -4.007874235025999710, -81.68874464050298911, 1.168997190988000145 ) ) ;
#31725=CARTESIAN_POINT ( 'NONE',  ( -0.3708117234359000203, -80.56882046129099706, -3.528037880666999637 ) ) ;
#31748=CARTESIAN_POINT ( 'NONE',  ( -3.852741965086999620, -83.09967856441200240, -1.488251573779999948 ) ) ;
#31788=CARTESIAN_POINT ( 'NONE',  ( -1.492232953141999774, -78.79842549782625838, -3.851191634116000184 ) ) ;
#31794=CARTESIAN_POINT ( 'NONE',  ( 3.088701407003000110, -85.59158141794600283, 1.744844263460000100 ) ) ;
#31803=CIRCLE ( 'NONE', #8251, 4.000000000000001776 ) ;
#31813=CARTESIAN_POINT ( 'NONE',  ( -3.559173281348999573, -84.91932450217399264, -0.4647828150262000024 ) ) ;
#31831=EDGE_CURVE ( 'NONE', #313, #35853, #15783, .T. ) ;
#31852=CARTESIAN_POINT ( 'NONE',  ( -0.5721033155193936404, -86.17851881763701272, 4.600989486740316714 ) ) ;
#31882=CARTESIAN_POINT ( 'NONE',  ( 3.965107357240976071, -85.94828564506400426, 0.4551303408112303273 ) ) ;
#31885=CARTESIAN_POINT ( 'NONE',  ( 2.103055900234938491, -78.40681307385639798, -3.641429946303727405 ) ) ;
#31896=CARTESIAN_POINT ( 'NONE',  ( 3.485499217011999828, -78.48547957940618858, -4.268505459544351420E-16 ) ) ;
#31938=CARTESIAN_POINT ( 'NONE',  ( 1.972671892376000047, -85.38829592649000233, 3.196865563702000035 ) ) ;
#31949=CARTESIAN_POINT ( 'NONE',  ( -3.380118192975993807, -85.79678895079199208, 1.504925579246014111 ) ) ;
#31965=CARTESIAN_POINT ( 'NONE',  ( -1.752823108115999950, -84.95894503318798741, -3.786512042056999761 ) ) ;
#31996=CARTESIAN_POINT ( 'NONE',  ( -2.532729724196000287, -81.70032136754298335, 2.543427862400999828 ) ) ;
#32007=CARTESIAN_POINT ( 'NONE',  ( -1.746263085257492076, -86.01534311877844630, 3.604194403367339650 ) ) ;
#32013=CARTESIAN_POINT ( 'NONE',  ( -2.945856725507999929, -81.56849421602200323, 2.958299893872000208 ) ) ;
#32017=CARTESIAN_POINT ( 'NONE',  ( 3.225488960277000050, -79.36632046129089701, -1.476744291601000070 ) ) ;
#32040=CARTESIAN_POINT ( 'NONE',  ( -3.935772911773000704, -85.98568853081499697, 0.4301246578429000489 ) ) ;
#32070=CARTESIAN_POINT ( 'NONE',  ( -0.03734840871947565227, -78.85171438276199751, -3.962636352599350875 ) ) ;
#32085=CARTESIAN_POINT ( 'NONE',  ( 0.6322550835224000076, -81.80853455456798429, -3.912310357318999454 ) ) ;
#32106=CARTESIAN_POINT ( 'NONE',  ( 3.478486924372000022, -84.19782450217398662, 0.8853622020908999968 ) ) ;
#32110=CARTESIAN_POINT ( 'NONE',  ( -2.243884148121614075, -84.90520834277080553, -2.611532020247723906 ) ) ;
#32143=CARTESIAN_POINT ( 'NONE',  ( -3.399999999999999911, -78.67389998024768261, 5.715921273723000819E-07 ) ) ;
#32145=CARTESIAN_POINT ( 'NONE',  ( 4.039219890226469545, -79.43229165378355106, -0.3057202085838180983 ) ) ;
#32170=CARTESIAN_POINT ( 'NONE',  ( 4.177667811529485853, -85.80681307385597734, 0.4795288509369720620 ) ) ;
#32173=CARTESIAN_POINT ( 'NONE',  ( 3.621447497674998850, -78.40681307385639798, -2.137281964302801374 ) ) ;
#32183=CIRCLE ( 'NONE', #20862, 4.000000000000000888 ) ;
#32205=CARTESIAN_POINT ( 'NONE',  ( 1.602084971415322467, -82.70833334961002947, 3.011342165955993799 ) ) ;
#32228=CARTESIAN_POINT ( 'NONE',  ( -2.279403987710999946, -83.35175613119999127, -2.714643365851999945 ) ) ;
#32238=CARTESIAN_POINT ( 'NONE',  ( -5.884117869723990424, -86.02148120184399716, -4.839282714492908255 ) ) ;
#32252=CARTESIAN_POINT ( 'NONE',  ( 4.172307908842999957, -85.43994503318799616, 0.04369406100051999309 ) ) ;
#32280=CARTESIAN_POINT ( 'NONE',  ( 3.194519230552451905, -80.85833332211321078, -1.285379839507373667 ) ) ;
#32296=CARTESIAN_POINT ( 'NONE',  ( -4.168302257862000815, -80.17668722926399028, 0.1879600432223000051 ) ) ;
#32305=B_SPLINE_CURVE_WITH_KNOTS ( 'NONE', 3,
 ( #14725, #18598, #45466, #5008, #45172, #23883, #40734, #45763, #28297, #14146, #1474, #23013, #19463, #36587, #899, #325, #4723, #37459, #54608, #15025, #23591, #49603, #9150, #28010, #32145, #18303, #50185, #22721, #27719, #5297, #23307, #36296, #41314, #32723, #18880, #19175, #36876, #54887, #14437, #55183, #50774, #32432, #50477, #10029, #46057, #42196, #51067, #56642, #33318, #47799, #37756, #55777, #47520, #10615, #38909, #28889, #46937, #2628, #1766, #38625, #7049, #16200, #2343, #20060, #20907, #33892, #56928, #11771, #43349, #11491, #29464, #7331, #25047, #6462, #43069, #19759, #15326, #51354, #20625, #28596, #33020, #34178, #10912, #52214, #29746, #38047, #51932, #25332 ),
 .UNSPECIFIED., .F., .F.,
 ( 4, 2, 2, 2, 2, 2, 1, 2, 2, 2, 2, 2, 2, 2, 2, 2, 2, 2, 2, 2, 2, 2, 2, 2, 2, 2, 2, 2, 2, 2, 2, 2, 2, 2, 2, 2, 2, 2, 1, 2, 2, 2, 2, 2, 4 ),
 ( 0.000000000000000000, 0.01562500000000002776, 0.03125000000000005551, 0.04687500000000008327, 0.06250000000000011102, 0.07812500000000012490, 0.09375000000000013878, 0.1093750000000001388, 0.1250000000000001388, 0.1406250000000001388, 0.1562500000000001388, 0.1718750000000001388, 0.1875000000000001388, 0.2187500000000001388, 0.2500000000000001110, 0.2812500000000001110, 0.3125000000000001110, 0.3437500000000001110, 0.3750000000000001110, 0.4062500000000000555, 0.4375000000000000000, 0.4687499999999999445, 0.4999999999999998890, 0.5312499999999997780, 0.5624999999999997780, 0.5937499999999996669, 0.6249999999999996669, 0.6562499999999995559, 0.6874999999999995559, 0.7187499999999994449, 0.7499999999999995559, 0.7812499999999995559, 0.8124999999999996669, 0.8281249999999996669, 0.8437499999999996669, 0.8593749999999997780, 0.8749999999999997780, 0.8906249999999997780, 0.9062499999999997780, 0.9218749999999998890, 0.9374999999999998890, 0.9531249999999998890, 0.9687499999999998890, 0.9843750000000000000, 1.000000000000000000 ),
 .UNSPECIFIED. ) ;
#32327=CARTESIAN_POINT ( 'NONE',  ( -3.886561630247999943, -84.55426028386798976, 1.524548671433000102 ) ) ;
#32339=SURFACE_STYLE_USAGE ( .BOTH. , #40039 ) ;
#32350=CARTESIAN_POINT ( 'NONE',  ( -2.718916690774999534, -78.85393255997098549, -2.277985697799999709 ) ) ;
#32372=CARTESIAN_POINT ( 'NONE',  ( 0.5519595447327000359, -78.91867549782628544, -4.093147992351998887 ) ) ;
#32392=CARTESIAN_POINT ( 'NONE',  ( -2.936671086216000148, -86.24207450217399185, 2.063821221035999631 ) ) ;
#32428=CARTESIAN_POINT ( 'NONE',  ( -3.914500761937000028, -78.48547955772869500, -9.512529912660000101E-10 ) ) ;
#32432=CARTESIAN_POINT ( 'NONE',  ( -2.759188190257293449, -80.39583333119153963, -2.967398781983584310 ) ) ;
#32442=CARTESIAN_POINT ( 'NONE',  ( -3.654181822837000215, -86.09999999943198645, 1.626946589673999854 ) ) ;
#32457=CARTESIAN_POINT ( 'NONE',  ( -0.4871519710310731610, -86.10000000000017906, 3.917790784212267674 ) ) ;
#32473=CARTESIAN_POINT ( 'NONE',  ( 2.236739823803636451, -78.43735716284257364, 3.872902599707189530 ) ) ;
#32492=CARTESIAN_POINT ( 'NONE',  ( -1.073871440473841865, -82.90104168234370263, 3.271588444796262873 ) ) ;
#32510=CARTESIAN_POINT ( 'NONE',  ( 2.570908280542000046, -82.25232046129099217, -3.285908224385000409 ) ) ;
#32515=CARTESIAN_POINT ( 'NONE',  ( 2.986993022240000073, -82.13767524227699823, -1.707903102581999955 ) ) ;
#32528=CARTESIAN_POINT ( 'NONE',  ( 0.3409554497599163736, -86.02148120184399716, -7.610863924474937647 ) ) ;
#32542=CARTESIAN_POINT ( 'NONE',  ( -0.8075106742674000859, -83.50967953870899407, -4.093222644815999622 ) ) ;
#32570=CARTESIAN_POINT ( 'NONE',  ( 3.437653462762137568, -80.93541665514577232, -0.2151425978537864214 ) ) ;
#32590=CARTESIAN_POINT ( 'NONE',  ( -3.743424489665999833, -80.36598997120898957, -1.848346091329999830 ) ) ;
#32594=CARTESIAN_POINT ( 'NONE',  ( -3.180808344062000081, -80.32832046129098558, -1.570672117285999869 ) ) ;
#32616=CARTESIAN_POINT ( 'NONE',  ( 0.2779842904343000076, -84.78704385015599598, -3.953316927815999637 ) ) ;
#32623=CARTESIAN_POINT ( 'NONE',  ( -3.851650068366999857, -78.96264283715740362, -1.616138016926814209E-14 ) ) ;
#32637=CARTESIAN_POINT ( 'NONE',  ( -1.194690127457000095, -81.97417810200299471, -3.340252635762999578 ) ) ;
#32660=CARTESIAN_POINT ( 'NONE',  ( 1.604500897319000030, -80.48192549782599770, -3.805795630178999911 ) ) ;
#32681=CARTESIAN_POINT ( 'NONE',  ( -3.193955991187000354, -85.15596544543099355, -2.346193924555000088 ) ) ;
#32693=CARTESIAN_POINT ( 'NONE',  ( 3.407095545933000569, -78.77851879815550262, 0.000000000000000000 ) ) ;
#32719=CARTESIAN_POINT ( 'NONE',  ( 1.577629893834067598, -86.25171438276198899, 3.635239426043075373 ) ) ;
#32723=CARTESIAN_POINT ( 'NONE',  ( -1.781408810351462479, -79.93333332603567953, 3.639624897007596616 ) ) ;
#32733=CARTESIAN_POINT ( 'NONE',  ( -3.140027144888993593, -85.94828564506399005, 1.398030157552013319 ) ) ;
#32750=CARTESIAN_POINT ( 'NONE',  ( -3.335532751159927312, -85.80681307385599155, 1.410355715538893051 ) ) ;
#32766=CARTESIAN_POINT ( 'NONE',  ( -3.913805356273367675, -78.48547955770028750, -0.07378243972141844409 ) ) ;
#32784=CARTESIAN_POINT ( 'NONE',  ( -3.219061024817564842, -83.28645834781006840, -1.224520844437955613 ) ) ;
#32800=CARTESIAN_POINT ( 'NONE',  ( -3.198229570894999707, -78.87905496681159434, -2.679852064138000145 ) ) ;
#32807=CARTESIAN_POINT ( 'NONE',  ( -3.299912862228999710, -84.55426028386798976, 1.294428919074000151 ) ) ;
#32821=CARTESIAN_POINT ( 'NONE',  ( 0.3854429861649060207, -85.83735716284299144, -8.603922067879931745 ) ) ;
#32832=CARTESIAN_POINT ( 'NONE',  ( -2.134093098436142366, -82.95885415248338290, 3.397881310131980470 ) ) ;
#32835=CARTESIAN_POINT ( 'NONE',  ( -1.752646046354000120, -84.95267953870899191, -3.786129546818000069 ) ) ;
#32862=CARTESIAN_POINT ( 'NONE',  ( -1.514197290259749362, -79.93333332572275651, 3.093681355356981744 ) ) ;
#32876=CARTESIAN_POINT ( 'NONE',  ( 0.9182913743456745381, -85.93361904366226156, 3.850309887564324463 ) ) ;
#32882=CARTESIAN_POINT ( 'NONE',  ( 3.981833008139999741, -82.53049761187099875, 0.4016559218788000041 ) ) ;
#32909=CARTESIAN_POINT ( 'NONE',  ( 1.204975038778999918, -83.34403886695498898, -3.775450321737999992 ) ) ;
#32932=CARTESIAN_POINT ( 'NONE',  ( 2.784356622819999849, -80.77793935167099448, -2.197482209534999953 ) ) ;
#32934=ORIENTED_EDGE ( 'NONE', *, *, #53131, .F. ) ;
#32956=CARTESIAN_POINT ( 'NONE',  ( 3.603372836998999684, -79.04278455456849883, -1.649753055453999862 ) ) ;
#32961=CARTESIAN_POINT ( 'NONE',  ( -3.851650068366999857, -78.96264283715740362, -1.616138016926814209E-14 ) ) ;
#32976=CARTESIAN_POINT ( 'NONE',  ( -3.689341079140000090, -84.91546544543099628, 1.447322771837999955 ) ) ;
#32991=CARTESIAN_POINT ( 'NONE',  ( 2.981707138340699004, -78.99744281236651489, -2.266066515766057332 ) ) ;
#33020=CARTESIAN_POINT ( 'NONE',  ( 2.112424695814874909, -82.20729168471808634, -3.411783024464547953 ) ) ;
#33044=CARTESIAN_POINT ( 'NONE',  ( 3.274617103212182911, -85.88547957940600952, 2.378452838117370405 ) ) ;
#33059=CARTESIAN_POINT ( 'NONE',  ( -0.03211073419994320277, -78.62148120184446043, 3.406944226116074503 ) ) ;
#33103=CARTESIAN_POINT ( 'NONE',  ( -2.902137050060999979, -86.06631758453399073, 2.039322401418999675 ) ) ;
#33117=CARTESIAN_POINT ( 'NONE',  ( 0.3781279528989071603, -85.80681307243297340, -8.440634685827930639 ) ) ;
#33129=CARTESIAN_POINT ( 'NONE',  ( 1.285423637123966012, -84.24999999971510078, 3.956127134342454887 ) ) ;
#33132=CARTESIAN_POINT ( 'NONE',  ( -1.732798278134000114, -82.90842953870898668, 3.795253925594999966 ) ) ;
#33159=CARTESIAN_POINT ( 'NONE',  ( 2.964513727003363019, -82.32291664973151057, -1.751382667063024590 ) ) ;
#33171=CARTESIAN_POINT ( 'NONE',  ( -0.4631402796970099933, -85.97511617271671014, 3.956885520969557479 ) ) ;
#33203=CARTESIAN_POINT ( 'NONE',  ( 3.126063113129000204, -82.02128429901999596, -1.787420609967999896 ) ) ;
#33225=CARTESIAN_POINT ( 'NONE',  ( 0.4738570603385999780, -79.09443340893348307, -3.515258366932000111 ) ) ;
#33251=CARTESIAN_POINT ( 'NONE',  ( 3.415553852041999683, -79.04278455456849883, -1.563762801788000090 ) ) ;
#33271=CARTESIAN_POINT ( 'NONE',  ( 1.972823595576999933, -85.99771544543098400, 3.196770659314999818 ) ) ;
#33286=CARTESIAN_POINT ( 'NONE',  ( 2.589532191826647622, -78.97650882476808931, -2.803207326140070510 ) ) ;
#33311=CARTESIAN_POINT ( 'NONE',  ( -3.399395987256165430, -78.69999999999998863, 0.06408526995191232700 ) ) ;
#33318=CARTESIAN_POINT ( 'NONE',  ( 3.461210433975990597, -80.81979166925117397, -2.107082871561129611 ) ) ;
#33349=CARTESIAN_POINT ( 'NONE',  ( 3.399999999999980371, -78.70000000000000284, -1.260385025514398905E-15 ) ) ;
#33384=CARTESIAN_POINT ( 'NONE',  ( 3.194290819684984850, -86.12609999968211127, 2.320109443757182088 ) ) ;
#33402=CARTESIAN_POINT ( 'NONE',  ( 2.951756723799000337, -82.33855471126298653, -1.687755689119000202 ) ) ;
#33426=CARTESIAN_POINT ( 'NONE',  ( 2.702538634015742680, -83.74895832765501780, -3.019410798344609681 ) ) ;
#33473=CARTESIAN_POINT ( 'NONE',  ( 0.9272340829244000160, -81.25267555511598516, 4.067774877469999772 ) ) ;
#33491=B_SPLINE_CURVE_WITH_KNOTS ( 'NONE', 3,
 ( #58310, #16995, #8414, #53005, #12556, #21988, #45032, #57434, #13717, #3986, #39708, #39997, #44153, #49762, #36160, #53587, #31121, #48586, #30554, #58010, #35561, #8712, #22282, #26703, #8131, #44734, #26996, #31712, #25842, #22584, #3700, #40300, #21703, #39427, #57715, #17272, #35262, #53292, #35862, #40597, #53890, #13421, #19614, #5450, #37612, #55042, #18455, #54752, #36445, #37319, #4878, #50337, #42051, #28455, #46210, #5164, #23453, #55335, #18743, #55627, #9888, #37028, #27867, #45914, #14297, #41465, #14591, #15178, #14880, #14010, #32876, #50920, #50631, #33171, #1051, #24037, #32007, #54475, #27291, #10469, #9595, #46503 ),
 .UNSPECIFIED., .F., .F.,
 ( 4, 2, 2, 2, 2, 2, 2, 2, 1, 1, 1, 2, 2, 2, 2, 2, 1, 1, 1, 2, 2, 2, 2, 2, 2, 2, 1, 1, 1, 1, 2, 2, 2, 2, 2, 1, 1, 1, 1, 2, 2, 2, 2, 2, 2, 2, 2, 4 ),
 ( 0.000000000000000000, 0.01562499999999791833, 0.03124999999999583666, 0.04687499999999375500, 0.06249999999999167333, 0.09374999999998750999, 0.1093749999999854006, 0.1171874999999843320, 0.1210937499999838463, 0.1230468749999836242, 0.1240234374999835132, 0.1245117187499834299, 0.1249999999999833328, 0.1874999999999746314, 0.2187499999999702460, 0.2343749999999679978, 0.2421874999999668876, 0.2460937499999663325, 0.2480468749999660827, 0.2490234374999659994, 0.2499999999999658884, 0.3749999999999674705, 0.4999999999999690248, 0.6249999999999705791, 0.6874999999999713562, 0.7187499999999715783, 0.7343749999999715783, 0.7421874999999714673, 0.7460937499999714673, 0.7480468749999713562, 0.7490234374999714673, 0.7499999999999715783, 0.8124999999999781286, 0.8437499999999813483, 0.8593749999999830136, 0.8671874999999837907, 0.8710937499999842348, 0.8730468749999843459, 0.8740234374999844569, 0.8745117187499845679, 0.8749999999999845679, 0.9062499999999884537, 0.9218749999999904521, 0.9374999999999923395, 0.9531249999999942268, 0.9687499999999961142, 0.9843749999999981126, 1.000000000000000000 ),
 .UNSPECIFIED. ) ;
#33505=CARTESIAN_POINT ( 'NONE',  ( -1.577929596948000057, -84.66679343488898724, -3.409033368874000214 ) ) ;
#33524=CARTESIAN_POINT ( 'NONE',  ( -1.281863394863000050, -78.96791748997289062, -3.307769143335999917 ) ) ;
#33547=CARTESIAN_POINT ( 'NONE',  ( -0.3751936674244999992, -80.36167549782599906, -3.569729292793000219 ) ) ;
#33567=CARTESIAN_POINT ( 'NONE',  ( -1.645978843960999916, -83.23196544543098696, 3.605098035829000125 ) ) ;
#33650=CARTESIAN_POINT ( 'NONE',  ( -3.399395994687518296, -78.67390000031814168, -0.06408487577575498750 ) ) ;
#33654=CARTESIAN_POINT ( 'NONE',  ( 3.365090863054962966, -82.21166587810114379, -0.7152718134427592522 ) ) ;
#33678=ORIENTED_EDGE ( 'NONE', *, *, #31831, .F. ) ;
#33691=CARTESIAN_POINT ( 'NONE',  ( -0.6679575896827999459, -84.31375945333499544, 3.481207230722999757 ) ) ;
#33718=CARTESIAN_POINT ( 'NONE',  ( -1.046437039839534400, -85.88802085068084580, 3.873386318261602401 ) ) ;
#33736=( LENGTH_UNIT ( ) NAMED_UNIT ( * ) SI_UNIT ( .MILLI., .METRE. ) );
#33762=CARTESIAN_POINT ( 'NONE',  ( -4.005222689013000270, -81.61342682855999442, 1.168223800990999983 ) ) ;
#33785=CARTESIAN_POINT ( 'NONE',  ( 3.999999999999605649, -78.67389998729011324, 2.360693471584012659 ) ) ;
#33809=CARTESIAN_POINT ( 'NONE',  ( 3.383036022311000313, -82.46144529440799431, 0.3412540027450999824 ) ) ;
#33821=CARTESIAN_POINT ( 'NONE',  ( -1.473730639944037524, -86.36264282632897960, -3.227832877233638431 ) ) ;
#33833=CARTESIAN_POINT ( 'NONE',  ( -3.522214246756000033, -78.55792549782628953, -0.6909427624360000575 ) ) ;
#33838=CARTESIAN_POINT ( 'NONE',  ( 1.939913477021999899, -82.74324735065199832, 2.966757473053999838 ) ) ;
#33857=CARTESIAN_POINT ( 'NONE',  ( 4.171544725960999678, -82.46507062100899077, -0.06562968391973000859 ) ) ;
#33892=CARTESIAN_POINT ( 'NONE',  ( -3.942583242386946019, -81.74479167956226888, -0.7493896997992520737 ) ) ;
#33894=CARTESIAN_POINT ( 'NONE',  ( 0.5575618792808999524, -79.12582046129089974, -4.134693037866999710 ) ) ;
#33977=CARTESIAN_POINT ( 'NONE',  ( 2.575543530473000331, -83.78155969446399354, -2.438881961842000123 ) ) ;
#33998=CARTESIAN_POINT ( 'NONE',  ( -3.962108358898298821, -78.54828561723799396, 0.07469349987780400657 ) ) ;
#34003=CARTESIAN_POINT ( 'NONE',  ( 3.315849953455010990, -84.09583333138887440, 2.328886385603761155 ) ) ;
#34073=CARTESIAN_POINT ( 'NONE',  ( 3.992904449609000039, -78.62148118236264338, 2.356505866712913289 ) ) ;
#34094=CARTESIAN_POINT ( 'NONE',  ( 3.438062876453999994, -82.49041413704399872, -0.2266124004514999957 ) ) ;
#34105=CARTESIAN_POINT ( 'NONE',  ( -3.244210320986640639, -86.17851879815596305, -2.264204901133591186 ) ) ;
#34114=CARTESIAN_POINT ( 'NONE',  ( 2.314806860876999828, -81.92878455456799713, -2.958581976489000009 ) ) ;
#34120=CARTESIAN_POINT ( 'NONE',  ( -0.6865296035375000328, -83.51594503318798957, -3.479976932919000010 ) ) ;
#34143=CARTESIAN_POINT ( 'NONE',  ( -3.903163414993999769, -86.14648452804499357, 1.102130188697999946 ) ) ;
#34148=CARTESIAN_POINT ( 'NONE',  ( 2.059442021937579081, -78.96127176157177985, -2.897349721442271431 ) ) ;
#34153=FILL_AREA_STYLE_COLOUR ( '', #45390 ) ;
#34163=CARTESIAN_POINT ( 'NONE',  ( -3.140027178014999976, -86.25171435779598994, 1.398030083151000191 ) ) ;
#34178=CARTESIAN_POINT ( 'NONE',  ( 2.632379610102243639, -82.24583335181431210, -3.029167836885550802 ) ) ;
#34180=CARTESIAN_POINT ( 'NONE',  ( 0.5576182071907999083, -79.11955496681159161, -4.135110746870999776 ) ) ;
#34241=CARTESIAN_POINT ( 'NONE',  ( -0.4871519710308191420, -86.12609999968211127, 3.917790784211915955 ) ) ;
#34253=UNCERTAINTY_MEASURE_WITH_UNIT (LENGTH_MEASURE( 1.000000000000000082E-05 ), #26747, 'distance_accuracy_value', 'NONE');
#34266=CARTESIAN_POINT ( 'NONE',  ( 0.1743543163984999922, -85.83208224847899714, 3.543178075967999607 ) ) ;
#34286=CARTESIAN_POINT ( 'NONE',  ( -3.957350048490399175, -78.48547955770027329, -2.236040895654427985 ) ) ;
#34309=PRESENTATION_STYLE_ASSIGNMENT (( #16613 ) ) ;
#34388=CARTESIAN_POINT ( 'NONE',  ( -2.656488545785999911, -81.92924548946498930, -2.346920921671000304 ) ) ;
#34390=VERTEX_POINT ( 'NONE', #25345 ) ;
#34400=CARTESIAN_POINT ( 'NONE',  ( -3.237453996416379542, -86.12609999968209706, -2.259489515355698419 ) ) ;
#34411=CARTESIAN_POINT ( 'NONE',  ( 3.645312643188000301, -82.04903455456799577, -1.554753716817999898 ) ) ;
#34415=CARTESIAN_POINT ( 'NONE',  ( 1.078420410906000049, -83.63619503318798820, -3.379137726269000108 ) ) ;
#34435=CARTESIAN_POINT ( 'NONE',  ( 3.632931406222999815, -85.58531592346599837, 2.052286280999000123 ) ) ;
#34440=CARTESIAN_POINT ( 'NONE',  ( -3.548349909811000291, -78.96264282632948550, -1.488874400533411246E-14 ) ) ;
#34459=CARTESIAN_POINT ( 'NONE',  ( 3.699999999670000594, -79.00321104920828930, -1.355252715606880543E-15 ) ) ;
#34506=CARTESIAN_POINT ( 'NONE',  ( 3.962812355711000212, -78.54828561723799396, 0.000000000000000000 ) ) ;
#34649=CARTESIAN_POINT ( 'NONE',  ( 2.877569803687999972, -84.07371544543099162, -2.724990427310999941 ) ) ;
#34676=CARTESIAN_POINT ( 'NONE',  ( 2.136931703850000197, -79.41556330239998829, -2.883967052643999995 ) ) ;
#34689=CARTESIAN_POINT ( 'NONE',  ( -3.938198560205464993, -86.17851879815596305, -0.3769834764405665672 ) ) ;
#34699=CARTESIAN_POINT ( 'NONE',  ( 1.665232602310000143, -79.65175264934788402, 3.129211432048999875 ) ) ;
#34702=CARTESIAN_POINT ( 'NONE',  ( -1.473190823115000159, -82.91469503318799639, 3.226649821350000114 ) ) ;
#34721=CARTESIAN_POINT ( 'NONE',  ( 3.474217323525000012, -82.26950239379898733, -1.986488251467000143 ) ) ;
#34728=CARTESIAN_POINT ( 'NONE',  ( 3.621447497675001070, -78.99318692614360771, 7.242894995350030563 ) ) ;
#34741=CARTESIAN_POINT ( 'NONE',  ( -3.620209226088999976, -86.25171438269200053, 1.611820996859000044 ) ) ;
#34748=CARTESIAN_POINT ( 'NONE',  ( 3.778552491321001128, -78.99318692756679638, -1.395910297075086959E-15 ) ) ;
#34760=CARTESIAN_POINT ( 'NONE',  ( -3.559953446648999709, -80.08155496681199281, 2.176417643061999918 ) ) ;
#34800=CARTESIAN_POINT ( 'NONE',  ( 3.914500761937000028, -78.48547955770028750, 0.000000000000000000 ) ) ;
#34821=CARTESIAN_POINT ( 'NONE',  ( -0.5301359684276694129, -86.40321104920798234, 4.263478205968190160 ) ) ;
#34839=CARTESIAN_POINT ( 'NONE',  ( 4.115840777475000323, -80.89192428167199012, -0.6829423103135000561 ) ) ;
#34854=CARTESIAN_POINT ( 'NONE',  ( 3.576074390005977488, -85.88547955769999476, -1.592170899228049441 ) ) ;
#34859=CARTESIAN_POINT ( 'NONE',  ( 3.914500761936999140, -78.48547955770027329, -2.310234204170795280 ) ) ;
#34933=CARTESIAN_POINT ( 'NONE',  ( 1.276300174619999783, -84.43832450217399810, 3.928048035916000380 ) ) ;
#34962=CARTESIAN_POINT ( 'NONE',  ( -3.263865106102529889, -78.77708333023421972, -1.096753143766827643 ) ) ;
#34974=CARTESIAN_POINT ( 'NONE',  ( 3.241578942234940808, -86.36264282632899381, -1.443243930775132133 ) ) ;
#34981=CARTESIAN_POINT ( 'NONE',  ( -1.334654685515000105, -82.29771400872598974, -3.731581711997999928 ) ) ;
#34984=CARTESIAN_POINT ( 'NONE',  ( -3.026296275368999922, -80.08155496681199281, 1.850160319665000053 ) ) ;
#34987=CARTESIAN_POINT ( 'NONE',  ( 1.077708808469999946, -83.70524735065198740, -3.376907981158000283 ) ) ;
#35008=CARTESIAN_POINT ( 'NONE',  ( 4.174306380842000230, -82.38975280906599608, -0.06567313222218000568 ) ) ;
#35014=CARTESIAN_POINT ( 'NONE',  ( -1.242879273300786513, -78.85062977682864016, -3.768395784351273647 ) ) ;
#35030=CARTESIAN_POINT ( 'NONE',  ( -3.913805347717917105, -78.91452044229970397, 0.07378289354579982418 ) ) ;
#35039=CARTESIAN_POINT ( 'NONE',  ( -0.4363934998635000118, -80.49350264934798815, -4.152006803154999481 ) ) ;
#35103=CARTESIAN_POINT ( 'NONE',  ( 3.965107357241011155, -86.25171435493598437, 0.4551303408108293702 ) ) ;
#35123=CARTESIAN_POINT ( 'NONE',  ( -0.06100561046413999905, -79.80967046134098553, 4.171670386524000129 ) ) ;
#35138=CARTESIAN_POINT ( 'NONE',  ( 3.620209227049977052, -85.94828561723799965, -1.611820994701049781 ) ) ;
#35144=CARTESIAN_POINT ( 'NONE',  ( -2.375990957848951091, -78.54828561723799396, -3.940594315429740480 ) ) ;
#35219=CARTESIAN_POINT ( 'NONE',  ( 0.3143049556117999965, -82.79444503318798354, 4.160684000108000546 ) ) ;
#35249=CARTESIAN_POINT ( 'NONE',  ( 2.498996544723999680, -81.45596103735698534, 2.804707967251000245 ) ) ;
#35261=CARTESIAN_POINT ( 'NONE',  ( 0.4816222532846568538, -86.25171438276197478, -4.576205428947634601 ) ) ;
#35262=CARTESIAN_POINT ( 'NONE',  ( 3.471857344089170017, -85.80962377308421196, 1.038510158527778726 ) ) ;
#35268=CARTESIAN_POINT ( 'NONE',  ( 3.799029956959000032, -82.54207433891198775, -1.620318395421999957 ) ) ;
#35271=CARTESIAN_POINT ( 'NONE',  ( -3.480664168985999840, -78.75880496681158149, -0.6827920017205999503 ) ) ;
#35293=CARTESIAN_POINT ( 'NONE',  ( 3.632564424962000160, -85.59158141794600283, 2.052078968907000256 ) ) ;
#35300=CARTESIAN_POINT ( 'NONE',  ( -3.699999999670000150, -79.00321104920828930, -1.552506213169860872E-14 ) ) ;
#35320=CARTESIAN_POINT ( 'NONE',  ( -0.03239454126609288276, -78.85171435493609238, -3.437034970110011134 ) ) ;
#35332=CARTESIAN_POINT ( 'NONE',  ( -4.052894509781999943, -78.55792549782628953, -0.7950448020103999536 ) ) ;
#35370=CARTESIAN_POINT ( 'NONE',  ( 3.088780581828999949, -85.55392953870899930, 1.744701995914999859 ) ) ;
#35390=CARTESIAN_POINT ( 'NONE',  ( 1.368374140978811271, -86.25171435493598437, 3.153063748541271583 ) ) ;
#35426=CARTESIAN_POINT ( 'NONE',  ( -0.5608696358179350305, -85.88547955769999476, 4.510645591149664568 ) ) ;
#35431=CARTESIAN_POINT ( 'NONE',  ( -3.523652525393907720, -78.48547957940618858, -1.990986658322625669 ) ) ;
#35489=ADVANCED_FACE ( 'NONE', ( #39094 ), #52382, .T. ) ;
#35514=CARTESIAN_POINT ( 'NONE',  ( -2.667898297452999667, -84.54699735065199206, 3.211217596898999993 ) ) ;
#35543=CARTESIAN_POINT ( 'NONE',  ( 1.730605770088500472, -79.20104166191323714, -2.976826296013844075 ) ) ;
#35547=CARTESIAN_POINT ( 'NONE',  ( -1.963416759258999722, -80.25345679254499487, 3.442525934388999787 ) ) ;
#35560=CARTESIAN_POINT ( 'NONE',  ( -4.452050888846053489, -86.36264283715696877, -0.4261719148253248490 ) ) ;
#35561=CARTESIAN_POINT ( 'NONE',  ( 2.133191202286643051, -85.88405207176444378, 2.764547849547144498 ) ) ;
#35569=CARTESIAN_POINT ( 'NONE',  ( -3.412299873766000413, -78.67863830014491100, 0.4934769004953000193 ) ) ;
#35575=ORIENTED_EDGE ( 'NONE', *, *, #24696, .F. ) ;
#35591=CARTESIAN_POINT ( 'NONE',  ( -3.844964336665000371, -84.42243313234698121, 1.508231652767000108 ) ) ;
#35599=CARTESIAN_POINT ( 'NONE',  ( 3.407095545933001013, -78.77851879815550262, 6.814191091866031336 ) ) ;
#35619=CARTESIAN_POINT ( 'NONE',  ( 1.974456364585914558, -78.72609999968184979, -3.418760544058739637 ) ) ;
#35629=CARTESIAN_POINT ( 'NONE',  ( 1.620950162628999935, -80.68280496681198599, -3.844812462229999728 ) ) ;
#35652=CARTESIAN_POINT ( 'NONE',  ( -2.293752191199000201, -84.67882450217399537, 2.760876382108000016 ) ) ;
#35697=CARTESIAN_POINT ( 'NONE',  ( 3.930393413736140928, -86.17851879815599148, 0.4511457402659648230 ) ) ;
#35718=ORIENTED_EDGE ( 'NONE', *, *, #18313, .F. ) ;
#35731=CARTESIAN_POINT ( 'NONE',  ( 3.677662896325250674, -85.88547955769999476, 2.671197113343194651 ) ) ;
#35734=CARTESIAN_POINT ( 'NONE',  ( 1.996052055574059514, -78.54828564506388489, -3.456153366506571789 ) ) ;
#35785=CARTESIAN_POINT ( 'NONE',  ( -3.357666099452000008, -85.94560505905998582, 0.9480989593101001311 ) ) ;
#35795=CARTESIAN_POINT ( 'NONE',  ( 3.140027144888999810, -86.25171435493598437, -1.398030157551999997 ) ) ;
#35799=( BOUNDED_SURFACE ( )  B_SPLINE_SURFACE ( 3, 3, ( 
 ( #39017, #52606, #26300, #44312, #39305, #39877, #57316 ),
 ( #17157, #2730, #16307, #47624, #16588, #8297, #53174 ),
 ( #26007, #29853, #43175, #43455, #57890, #12156, #11875 ),
 ( #33998, #52035, #35144, #7147, #3584, #12724, #57029 ),
 ( #30716, #34286, #21012, #47908, #7440, #34859, #25439 ),
 ( #18628, #36619, #5042, #45497, #13891, #53764, #27459 ),
 ( #9473, #50213, #44609, #23042, #54640, #22459, #18335 ),
 ( #27164, #49928, #53461, #41057, #4164, #9763, #14176 ),
 ( #17445, #49339, #644, #22163, #31885, #32173, #27750 ),
 ( #13004, #45795, #40169, #5330, #23337, #41348, #4457 ),
 ( #31003, #35431, #49042, #8587, #26575, #357, #58183 ),
 ( #17747, #40471, #8885, #45203, #35734, #13301, #13594 ),
 ( #44904, #31293, #4750, #26880, #63, #18040, #22751 ),
 ( #36034, #54058, #49633, #31590, #9180, #40762, #36327 ),
 ( #54352, #15641, #41930, #55804, #38075, #47252, #33349 ) ),
 .UNSPECIFIED., .F., .F., .F. ) 
 B_SPLINE_SURFACE_WITH_KNOTS ( ( 4, 1, 1, 1, 1, 1, 1, 1, 1, 1, 1, 1, 4 ),
 ( 4, 3, 4 ),
 ( 0.009836358966825000175, 0.09153389967814999639, 0.1732269073519000224, 0.2549246240467999969, 0.3366128957582000258, 0.4183102327763000283, 0.5000049915179999305, 0.5816997512343000665, 0.6633971206824998967, 0.7450853986059999823, 0.8267830947368000061, 0.9084761241232000017, 0.9901736240545999657 ),
 ( 0.000000000000000000, 0.5000000000000000000, 1.000000000000000000 ),
 .UNSPECIFIED. ) 
 GEOMETRIC_REPRESENTATION_ITEM ( )  RATIONAL_B_SPLINE_SURFACE ( (
 ( 1.000000000000000000, 0.8025111667134329219, 0.8025111667134329219, 1.000000000000000000, 0.8025111667134329219, 0.8025111667134329219, 1.000000000000000000),
 ( 1.000000000000000000, 0.8025111667134329219, 0.8025111667134329219, 1.000000000000000000, 0.8025111667134329219, 0.8025111667134329219, 1.000000000000000000),
 ( 1.000000000000000000, 0.8025111667134329219, 0.8025111667134329219, 1.000000000000000000, 0.8025111667134329219, 0.8025111667134329219, 1.000000000000000000),
 ( 1.000000000000000000, 0.8025111667134329219, 0.8025111667134329219, 1.000000000000000000, 0.8025111667134329219, 0.8025111667134329219, 1.000000000000000000),
 ( 1.000000000000000000, 0.8025111667134329219, 0.8025111667134329219, 1.000000000000000000, 0.8025111667134329219, 0.8025111667134329219, 1.000000000000000000),
 ( 1.000000000000000000, 0.8025111667134329219, 0.8025111667134329219, 1.000000000000000000, 0.8025111667134329219, 0.8025111667134329219, 1.000000000000000000),
 ( 1.000000000000000000, 0.8025111667134329219, 0.8025111667134329219, 1.000000000000000000, 0.8025111667134329219, 0.8025111667134329219, 1.000000000000000000),
 ( 1.000000000000000000, 0.8025111667134329219, 0.8025111667134329219, 1.000000000000000000, 0.8025111667134329219, 0.8025111667134329219, 1.000000000000000000),
 ( 1.000000000000000000, 0.8025111667134329219, 0.8025111667134329219, 1.000000000000000000, 0.8025111667134329219, 0.8025111667134329219, 1.000000000000000000),
 ( 1.000000000000000000, 0.8025111667134329219, 0.8025111667134329219, 1.000000000000000000, 0.8025111667134329219, 0.8025111667134329219, 1.000000000000000000),
 ( 1.000000000000000000, 0.8025111667134329219, 0.8025111667134329219, 1.000000000000000000, 0.8025111667134329219, 0.8025111667134329219, 1.000000000000000000),
 ( 1.000000000000000000, 0.8025111667134329219, 0.8025111667134329219, 1.000000000000000000, 0.8025111667134329219, 0.8025111667134329219, 1.000000000000000000),
 ( 1.000000000000000000, 0.8025111667134329219, 0.8025111667134329219, 1.000000000000000000, 0.8025111667134329219, 0.8025111667134329219, 1.000000000000000000),
 ( 1.000000000000000000, 0.8025111667134329219, 0.8025111667134329219, 1.000000000000000000, 0.8025111667134329219, 0.8025111667134329219, 1.000000000000000000),
 ( 1.000000000000000000, 0.8025111667134329219, 0.8025111667134329219, 1.000000000000000000, 0.8025111667134329219, 0.8025111667134329219, 1.000000000000000000) ) ) 
 REPRESENTATION_ITEM ( '' )  SURFACE ( )  );
#35816=CARTESIAN_POINT ( 'NONE',  ( 3.472271713658000358, -82.31344503318798900, -1.985370858487000012 ) ) ;
#35847=CARTESIAN_POINT ( 'NONE',  ( -2.815216471715999980, -82.17746358424498965, -2.487151863305999910 ) ) ;
#35853=VERTEX_POINT ( 'NONE', #12849 ) ;
#35861=CARTESIAN_POINT ( 'NONE',  ( -4.623525823812755675, -86.12610001270961391, -0.4425863276891007225 ) ) ;
#35862=CARTESIAN_POINT ( 'NONE',  ( 3.604156498665337161, -85.79994401664013992, 0.7643492597376573272 ) ) ;
#35868=CARTESIAN_POINT ( 'NONE',  ( -1.093645373922000230, -81.69646188631999451, 3.809190202271000025 ) ) ;
#35871=CARTESIAN_POINT ( 'NONE',  ( 3.222977620591999770, -79.29100264934788811, -1.475594510407999937 ) ) ;
#35893=CARTESIAN_POINT ( 'NONE',  ( 2.192371239512000525, -85.63651402127000267, 3.552905146332000275 ) ) ;
#35919=CARTESIAN_POINT ( 'NONE',  ( -2.394033331947576837, -78.77851881763733388, -3.970517693957353877 ) ) ;
#35931=CARTESIAN_POINT ( 'NONE',  ( -2.386247763912000330, -80.37325264934800373, -3.425700131269000082 ) ) ;
#35954=CARTESIAN_POINT ( 'NONE',  ( -3.497041162369999956, -84.91546544543099628, 1.371883813336999935 ) ) ;
#35959=DIRECTION ( 'NONE',  ( -0.9135454518431509463, 0.000000000000000000, 0.4067366561015779980 ) ) ;
#35972=CARTESIAN_POINT ( 'NONE',  ( -0.6866111826235999915, -83.50967953870899407, -3.480390452359999998 ) ) ;
#35995=CARTESIAN_POINT ( 'NONE',  ( -0.4994022981156016061, -86.31452042059399332, 4.016310797290853607 ) ) ;
#36028=CARTESIAN_POINT ( 'NONE',  ( 1.558396630253658044, -85.88547955769999476, 3.590921352246429610 ) ) ;
#36034=CARTESIAN_POINT ( 'NONE',  ( -3.399395987256549567, -78.67390000031814168, 0.06408526995191954345 ) ) ;
#36046=CARTESIAN_POINT ( 'NONE',  ( -3.740501050291150431, -78.39678895079168797, 2.113514116493498296 ) ) ;
#36090=CARTESIAN_POINT ( 'NONE',  ( 3.589194950545000040, -85.26418603921399608, 0.03774597188233999590 ) ) ;
#36118=CARTESIAN_POINT ( 'NONE',  ( 3.637908496719999718, -85.52057450217398582, -1.955537114970999912 ) ) ;
#36149=CARTESIAN_POINT ( 'NONE',  ( 3.301590358683000215, -82.54207433891198775, -1.408156201170000177 ) ) ;
#36159=CARTESIAN_POINT ( 'NONE',  ( 0.4681120926950248506, -86.36264283715696877, -4.447836629928476171 ) ) ;
#36160=CARTESIAN_POINT ( 'NONE',  ( 1.895286063978128821, -85.89372256580323040, 2.922279908445652552 ) ) ;
#36167=CARTESIAN_POINT ( 'NONE',  ( -3.703359171702000019, -80.49781712273099288, -1.828563516828999980 ) ) ;
#36171=CARTESIAN_POINT ( 'NONE',  ( 3.440332551270000039, -82.44647163347798369, -0.2267637900948999974 ) ) ;
#36195=CARTESIAN_POINT ( 'NONE',  ( -3.315815974107000130, -82.85917773387799912, 2.462494273907000153 ) ) ;
#36220=CARTESIAN_POINT ( 'NONE',  ( 3.999999999999815703, -78.72610001270986402, -2.360693579763180949 ) ) ;
#36233=CARTESIAN_POINT ( 'NONE',  ( -3.165774207400000151, -78.67817549782625974, -2.652657151789000078 ) ) ;
#36256=CARTESIAN_POINT ( 'NONE',  ( -2.900113492901999823, -86.11024735065198854, 2.038129431027000393 ) ) ;
#36260=CARTESIAN_POINT ( 'NONE',  ( 3.442912721433392775, -85.44479167442446510, -0.07965019996499557442 ) ) ;
#36296=CARTESIAN_POINT ( 'NONE',  ( 0.1182020803831417416, -79.81770832474683175, 4.050395722669112963 ) ) ;
#36324=CARTESIAN_POINT ( 'NONE',  ( 1.412628807274612042, -85.83735717367099483, 3.255037163431188318 ) ) ;
#36327=CARTESIAN_POINT ( 'NONE',  ( 3.400000000000109157, -78.67390000031814168, -1.233279971202261294E-15 ) ) ;
#36337=CARTESIAN_POINT ( 'NONE',  ( -2.127490618600312633, -78.43735717367052018, 3.528455733208861300 ) ) ;
#36378=CARTESIAN_POINT ( 'NONE',  ( 1.091356032651999985, -83.46042981021199125, -3.419457127327000023 ) ) ;
#36391=CARTESIAN_POINT ( 'NONE',  ( -6.760416188461989329, -85.88547955770000897, -5.559977880783894655 ) ) ;
#36402=CARTESIAN_POINT ( 'NONE',  ( 3.912590402935000267, -82.39999999999999147, -0.8316467632710000668 ) ) ;
#36406=CARTESIAN_POINT ( 'NONE',  ( 3.805232393909999900, -82.34726287204199480, -1.402232436220000045 ) ) ;
#36433=CARTESIAN_POINT ( 'NONE',  ( -3.250112804463431093, -80.28020832436914134, -1.140199822464329715 ) ) ;
#36434=CARTESIAN_POINT ( 'NONE',  ( 3.455307648225000250, -82.65846528216999900, -1.473717924758000120 ) ) ;
#36444=CARTESIAN_POINT ( 'NONE',  ( -1.661313768260326951, -86.12610001270964233, -3.638686103992151200 ) ) ;
#36445=CARTESIAN_POINT ( 'NONE',  ( 3.520322167287936566, -85.82207524133897891, 1.464606465184206563 ) ) ;
#36452=CARTESIAN_POINT ( 'NONE',  ( 2.777313436393999968, -81.20774294257799397, 3.117072386135000261 ) ) ;
#36457=CARTESIAN_POINT ( 'NONE',  ( -0.9790058809313999522, -81.41057046129098751, 3.409706750568999745 ) ) ;
#36480=CARTESIAN_POINT ( 'NONE',  ( -3.364564966397000312, -84.79476111440199304, -2.471702357780000359 ) ) ;
#36510=CARTESIAN_POINT ( 'NONE',  ( 3.962812355710999768, -78.85171438276198330, -2.338746421483398841 ) ) ;
#36524=CARTESIAN_POINT ( 'NONE',  ( 3.737144282028000308, -80.72628455456799657, 1.318989544820000193 ) ) ;
#36549=CARTESIAN_POINT ( 'NONE',  ( -1.507852503906999875, -85.15982450217398991, -3.257317659296999679 ) ) ;
#36584=CARTESIAN_POINT ( 'NONE',  ( -3.778552491321000240, -78.40681307243859521, -1.659736609915999906E-10 ) ) ;
#36587=CARTESIAN_POINT ( 'NONE',  ( 0.1757403804742654341, -79.08541664991678033, -4.009081873298199206 ) ) ;
#36615=CARTESIAN_POINT ( 'NONE',  ( -2.557474545126054100, -85.79678895079199208, 3.452189813555863740 ) ) ;
#36619=CARTESIAN_POINT ( 'NONE',  ( -3.893811372584298880, -78.43735716284257364, -2.200139326159465281 ) ) ;
#36632=CARTESIAN_POINT ( 'NONE',  ( -3.587190963684412370, -78.43735717367052018, 2.026888547381852312 ) ) ;
#36672=CARTESIAN_POINT ( 'NONE',  ( -3.420428384795999754, -85.98568853081499697, 0.3738047447517999777 ) ) ;
#36682=CARTESIAN_POINT ( 'NONE',  ( 0.3702670344839096850, -85.79678895079197787, -8.265161965197931337 ) ) ;
#36696=CARTESIAN_POINT ( 'NONE',  ( 3.685140862346000024, -82.54767953870899078, 1.956143928933999687 ) ) ;
#36712=VERTEX_POINT ( 'NONE', #38864 ) ;
#36717=ORIENTED_EDGE ( 'NONE', *, *, #46934, .F. ) ;
#36724=CARTESIAN_POINT ( 'NONE',  ( -3.412338500972434741, -81.66770831895492222, 0.4596473917829690392 ) ) ;
#36742=CARTESIAN_POINT ( 'NONE',  ( 3.936899005229999471, -81.08749251809699388, 1.389401455896000170 ) ) ;
#36747=CARTESIAN_POINT ( 'NONE',  ( -3.461625351506000481, -81.76505496681200214, -0.7737650771603999944 ) ) ;
#36770=CARTESIAN_POINT ( 'NONE',  ( -2.655896506213000219, -83.21992897967898273, -3.163025014367999876 ) ) ;
#36777=CARTESIAN_POINT ( 'NONE',  ( -3.851650068367032276, -78.96264283715741783, 7.703300136734017478 ) ) ;
#36813=CARTESIAN_POINT ( 'NONE',  ( 3.459153386863000446, -79.39967549782629419, 2.256714709944000141 ) ) ;
#36835=CARTESIAN_POINT ( 'NONE',  ( -0.6947249814979998828, -83.71682450217399207, -3.521518806877999896 ) ) ;
#36840=CARTESIAN_POINT ( 'NONE',  ( 0.4739077948423049413, -85.79166667334425256, 3.377908686572150820 ) ) ;
#36876=CARTESIAN_POINT ( 'NONE',  ( -3.856336781450672824, -80.12604166151689356, 1.240447633703557706 ) ) ;
#36885=CARTESIAN_POINT ( 'NONE',  ( -3.184161977317994108, -85.88547957940599531, 1.417680250971013356 ) ) ;
#36901=CARTESIAN_POINT ( 'NONE',  ( -2.503178322335409600, -85.80681307385597734, 3.378898422409377655 ) ) ;
#36919=CARTESIAN_POINT ( 'NONE',  ( -3.850965828042431482, -78.43735716284258785, -0.07259779887146158850 ) ) ;
#36936=CARTESIAN_POINT ( 'NONE',  ( -3.374925386387973347, -83.24791668126330535, -0.6818111582454060571 ) ) ;
#36960=CARTESIAN_POINT ( 'NONE',  ( 2.949808988708999991, -82.26950239379898733, -1.686642012998000206 ) ) ;
#36973=CARTESIAN_POINT ( 'NONE',  ( -3.518657424384993959, -85.83735716284299144, 1.566607219110014659 ) ) ;
#36987=CARTESIAN_POINT ( 'NONE',  ( 4.043613182668000405, -83.99694503318799832, 1.029201014592999952 ) ) ;
#37014=CARTESIAN_POINT ( 'NONE',  ( -3.292147582310161802, -81.62916665243866987, 1.011281930930018058 ) ) ;
#37028=CARTESIAN_POINT ( 'NONE',  ( 2.410958077658777565, -85.88312199482444953, 3.074828045483646743 ) ) ;
#37033=CARTESIAN_POINT ( 'NONE',  ( 1.961420010778000211, -79.76473784880299434, 3.685436439494999661 ) ) ;
#37038=CARTESIAN_POINT ( 'NONE',  ( -2.502884433417999599, -81.52455496681199065, 2.513390501795000009 ) ) ;
#37059=CARTESIAN_POINT ( 'NONE',  ( -1.646006820151000083, -82.62253637535398809, 3.605086534529000186 ) ) ;
#37079=CARTESIAN_POINT ( 'NONE',  ( 1.378041103583000027, -80.65142343270998992, -3.268877919052000092 ) ) ;
#37087=CARTESIAN_POINT ( 'NONE',  ( -4.043785186575744817, -78.69999999999998863, -2.284879765406194974 ) ) ;
#37102=CARTESIAN_POINT ( 'NONE',  ( -1.139821578811999858, -81.20342549782600372, 3.969799781000000305 ) ) ;
#37125=CARTESIAN_POINT ( 'NONE',  ( 1.255715561858000040, -83.83707450217399071, -3.934676852947000203 ) ) ;
#37134=CARTESIAN_POINT ( 'NONE',  ( 3.778552491321000240, -78.99318692756679638, 0.000000000000000000 ) ) ;
#37167=CARTESIAN_POINT ( 'NONE',  ( -2.759932835649922200, -86.17851881763701272, 3.725476775316761469 ) ) ;
#37226=CARTESIAN_POINT ( 'NONE',  ( 1.103369793158732737, -82.74687501615673568, 3.250074485770516830 ) ) ;
#37246=CARTESIAN_POINT ( 'NONE',  ( 2.775417664047000077, -81.17007046129099024, 3.115060498111000165 ) ) ;
#37251=CARTESIAN_POINT ( 'NONE',  ( 1.096008713999000017, -84.26256135553198590, 3.373475151840000130 ) ) ;
#37262=CARTESIAN_POINT ( 'NONE',  ( 3.112536659741979239, -86.02148120184399716, -1.385790604991046671 ) ) ;
#37272=CARTESIAN_POINT ( 'NONE',  ( -1.257344828728125696, -82.90104165186102136, 3.810723461902208342 ) ) ;
#37277=CARTESIAN_POINT ( 'NONE',  ( -2.683170449497999765, -83.39569503318799093, -3.195412127327000196 ) ) ;
#37305=CARTESIAN_POINT ( 'NONE',  ( 0.7812709553989065636, -82.13020831715014936, -3.320429094668629677 ) ) ;
#37319=CARTESIAN_POINT ( 'NONE',  ( 3.516302236083875599, -85.82247364775101062, 1.476714140108094542 ) ) ;
#37326=CARTESIAN_POINT ( 'NONE',  ( -3.809107967971999908, -78.61343171100860161, 1.220272423491999936 ) ) ;
#37330=CARTESIAN_POINT ( 'NONE',  ( 2.359605203086000191, -81.16380496681199475, 2.648362822824000151 ) ) ;
#37353=CARTESIAN_POINT ( 'NONE',  ( -3.242523719075999900, -85.74904717229100015, 2.278511022525999685 ) ) ;
#37371=ORIENTED_EDGE ( 'NONE', *, *, #48114, .T. ) ;
#37373=CARTESIAN_POINT ( 'NONE',  ( 3.225423266044999959, -79.32866876341660145, -1.476890314707000051 ) ) ;
#37393=CARTESIAN_POINT ( 'NONE',  ( 2.545076011845999631, -82.04517549782597996, -3.252891696798999810 ) ) ;
#37416=CARTESIAN_POINT ( 'NONE',  ( 2.998912544640999656, -83.95732450217400356, -2.839899128081999624 ) ) ;
#37425=CARTESIAN_POINT ( 'NONE',  ( -2.682853591918000102, -83.42707394314300018, -3.195129404054000144 ) ) ;
#37459=CARTESIAN_POINT ( 'NONE',  ( 2.022162896325808479, -79.20104165120571338, -3.466033633082603593 ) ) ;
#37465=CARTESIAN_POINT ( 'NONE',  ( -3.112536659741994338, -86.02148120184399716, 1.385790604991013142 ) ) ;
#37481=CARTESIAN_POINT ( 'NONE',  ( 3.333665159394552546, -85.83735717367099483, 2.421341216326917678 ) ) ;
#37525=EDGE_LOOP ( 'NONE', ( #49090, #55843, #44845, #27052 ) ) ;
#37541=CARTESIAN_POINT ( 'NONE',  ( -2.900222056821999850, -85.99726526706999152, 2.037976741810000103 ) ) ;
#37553=CARTESIAN_POINT ( 'NONE',  ( -6.895820826652922619, -86.02148118236289065, -5.671338893525836866 ) ) ;
#37568=CARTESIAN_POINT ( 'NONE',  ( 2.599519341589024091, -85.65677084819145648, 3.056421543846630673 ) ) ;
#37571=CARTESIAN_POINT ( 'NONE',  ( 0.2925143690059999746, -85.07919503318798604, -4.162270734640999947 ) ) ;
#37599=CARTESIAN_POINT ( 'NONE',  ( 3.325701842495000005, -82.39999999999999147, -0.7068997487804000723 ) ) ;
#37612=CARTESIAN_POINT ( 'NONE',  ( 3.574842537148360755, -85.81605190634385849, 1.280382247947833063 ) ) ;
#37616=CARTESIAN_POINT ( 'NONE',  ( -1.405052895698000182, -81.97417810200299471, -3.928409158472000229 ) ) ;
#37649=CARTESIAN_POINT ( 'NONE',  ( -3.015813095775000008, -82.74278679062099684, 2.239696815961000009 ) ) ;
#37667=CARTESIAN_POINT ( 'NONE',  ( -3.180857842748000319, -80.29067215926599488, -1.570574263471999910 ) ) ;
#37693=CARTESIAN_POINT ( 'NONE',  ( -3.606252685672000524, -81.32753455456798974, 1.051809756341999913 ) ) ;
#37712=CARTESIAN_POINT ( 'NONE',  ( -3.852759956968999866, -83.47632450217398059, -1.488201649610999988 ) ) ;
#37720=CARTESIAN_POINT ( 'NONE',  ( 3.029408902660999825, -83.78782518894399800, -2.868664668380999760 ) ) ;
#37727=CARTESIAN_POINT ( 'NONE',  ( -1.703153893272331576, -78.82703160532072673, -2.986442783030232917 ) ) ;
#37748=CARTESIAN_POINT ( 'NONE',  ( -2.038544480927453773, -78.69999999999998863, -3.380937442862138376 ) ) ;
#37756=CARTESIAN_POINT ( 'NONE',  ( 4.044298153132396045, -80.93541667053997912, -0.2531087429660031640 ) ) ;
#37790=CARTESIAN_POINT ( 'NONE',  ( -3.399999999999999911, -78.69999997992952956, 5.715921273723000819E-07 ) ) ;
#37795=CARTESIAN_POINT ( 'NONE',  ( 3.407095545933005454, -78.62148120184446043, 2.010777053086950872 ) ) ;
#37837=CARTESIAN_POINT ( 'NONE',  ( -3.514740471877999983, -83.18030761812998719, 0.4776706111134000343 ) ) ;
#37861=CARTESIAN_POINT ( 'NONE',  ( 0.9857603460642816451, -83.63333332641040840, -3.930466141329476581 ) ) ;
#37890=SHAPE_DEFINITION_REPRESENTATION ( #21031, #52046 ) ;
#37907=ADVANCED_FACE ( 'NONE', ( #12942 ), #9986, .T. ) ;
#37908=CARTESIAN_POINT ( 'NONE',  ( 2.483853621210999840, -79.20841833893540240, -3.352167031944000009 ) ) ;
#37936=CARTESIAN_POINT ( 'NONE',  ( -0.7669882343743998909, -83.22378845168798023, -3.888151105264999519 ) ) ;
#37955=DIRECTION ( 'NONE',  ( -0.9135454576426007556, 0.000000000000000000, 0.4067366430758003193 ) ) ;
#37956=CARTESIAN_POINT ( 'NONE',  ( -3.026593009001000034, -80.05017131030399469, 1.850485041987000034 ) ) ;
#37980=CARTESIAN_POINT ( 'NONE',  ( 3.006216744975000132, -79.39967549782629419, 1.961223684219999930 ) ) ;
#37998=CARTESIAN_POINT ( 'NONE',  ( 0.3111154154752000522, -82.99532450217398605, 4.118461730375999608 ) ) ;
#38013=CARTESIAN_POINT ( 'NONE',  ( 2.845090514860381781, -78.98918610123767792, -2.490951044996013497 ) ) ;
#38047=CARTESIAN_POINT ( 'NONE',  ( 3.740094692943897403, -82.36145835310306040, -1.455080866065831868 ) ) ;
#38075=CARTESIAN_POINT ( 'NONE',  ( 1.974456364586083756, -78.70000000000000284, -3.418760544059030959 ) ) ;
#38108=FACE_OUTER_BOUND ( 'NONE', #27885, .T. ) ;
#38124=CARTESIAN_POINT ( 'NONE',  ( 0.1742185655343000128, -85.75676443653598824, 3.540419386099000310 ) ) ;
#38150=CARTESIAN_POINT ( 'NONE',  ( -4.022178672785524434, -83.17083332143187135, 0.4884531335743385605 ) ) ;
#38247=CARTESIAN_POINT ( 'NONE',  ( 0.5659361347325999603, -82.09442852648498956, -3.502031804551999805 ) ) ;
#38271=CARTESIAN_POINT ( 'NONE',  ( -0.9905749567282999823, -81.20342549782600372, 3.449999823992999648 ) ) ;
#38277=CARTESIAN_POINT ( 'NONE',  ( -2.280948012154000004, -83.39569503318799093, -2.716401763145999571 ) ) ;
#38289=CARTESIAN_POINT ( 'NONE',  ( -2.532550380305000015, -84.79521544543099765, 3.048305984539999791 ) ) ;
#38290=CARTESIAN_POINT ( 'NONE',  ( 3.112536659742000111, -86.02148120184399716, -1.385790604991000041 ) ) ;
#38305=CARTESIAN_POINT ( 'NONE',  ( -3.399999999999999911, -78.69999997992952956, 5.715921273723000819E-07 ) ) ;
#38334=CARTESIAN_POINT ( 'NONE',  ( 2.484261087175999805, -79.23980496681159025, -3.352388143773000095 ) ) ;
#38385=AXIS2_PLACEMENT_3D ( 'NONE', #16640, #2777, #25778 ) ;
#38417=CARTESIAN_POINT ( 'NONE',  ( 3.133403074829000268, -82.58532103627599952, 1.663280530810000268 ) ) ;
#38443=CARTESIAN_POINT ( 'NONE',  ( 2.414596980239923418, -84.17291666555200891, 3.253361081415106604 ) ) ;
#38483=CARTESIAN_POINT ( 'NONE',  ( -0.5731199659189539775, -86.09999999999978115, 4.609165628485380140 ) ) ;
#38517=CARTESIAN_POINT ( 'NONE',  ( -0.03769866006636662936, -78.67389998729011324, 3.999822347433201308 ) ) ;
#38535=ORIENTED_EDGE ( 'NONE', *, *, #57438, .T. ) ;
#38539=CARTESIAN_POINT ( 'NONE',  ( 3.222911977508000181, -79.40398657535959615, -1.475740419821999883 ) ) ;
#38553=FACE_OUTER_BOUND ( 'NONE', #30059, .T. ) ;
#38563=CARTESIAN_POINT ( 'NONE',  ( 0.7976678868801999611, -81.08317549782599087, 3.499637616860999945 ) ) ;
#38569=CARTESIAN_POINT ( 'NONE',  ( -1.472218728959000078, -82.98374735065199559, 3.224520696334999936 ) ) ;
#38598=CARTESIAN_POINT ( 'NONE',  ( -1.003981881343347426, -78.85407511475472120, -3.332975353450012168 ) ) ;
#38610=CARTESIAN_POINT ( 'NONE',  ( -3.451879464883000015, -86.39318692756398832, 1.536875756067000109 ) ) ;
#38625=CARTESIAN_POINT ( 'NONE',  ( -1.828200671114641018, -81.43645834279209339, 3.614657775617112545 ) ) ;
#38628=CARTESIAN_POINT ( 'NONE',  ( 3.793437728763999761, -79.36632046129089701, -1.736771565640999881 ) ) ;
#38661=CARTESIAN_POINT ( 'NONE',  ( -2.038544192961673218, -78.67390000031815589, 3.380937561918606615 ) ) ;
#38731=CARTESIAN_POINT ( 'NONE',  ( -3.766856363023864951, -84.78958333885674392, -1.489932256642206410 ) ) ;
#38772=CARTESIAN_POINT ( 'NONE',  ( 3.654181830569951384, -86.12610001270965654, -1.626946572303266114 ) ) ;
#38829=CARTESIAN_POINT ( 'NONE',  ( 2.358097774615999676, -81.20774294257799397, 2.646572533277999906 ) ) ;
#38841=CARTESIAN_POINT ( 'NONE',  ( 3.106054555985034771, -86.09999999999998010, -1.382904586457756047 ) ) ;
#38851=CARTESIAN_POINT ( 'NONE',  ( 0.5020202678138999675, -78.80228455456848735, -3.722814961589000493 ) ) ;
#38855=CARTESIAN_POINT ( 'NONE',  ( 3.124270252784000057, -85.31969503318799752, -1.679433785107000032 ) ) ;
#38864=CARTESIAN_POINT ( 'NONE',  ( -3.106054822367000146, -86.10000002299598520, 1.382903988153999952 ) ) ;
#38876=CARTESIAN_POINT ( 'NONE',  ( 1.268661270421000076, -83.66130927919799376, -3.974993213500999545 ) ) ;
#38882=CARTESIAN_POINT ( 'NONE',  ( 0.5664082909794043719, -78.90708710382101287, -3.437496070717471763 ) ) ;
#38894=CARTESIAN_POINT ( 'NONE',  ( -3.106054822367000146, -86.10000002299598520, 1.382903988153999952 ) ) ;
#38901=CARTESIAN_POINT ( 'NONE',  ( 3.699999999669999262, -79.00321104920828930, -2.183641561086286487 ) ) ;
#38909=CARTESIAN_POINT ( 'NONE',  ( 2.499201589291803138, -81.16666667311758943, 3.189714631542692747 ) ) ;
#38912=CARTESIAN_POINT ( 'NONE',  ( 3.494263450112999880, -79.60682046129089429, 2.279620140072000201 ) ) ;
#39017=CARTESIAN_POINT ( 'NONE',  ( -3.999289396772167660, -78.69999999999998863, 0.07539443523754783827 ) ) ;
#39094=FACE_OUTER_BOUND ( 'NONE', #37525, .T. ) ;
#39121=CARTESIAN_POINT ( 'NONE',  ( 1.376968171896000070, -80.72674124465299883, -3.266332797073000282 ) ) ;
#39142=CARTESIAN_POINT ( 'NONE',  ( -0.3705230124191999930, -80.49350264934798815, -3.525290978833000022 ) ) ;
#39145=CARTESIAN_POINT ( 'NONE',  ( 3.432824520865000117, -83.87669503318799968, -0.8929043418966999823 ) ) ;
#39165=CARTESIAN_POINT ( 'NONE',  ( -2.683124628265999956, -83.42080844866399048, -3.195452193269000318 ) ) ;
#39170=CARTESIAN_POINT ( 'NONE',  ( 1.262641813692434667, -78.92689010668476612, -3.687440721609341665 ) ) ;
#39186=CARTESIAN_POINT ( 'NONE',  ( 3.399999999999689493, -78.72609999968184979, -2.006589542798614012 ) ) ;
#39196=CARTESIAN_POINT ( 'NONE',  ( 4.115854587004999843, -80.92957046129099297, -0.6828514729849000098 ) ) ;
#39242=CARTESIAN_POINT ( 'NONE',  ( 3.911993909898488830, -82.39999677995871252, -0.8315195909956012432 ) ) ;
#39284=CARTESIAN_POINT ( 'NONE',  ( 1.960122366415000261, -79.68942003686028386, 3.682998213212000049 ) ) ;
#39305=CARTESIAN_POINT ( 'NONE',  ( 2.322889840689456697, -78.69999999999998863, -4.022071228304650248 ) ) ;
#39382=B_SPLINE_CURVE_WITH_KNOTS ( 'NONE', 3,
 ( #4195, #40203, #4781, #17776, #22783, #19234, #46117, #32205, #37226, #50246, #5360, #55241, #32492, #18944, #9796, #14789, #50830, #50537, #36936, #32784, #10375, #54949, #23653, #27780, #41665, #1244, #45823, #5643, #23367, #41378, #961, #14500, #10092, #28070, #49564, #54283, #44831, #26503, #27394, #23271, #45429, #288, #58405, #27098, #9403, #18267, #45134, #32110, #41277, #4969, #22979, #862, #40988, #8809, #40093, #50440, #36260, #14398, #44527, #40696, #26801, #580, #18847, #54574, #36840, #49257, #9110, #58107, #4386, #50151, #18560, #14114 ),
 .UNSPECIFIED., .F., .F.,
 ( 4, 2, 2, 2, 1, 2, 2, 2, 2, 2, 2, 2, 2, 2, 2, 2, 2, 2, 2, 2, 2, 2, 2, 2, 2, 2, 2, 2, 2, 2, 2, 2, 1, 2, 2, 2, 4 ),
 ( 0.000000000000000000, 0.03125000000000001388, 0.06250000000000002776, 0.07812500000000001388, 0.09375000000000000000, 0.1093749999999999722, 0.1249999999999999722, 0.1562499999999999445, 0.1874999999999999445, 0.2187499999999999167, 0.2499999999999999167, 0.2812499999999998890, 0.3124999999999998890, 0.3437499999999999445, 0.3749999999999999445, 0.4062499999999999445, 0.4374999999999999445, 0.4687499999999999445, 0.4999999999999998890, 0.5312499999999998890, 0.5624999999999998890, 0.5937499999999998890, 0.6249999999999998890, 0.6562500000000000000, 0.6875000000000000000, 0.7187500000000000000, 0.7500000000000000000, 0.7812500000000000000, 0.8125000000000000000, 0.8437500000000000000, 0.8750000000000000000, 0.8906250000000001110, 0.9062500000000001110, 0.9218750000000001110, 0.9375000000000001110, 0.9687500000000001110, 1.000000000000000000 ),
 .UNSPECIFIED. ) ;
#39388=CARTESIAN_POINT ( 'NONE',  ( -1.735035607296000038, -85.15982450217398991, -3.748086837743999755 ) ) ;
#39415=CARTESIAN_POINT ( 'NONE',  ( -2.658242603751999944, -81.86019317200199907, -2.348470574630999952 ) ) ;
#39427=CARTESIAN_POINT ( 'NONE',  ( 3.284677190815898484, -85.82402986354867380, 1.430105188728104881 ) ) ;
#39433=CARTESIAN_POINT ( 'NONE',  ( -1.139762735568999874, -81.58007094306199747, 3.969817958149999715 ) ) ;
#39436=CARTESIAN_POINT ( 'NONE',  ( 2.970753672374999876, -79.60055496681158616, 1.938087954564000182 ) ) ;
#39439=CARTESIAN_POINT ( 'NONE',  ( 3.546563745408000123, -82.43369503318800184, -0.05579941425955000506 ) ) ;
#39455=CARTESIAN_POINT ( 'NONE',  ( 3.576074390006000137, -85.88547955769999476, -1.592170899227999925 ) ) ;
#39459=CARTESIAN_POINT ( 'NONE',  ( -3.892240088685000377, -83.30055803339699594, -1.503509056668000055 ) ) ;
#39466=CARTESIAN_POINT ( 'NONE',  ( 3.407095545933000569, -78.77851879815550262, -4.172488654716052899E-16 ) ) ;
#39484=CARTESIAN_POINT ( 'NONE',  ( 3.851650068367000301, -78.96264283715740362, -2.273141396972203854 ) ) ;
#39493=CARTESIAN_POINT ( 'NONE',  ( 2.775698051716999792, -81.16380496681199475, 3.115375198333000473 ) ) ;
#39531=CARTESIAN_POINT ( 'NONE',  ( 3.437861145763999815, -83.99067953870898862, 0.8750219220807000653 ) ) ;
#39552=CARTESIAN_POINT ( 'NONE',  ( -3.407883501310938978, -86.40321104920799655, 1.440947618426480670 ) ) ;
#39573=CARTESIAN_POINT ( 'NONE',  ( 4.047001421017999867, -82.42136181958099428, -0.2667492537523999951 ) ) ;
#39587=CARTESIAN_POINT ( 'NONE',  ( -0.5731199659192217633, -86.07389998728977787, 4.609165628485452970 ) ) ;
#39667=CARTESIAN_POINT ( 'NONE',  ( 3.805616819021000463, -82.35352836652198505, -1.402374097307999889 ) ) ;
#39696=CARTESIAN_POINT ( 'NONE',  ( 3.260490012720000053, -82.41024718738999866, -1.390626556135999836 ) ) ;
#39707=CARTESIAN_POINT ( 'NONE',  ( -1.625803502918283128, -86.31452044229997966, -3.560909881631929785 ) ) ;
#39708=CARTESIAN_POINT ( 'NONE',  ( 0.8759936321165389117, -85.93109222455437646, 3.362092887207752234 ) ) ;
#39715=CARTESIAN_POINT ( 'NONE',  ( 2.545068763118000454, -82.42182391443098766, -3.252898933875000065 ) ) ;
#39718=CARTESIAN_POINT ( 'NONE',  ( -3.238159006571999843, -78.63855496681158286, 1.037165980353000005 ) ) ;
#39740=CARTESIAN_POINT ( 'NONE',  ( 0.2926469569035999863, -85.11057975687899102, -4.161840105401999779 ) ) ;
#39746=CARTESIAN_POINT ( 'NONE',  ( -2.040407335258644039, -78.82460961380570552, -3.421830084111916026 ) ) ;
#39750=CARTESIAN_POINT ( 'NONE',  ( 0.000000000000000000, -86.09999999999999432, 0.000000000000000000 ) ) ;
#39763=CARTESIAN_POINT ( 'NONE',  ( -3.620804144604786057, -78.99318692614357929, 0.06825924720741134710 ) ) ;
#39773=CARTESIAN_POINT ( 'NONE',  ( -3.770520861067999885, -78.43767549782629089, 1.207678794456000126 ) ) ;
#39811=CARTESIAN_POINT ( 'NONE',  ( -1.473365879748000040, -82.90842953870898668, 3.227033238383000047 ) ) ;
#39836=CARTESIAN_POINT ( 'NONE',  ( 1.533375225220143134, -86.36264283715698298, 3.533266005812232269 ) ) ;
#39871=CARTESIAN_POINT ( 'NONE',  ( 4.606177061618020652, -86.02148118236286223, 0.5287147981160357224 ) ) ;
#39877=CARTESIAN_POINT ( 'NONE',  ( 3.999999999999884981, -78.69999999999998863, -2.360693579763222694 ) ) ;
#39955=CARTESIAN_POINT ( 'NONE',  ( -1.733945428922999854, -82.98374735065199559, 3.797766467643000077 ) ) ;
#39985=CARTESIAN_POINT ( 'NONE',  ( 0.5018391472701999589, -79.41170382117660154, -3.722840512358000176 ) ) ;
#39996=CARTESIAN_POINT ( 'NONE',  ( -3.545429070608171696, -86.31452044229996545, 1.659291692407262930 ) ) ;
#39997=CARTESIAN_POINT ( 'NONE',  ( 1.437416630538960405, -85.91103235223293666, 3.161135301328009906 ) ) ;
#40002=CARTESIAN_POINT ( 'NONE',  ( -0.06039263125621000677, -80.01681542480598353, 4.129753795741000211 ) ) ;
#40005=CARTESIAN_POINT ( 'NONE',  ( -3.178331792343999762, -80.25300264934799088, -1.569449204645999796 ) ) ;
#40029=CARTESIAN_POINT ( 'NONE',  ( -3.413899980018999969, -86.06631758453399073, 2.398936571692999564 ) ) ;
#40035=CARTESIAN_POINT ( 'NONE',  ( -4.000000000000000000, -78.69999999915415856, 2.834003763004000336E-08 ) ) ;
#40039=SURFACE_SIDE_STYLE ('',( #11747 ) ) ;
#40050=ORIENTED_EDGE ( 'NONE', *, *, #15855, .T. ) ;
#40053=CARTESIAN_POINT ( 'NONE',  ( 3.407095545933001457, -78.77851879815550262, -1.253608761936364502E-15 ) ) ;
#40064=CARTESIAN_POINT ( 'NONE',  ( -1.152152900689999759, -81.33525264934799281, 4.012747624594999785 ) ) ;
#40093=CARTESIAN_POINT ( 'NONE',  ( 3.009949031611931947, -85.32916667478426120, -1.673658179043767458 ) ) ;
#40105=CARTESIAN_POINT ( 'NONE',  ( 0.000000000000000000, -78.69999999999998863, 0.000000000000000000 ) ) ;
#40132=CARTESIAN_POINT ( 'NONE',  ( -2.739132899390686049, -86.25171438276198899, 3.697400121254383887 ) ) ;
#40169=CARTESIAN_POINT ( 'NONE',  ( -2.127490919130949454, -78.43735717367049176, -3.528455608958080525 ) ) ;
#40203=CARTESIAN_POINT ( 'NONE',  ( 3.439647241017512069, -82.43854168378354075, -0.1699550553820542431 ) ) ;
#40253=CARTESIAN_POINT ( 'NONE',  ( 2.242205298352999865, -85.40032450217400140, -3.468575908922999940 ) ) ;
#40286=CARTESIAN_POINT ( 'NONE',  ( 3.542379078311999940, -81.33571061287598525, 1.250168379276000108 ) ) ;
#40299=CARTESIAN_POINT ( 'NONE',  ( 2.694001289665577392, -86.12610001270965654, -3.783547376761781322 ) ) ;
#40300=CARTESIAN_POINT ( 'NONE',  ( 3.277027672054567908, -85.82457000994830310, 1.444457732302927733 ) ) ;
#40307=CARTESIAN_POINT ( 'NONE',  ( -0.4143623072097000204, -80.85470891495099011, -3.941356880154000208 ) ) ;
#40310=CARTESIAN_POINT ( 'NONE',  ( -3.410048246405999794, -78.60958598268121023, 0.4931512766838000439 ) ) ;
#40332=CARTESIAN_POINT ( 'NONE',  ( 0.3110912592032999968, -82.61867690334500480, 4.118464764383999999 ) ) ;
#40340=CARTESIAN_POINT ( 'NONE',  ( -3.548349909811030045, -78.96264282632948550, 7.096699819622017458 ) ) ;
#40359=CARTESIAN_POINT ( 'NONE',  ( 2.322889840689416285, -78.72610001270986402, -4.022071228304580082 ) ) ;
#40370=CARTESIAN_POINT ( 'NONE',  ( -3.128728754627999820, -81.81625264934800157, -2.764173162666000216 ) ) ;
#40377=CARTESIAN_POINT ( 'NONE',  ( 2.575849577708000382, -83.78782518894399800, -2.439171769826999903 ) ) ;
#40392=CARTESIAN_POINT ( 'NONE',  ( -0.7077633922091999263, -84.67496544543098480, 3.689232043295000096 ) ) ;
#40410=CARTESIAN_POINT ( 'NONE',  ( 0.2672206133491000224, -82.78817953870900226, 3.537394210971000152 ) ) ;
#40433=CARTESIAN_POINT ( 'NONE',  ( -3.165820273081705327, -86.25171435493598437, 1.338596575002905409 ) ) ;
#40468=CARTESIAN_POINT ( 'NONE',  ( -0.5731199659188778162, -86.10000000000000853, 4.609165628485354382 ) ) ;
#40471=CARTESIAN_POINT ( 'NONE',  ( -3.474812103689401965, -78.54828564506388489, -1.963390115445670991 ) ) ;
#40524=CARTESIAN_POINT ( 'NONE',  ( -2.293836348570999828, -84.30218271708000088, 2.760807823936999750 ) ) ;
#40549=CARTESIAN_POINT ( 'NONE',  ( 3.636872000734241883, -82.55416664812710792, 1.696597269464540814 ) ) ;
#40554=CARTESIAN_POINT ( 'NONE',  ( 0.2926784520318999605, -85.14824735065198524, -4.164605519011000290 ) ) ;
#40584=CARTESIAN_POINT ( 'NONE',  ( 2.387822949045000254, -81.33957009409999728, 2.679934097432000062 ) ) ;
#40597=CARTESIAN_POINT ( 'NONE',  ( 3.638642783662472624, -85.80035203905988794, 0.7847452661105541738 ) ) ;
#40602=CARTESIAN_POINT ( 'NONE',  ( -3.804546608024999887, -81.93696273528199470, 1.109691581360999990 ) ) ;
#40630=CARTESIAN_POINT ( 'NONE',  ( -2.667996182181000098, -84.43400986860198998, 3.211137855840999755 ) ) ;
#40643=DIRECTION ( 'NONE',  ( 0.000000000000000000, 1.000000000000000000, 0.000000000000000000 ) ) ;
#40657=CARTESIAN_POINT ( 'NONE',  ( 3.962812355711000212, -78.85171438276199751, -1.463672932855430986E-15 ) ) ;
#40669=CARTESIAN_POINT ( 'NONE',  ( 2.459051015536999785, -79.03892549782628407, -3.318368392105000453 ) ) ;
#40693=CARTESIAN_POINT ( 'NONE',  ( 3.544514923079999935, -85.50899735065199536, 0.03711956419559000325 ) ) ;
#40696=CARTESIAN_POINT ( 'NONE',  ( 2.791771531253838923, -85.59895834061069309, 2.015565555989225377 ) ) ;
#40731=CARTESIAN_POINT ( 'NONE',  ( -2.557474545125634435, -86.40321104920798234, 3.452189813556158615 ) ) ;
#40734=CARTESIAN_POINT ( 'NONE',  ( -3.204655417894513025, -78.85416664733885739, -2.415670736004921881 ) ) ;
#40758=CARTESIAN_POINT ( 'NONE',  ( -0.5721033155199185538, -86.02148118236286223, 4.600989486740219014 ) ) ;
#40762=CARTESIAN_POINT ( 'NONE',  ( 3.400000000000108269, -78.67390000031812747, -2.006589542798860926 ) ) ;
#40773=CARTESIAN_POINT ( 'NONE',  ( -0.03689285838845265952, -78.48547955770028750, 3.914326906660362315 ) ) ;
#40817=CARTESIAN_POINT ( 'NONE',  ( -3.556697332079000518, -82.97942814914499365, 0.4833727558985000394 ) ) ;
#40826=CARTESIAN_POINT ( 'NONE',  ( 3.620209227050000145, -86.25171438276198899, -1.611820994701000043 ) ) ;
#40844=CARTESIAN_POINT ( 'NONE',  ( 2.191310644209000014, -85.68044503318799343, 3.550807881941000055 ) ) ;
#40872=CARTESIAN_POINT ( 'NONE',  ( -2.697861840213120921, -81.86041665153629765, -2.140231034139926436 ) ) ;
#40874=CARTESIAN_POINT ( 'NONE',  ( 2.359403609525000167, -79.53195424565778637, -3.184211391267000035 ) ) ;
#40891=CARTESIAN_POINT ( 'NONE',  ( -0.06101177358013000485, -79.81593595582098999, 4.172091831179000287 ) ) ;
#40894=AXIS2_PLACEMENT_3D ( 'NONE', #43556, #56268, #37955 ) ;
#40896=CARTESIAN_POINT ( 'NONE',  ( -3.405171369683000382, -81.64480496681198929, 0.9931618166635001188 ) ) ;
#40923=CARTESIAN_POINT ( 'NONE',  ( 3.596064725228000025, -85.38443645448099062, 2.031459853198999799 ) ) ;
#40931=CARTESIAN_POINT ( 'NONE',  ( 3.992904449609001372, -78.77851881763731967, 7.985808899218034718 ) ) ;
#40949=CARTESIAN_POINT ( 'NONE',  ( 3.999999999999675371, -78.69999999999998863, -2.360693579763098349 ) ) ;
#40963=CARTESIAN_POINT ( 'NONE',  ( -3.804558069882999938, -81.32753455456798974, 1.109648059985999913 ) ) ;
#40984=CARTESIAN_POINT ( 'NONE',  ( -3.722285329556000111, -83.47246544543099844, 0.5059190862433999847 ) ) ;
#40988=CARTESIAN_POINT ( 'NONE',  ( 1.884520266331757066, -85.21354167514409994, -2.882774053612764398 ) ) ;
#41021=CARTESIAN_POINT ( 'NONE',  ( -3.548349909811000291, -78.43735717349129288, 5.104432642529999417E-09 ) ) ;
#41022=ADVANCED_FACE ( 'NONE', ( #11591 ), #35799, .T. ) ;
#41035=CARTESIAN_POINT ( 'NONE',  ( -3.106054822367000146, -86.10000002299598520, 1.382903988153999952 ) ) ;
#41054=CARTESIAN_POINT ( 'NONE',  ( 3.112536659741981016, -86.02148120184399716, -1.385790604991043118 ) ) ;
#41057=CARTESIAN_POINT ( 'NONE',  ( -0.03487147506507188438, -78.39678895079168797, -3.699835669024340579 ) ) ;
#41069=CARTESIAN_POINT ( 'NONE',  ( -2.171317872500211799, -78.40681307385641219, 3.601143492177988570 ) ) ;
#41107=CARTESIAN_POINT ( 'NONE',  ( 2.619065415988000023, -83.94143147127900306, 2.454433006111999660 ) ) ;
#41115=CARTESIAN_POINT ( 'NONE',  ( 3.451879464910999840, -86.39318692756698681, -1.536875756006000016 ) ) ;
#41117=CARTESIAN_POINT ( 'NONE',  ( 3.654181830570650824, -86.07389998728979208, -1.626946572303439753 ) ) ;
#41131=CARTESIAN_POINT ( 'NONE',  ( -1.831734064479000113, -85.92094503318799070, 3.749003839799999849 ) ) ;
#41157=CARTESIAN_POINT ( 'NONE',  ( 2.228740036544774483, -80.74270832256439689, -2.625067772272801747 ) ) ;
#41180=CARTESIAN_POINT ( 'NONE',  ( 4.116256581921999391, -80.89818977615198037, -0.6830113048311999835 ) ) ;
#41206=CARTESIAN_POINT ( 'NONE',  ( 3.648109280413999844, -82.37817607281098731, 1.936498112586999998 ) ) ;
#41218=PRESENTATION_STYLE_ASSIGNMENT (( #32339 ) ) ;
#41247=EDGE_CURVE ( 'NONE', #9865, #34390, #7045, .T. ) ;
#41251=CARTESIAN_POINT ( 'NONE',  ( 0.5296260211451999655, -78.80228455456848735, -3.927530026132000529 ) ) ;
#41274=CARTESIAN_POINT ( 'NONE',  ( 1.964367198619000110, -82.87507450217398741, 3.004155151946999780 ) ) ;
#41277=CARTESIAN_POINT ( 'NONE',  ( -1.308541769128729326, -84.98229167586391952, -3.186053244962748110 ) ) ;
#41314=CARTESIAN_POINT ( 'NONE',  ( -1.161982140497694216, -79.89479165893936852, 3.880497637639665154 ) ) ;
#41344=CARTESIAN_POINT ( 'NONE',  ( -3.131568623105725369, -86.10000000000019327, 1.324114027861367449 ) ) ;
#41348=CARTESIAN_POINT ( 'NONE',  ( 3.548349909810999847, -78.43735717367049176, -2.094141712711119485 ) ) ;
#41360=CARTESIAN_POINT ( 'NONE',  ( -3.699342699771063447, -78.39678895079168797, -0.06973942363209935380 ) ) ;
#41378=CARTESIAN_POINT ( 'NONE',  ( 3.227959076126192262, -83.86458334601041997, -1.201676990424012326 ) ) ;
#41401=CARTESIAN_POINT ( 'NONE',  ( -1.490802228383000028, -82.73892731861099037, 3.265157211617999877 ) ) ;
#41412=CARTESIAN_POINT ( 'NONE',  ( 3.106054555984663956, -86.10000000000019327, -1.382904586457956553 ) ) ;
#41414=CARTESIAN_POINT ( 'NONE',  ( 3.912590402935000267, -82.39999999999999147, -0.8316467632710000668 ) ) ;
#41426=CARTESIAN_POINT ( 'NONE',  ( -3.349446900146999972, -83.02867953870898532, 2.487518992154000408 ) ) ;
#41453=CARTESIAN_POINT ( 'NONE',  ( -2.345309999012545443, -80.39583332391796944, -2.522288602443209182 ) ) ;
#41465=CARTESIAN_POINT ( 'NONE',  ( 2.338897668117772888, -85.88596255424737080, 3.133429492702677344 ) ) ;
#41470=CARTESIAN_POINT ( 'NONE',  ( -3.200164631505999946, -78.92298487743470048, -2.681188903621000374 ) ) ;
#41475=CARTESIAN_POINT ( 'NONE',  ( 1.666530149241000069, -79.72707046129099240, 3.131649709249999969 ) ) ;
#41499=CARTESIAN_POINT ( 'NONE',  ( 3.490791149790999803, -85.02754468068998506, -1.876264172078000225 ) ) ;
#41506=CARTESIAN_POINT ( 'NONE',  ( -3.999999999999848566, -78.72610001270986402, 7.999999999999648281 ) ) ;
#41520=CARTESIAN_POINT ( 'NONE',  ( -3.405565740252999518, -81.61342682855999442, 0.9933187896184001442 ) ) ;
#41527=CARTESIAN_POINT ( 'NONE',  ( 2.301294140410000022, -78.85171438276198330, -3.984678389768961271 ) ) ;
#41541=CARTESIAN_POINT ( 'NONE',  ( -3.812522663964000191, -78.36136788790179253, 0.5513559584095000243 ) ) ;
#41563=CARTESIAN_POINT ( 'NONE',  ( 0.2829668327839999775, -83.11171544543098832, 3.745838405360000234 ) ) ;
#41600=CARTESIAN_POINT ( 'NONE',  ( 3.521763997193422036, -82.70470561765866080, -0.7485769115635626525 ) ) ;
#41602=CARTESIAN_POINT ( 'NONE',  ( 1.589609816838088552, -86.17851881763699851, 3.662844055364134377 ) ) ;
#41630=CARTESIAN_POINT ( 'NONE',  ( 3.922208058606658998, -86.10000000000017906, 0.4502061935813617133 ) ) ;
#41648=CARTESIAN_POINT ( 'NONE',  ( 2.148673218084974135, -78.39678895079168797, 3.720415760332554278 ) ) ;
#41665=CARTESIAN_POINT ( 'NONE',  ( 0.2803209884194523549, -83.59479168018397388, -3.431695889835921776 ) ) ;
#41684=CARTESIAN_POINT ( 'NONE',  ( 0.6656042537174000628, -82.13207046129099353, -4.118670586540000400 ) ) ;
#41690=CARTESIAN_POINT ( 'NONE',  ( -1.507731777991000000, -84.78318437814699848, -3.257374696832999739 ) ) ;
#41702=CARTESIAN_POINT ( 'NONE',  ( -6.128066803784989247, -85.83735717367099483, -5.039913953694903803 ) ) ;
#41716=CARTESIAN_POINT ( 'NONE',  ( -3.884332861548999816, -84.59819503318799150, 1.523817745045000116 ) ) ;
#41745=CARTESIAN_POINT ( 'NONE',  ( 1.651882416763933437, -81.20520832075965245, 3.020993344137217207 ) ) ;
#41763=CARTESIAN_POINT ( 'NONE',  ( 3.795871755532000513, -79.40398657535959615, -1.738093195592000040 ) ) ;
#41768=CARTESIAN_POINT ( 'NONE',  ( -2.658223501415000189, -81.88530496681200077, -2.348490597694000037 ) ) ;
#41792=CARTESIAN_POINT ( 'NONE',  ( 0.2985038077467999651, -82.50228596008699355, 3.951822424672999823 ) ) ;
#41812=CARTESIAN_POINT ( 'NONE',  ( 2.111974152998999710, -79.20841833893540240, -2.850284762170999908 ) ) ;
#41837=CARTESIAN_POINT ( 'NONE',  ( -0.06054963955015999627, -79.64017549782629146, 4.129750263999999227 ) ) ;
#41856=CARTESIAN_POINT ( 'NONE',  ( 0.2985269866015999862, -83.11171544543098832, 3.951819513428000086 ) ) ;
#41864=FACE_OUTER_BOUND ( 'NONE', #229, .T. ) ;
#41909=CARTESIAN_POINT ( 'NONE',  ( -3.308356911591993743, -85.80681307385599155, 1.472975398279013692 ) ) ;
#41926=CARTESIAN_POINT ( 'NONE',  ( -2.409209601448396576, -85.88547957940600952, 3.252055376540686105 ) ) ;
#41930=CARTESIAN_POINT ( 'NONE',  ( -2.038544480927606983, -78.70000000000000284, -3.380937442862391951 ) ) ;
#41977=CARTESIAN_POINT ( 'NONE',  ( 1.959975192012000100, -79.72707046129099240, 3.683075126482999728 ) ) ;
#41983=CARTESIAN_POINT ( 'NONE',  ( -3.515158122207999725, -83.18657311260999165, 0.4777273718585999807 ) ) ;
#41995=CARTESIAN_POINT ( 'NONE',  ( -6.908074975177627586, -86.09999999999999432, -5.681417088837195983 ) ) ;
#42006=CARTESIAN_POINT ( 'NONE',  ( -1.945056384218381451, -85.94583335130319313, 3.510275759367116777 ) ) ;
#42010=CARTESIAN_POINT ( 'NONE',  ( -0.7861470525832999767, -84.35769503318799423, 4.097808574246000646 ) ) ;
#42019=CARTESIAN_POINT ( 'NONE',  ( 0.000000000000000000, -78.69999999999998863, 0.000000000000000000 ) ) ;
#42038=CARTESIAN_POINT ( 'NONE',  ( 0.6616675926900500437, -79.77916665965761922, 3.378914762188844900 ) ) ;
#42051=CARTESIAN_POINT ( 'NONE',  ( 3.513334747297280902, -85.82276510432375005, 1.485566327356647731 ) ) ;
#42057=CARTESIAN_POINT ( 'NONE',  ( 1.621761508983999844, -80.72674124465299883, -3.847011800229999778 ) ) ;
#42059=B_SPLINE_CURVE_WITH_KNOTS ( 'NONE', 3,
 ( #48978, #25947, #21233, #56964, #53394, #16527, #30365, #43688, #8520, #26514, #34800, #34506, #25657, #8233, #3242 ),
 .UNSPECIFIED., .F., .F.,
 ( 4, 1, 1, 1, 1, 1, 1, 1, 1, 1, 1, 1, 4 ),
 ( 0.000000000000000000, 0.08333611588665000569, 0.1666676715620999949, 0.2500039875833999781, 0.3333306964953999807, 0.4166666792817999565, 0.4999999999924999994, 0.5833333197091999933, 0.6666692694150000431, 0.7499959719902999922, 0.8333323089881000678, 0.9166638425153998959, 1.000000000000000000 ),
 .UNSPECIFIED. ) ;
#42088=CARTESIAN_POINT ( 'NONE',  ( -1.560211831905000013, -82.62253637535398809, 3.417178226333000168 ) ) ;
#42101=APPLICATION_CONTEXT ( 'automotive_design' ) ;
#42109=CARTESIAN_POINT ( 'NONE',  ( -0.9788390260998998116, -81.37919147407698972, 3.409317240057000209 ) ) ;
#42134=CARTESIAN_POINT ( 'NONE',  ( 3.746130956990000094, -79.16303455456849747, 0.2790430962004000204 ) ) ;
#42137=CARTESIAN_POINT ( 'NONE',  ( -3.407095545933000569, -78.77851879815550262, -1.429604595782733033E-14 ) ) ;
#42153=CARTESIAN_POINT ( 'NONE',  ( 3.450648315675999722, -85.87746544543099958, 1.949103487304999938 ) ) ;
#42168=CARTESIAN_POINT ( 'NONE',  ( 2.264139176916503349, -78.96952922072273395, -2.758663917053780334 ) ) ;
#42196=CARTESIAN_POINT ( 'NONE',  ( 0.8825830062794586262, -80.62708333376913572, -3.954198616316053627 ) ) ;
#42206=( BOUNDED_SURFACE ( )  B_SPLINE_SURFACE ( 3, 3, ( 
 ( #18689, #5972, #41995, #24277 ),
 ( #41117, #1563, #14822, #19555 ),
 ( #5393, #27523, #37553, #45565 ),
 ( #55570, #6262, #55276, #14242 ),
 ( #15119, #42295, #36391, #46742 ),
 ( #10412, #32821, #10713, #36973 ),
 ( #54417, #33117, #23109, #28691 ),
 ( #1278, #36682, #5678, #31949 ),
 ( #23689, #28104, #54986, #28397 ),
 ( #49994, #9540, #41702, #5110 ),
 ( #46154, #54698, #711, #19271 ),
 ( #18981, #50571, #50281, #14534 ),
 ( #37262, #32528, #32238, #9832 ),
 ( #50866, #27813, #45860, #23402 ),
 ( #41412, #995, #48184, #2723 ) ),
 .UNSPECIFIED., .F., .F., .F. ) 
 B_SPLINE_SURFACE_WITH_KNOTS ( ( 4, 1, 1, 1, 1, 1, 1, 1, 1, 1, 1, 1, 4 ),
 ( 4, 4 ),
 ( 0.009836358966825000175, 0.09153389967814999639, 0.1732269073519000224, 0.2549246240467999969, 0.3366128957582000258, 0.4183102327763000283, 0.5000049915180999616, 0.5816997512343000665, 0.6633971206824998967, 0.7450853986059999823, 0.8267830947368000061, 0.9084761241232000017, 0.9901736480482069558 ),
 ( 0.000000000000000000, 1.000000000000000000 ),
 .UNSPECIFIED. ) 
 GEOMETRIC_REPRESENTATION_ITEM ( )  RATIONAL_B_SPLINE_SURFACE ( (
 ( 1.000000000000000000, 0.3333333333333369786, 0.3333333333333369786, 1.000000000000000000),
 ( 1.000000000000000000, 0.3333333333333369786, 0.3333333333333369786, 1.000000000000000000),
 ( 1.000000000000000000, 0.3333333333333369786, 0.3333333333333369786, 1.000000000000000000),
 ( 1.000000000000000000, 0.3333333333333369786, 0.3333333333333369786, 1.000000000000000000),
 ( 1.000000000000000000, 0.3333333333333369786, 0.3333333333333369786, 1.000000000000000000),
 ( 1.000000000000000000, 0.3333333333333369786, 0.3333333333333369786, 1.000000000000000000),
 ( 1.000000000000000000, 0.3333333333333369786, 0.3333333333333369786, 1.000000000000000000),
 ( 1.000000000000000000, 0.3333333333333369786, 0.3333333333333369786, 1.000000000000000000),
 ( 1.000000000000000000, 0.3333333333333369786, 0.3333333333333369786, 1.000000000000000000),
 ( 1.000000000000000000, 0.3333333333333369786, 0.3333333333333369786, 1.000000000000000000),
 ( 1.000000000000000000, 0.3333333333333369786, 0.3333333333333369786, 1.000000000000000000),
 ( 1.000000000000000000, 0.3333333333333369786, 0.3333333333333369786, 1.000000000000000000),
 ( 1.000000000000000000, 0.3333333333333369786, 0.3333333333333369786, 1.000000000000000000),
 ( 1.000000000000000000, 0.3333333333333369786, 0.3333333333333369786, 1.000000000000000000),
 ( 1.000000000000000000, 0.3333333333333369786, 0.3333333333333369786, 1.000000000000000000) ) ) 
 REPRESENTATION_ITEM ( '' )  SURFACE ( )  );
#42225=CARTESIAN_POINT ( 'NONE',  ( 1.368374140978463993, -85.94828564506399005, 3.153063748541422129 ) ) ;
#42239=CARTESIAN_POINT ( 'NONE',  ( 3.400000000000108713, -78.67390000031814168, -4.163799117101134173E-16 ) ) ;
#42281=CARTESIAN_POINT ( 'NONE',  ( -2.281180096131999679, -83.42707394314300018, -2.716758612191999767 ) ) ;
#42295=CARTESIAN_POINT ( 'NONE',  ( 0.3917325915499037525, -85.88547955770000897, -8.744319679239929144 ) ) ;
#42306=CARTESIAN_POINT ( 'NONE',  ( 3.651490241511724300, -84.05729166430741373, 1.754833245226501859 ) ) ;
#42338=PRODUCT_CONTEXT ( 'NONE', #42101, 'mechanical' ) ;
#42355=CARTESIAN_POINT ( 'NONE',  ( -4.094075590313999591, -78.72741664101050674, -0.8028934812383000663 ) ) ;
#42384=CARTESIAN_POINT ( 'NONE',  ( 2.741005327708999850, -83.82504052802198657, 2.568707870063999810 ) ) ;
#42405=CARTESIAN_POINT ( 'NONE',  ( -3.026233407092999705, -80.05643680478300439, 1.850265178281999878 ) ) ;
#42430=CARTESIAN_POINT ( 'NONE',  ( -2.051600333657000341, -80.24142549782600042, -2.945279881917999720 ) ) ;
#42449=CARTESIAN_POINT ( 'NONE',  ( -3.929712059496000442, -85.03571544543099492, -0.5131704721504000144 ) ) ;
#42457=CARTESIAN_POINT ( 'NONE',  ( 3.914500761937000028, -78.91452044229970397, 0.000000000000000000 ) ) ;
#42462=CARTESIAN_POINT ( 'NONE',  ( 2.220969153522253325, -78.96057212360685185, -3.162631883084828566 ) ) ;
#42482=CARTESIAN_POINT ( 'NONE',  ( -3.437217408589349432, -78.72609999968184979, -1.942147800595246165 ) ) ;
#42513=EDGE_LOOP ( 'NONE', ( #12380, #30590, #30743, #22623 ) ) ;
#42528=CARTESIAN_POINT ( 'NONE',  ( -3.399395994687390399, -78.70000000000000284, -0.06408487577575257277 ) ) ;
#42571=CARTESIAN_POINT ( 'NONE',  ( -0.6683986366931999878, -84.38281177079799988, 3.483505843786999900 ) ) ;
#42598=CARTESIAN_POINT ( 'NONE',  ( 1.197295183284138975, -85.75312501589537817, 3.856364711603536222 ) ) ;
#42602=ORIENTED_EDGE ( 'NONE', *, *, #28766, .T. ) ;
#42643=CARTESIAN_POINT ( 'NONE',  ( 3.494359274950000316, -79.56916961237898533, 2.279475529283999879 ) ) ;
#42671=CARTESIAN_POINT ( 'NONE',  ( -3.776522694978999617, -85.86929758755698572, 0.4127208475760000272 ) ) ;
#42692=CARTESIAN_POINT ( 'NONE',  ( -2.658558477971000311, -81.85392767752199461, -2.348749639193000061 ) ) ;
#42704=CARTESIAN_POINT ( 'NONE',  ( -3.079437091258620196, -86.09999999999995168, 1.441203386403855591 ) ) ;
#42716=CARTESIAN_POINT ( 'NONE',  ( -1.357221183918999818, -78.68203455456848872, -3.502749927983000333 ) ) ;
#42737=CARTESIAN_POINT ( 'NONE',  ( 3.840625598965000442, -84.31421544543098889, 0.9775355813133997929 ) ) ;
#42738=CARTESIAN_POINT ( 'NONE',  ( 3.184161977317999881, -85.88547957940599531, -1.417680250971000033 ) ) ;
#42745=CARTESIAN_POINT ( 'NONE',  ( 3.471918836458000257, -82.34482020574199623, -1.985174022353000334 ) ) ;
#42749=ADVANCED_FACE ( 'NONE', ( #30998 ), #50146, .F. ) ;
#42862=CARTESIAN_POINT ( 'NONE',  ( 0.1743336006483000022, -85.82581675399998744, 3.542757096472000100 ) ) ;
#42888=CARTESIAN_POINT ( 'NONE',  ( -0.08687330363763785812, -85.83020835005841320, 4.012123666634238361 ) ) ;
#42929=CARTESIAN_POINT ( 'NONE',  ( 3.647699722740822548, -86.17851881763699851, -1.624060551956400866 ) ) ;
#42931=CIRCLE ( 'NONE', #40894, 3.400000000000000799 ) ;
#42983=CARTESIAN_POINT ( 'NONE',  ( 3.496897448754000326, -80.96724209361498481, -0.5802409159389999571 ) ) ;
#42998=CARTESIAN_POINT ( 'NONE',  ( -3.280005808348441576, -86.39318692614396866, 1.535071293332731734 ) ) ;
#43007=CARTESIAN_POINT ( 'NONE',  ( -3.666040373708999933, -81.44778455456800259, -0.8194572562286999151 ) ) ;
#43012=CARTESIAN_POINT ( 'NONE',  ( 1.862820775644999927, -85.68044503318799343, 3.018521682574000220 ) ) ;
#43066=CARTESIAN_POINT ( 'NONE',  ( -3.962812355711000212, -78.54828561713269153, 3.526087981832999841E-09 ) ) ;
#43069=CARTESIAN_POINT ( 'NONE',  ( -1.005435018732895314, -82.01458334923671600, -3.884934934212340263 ) ) ;
#43154=CARTESIAN_POINT ( 'NONE',  ( -3.514851922797999961, -84.67451069913499850, -0.4591155470951999717 ) ) ;
#43175=CARTESIAN_POINT ( 'NONE',  ( -2.394033331947576837, -78.62148118236265759, -3.970517693957353877 ) ) ;
#43179=CARTESIAN_POINT ( 'NONE',  ( -2.639864145299684939, -84.90520834010136753, -3.072390398173608261 ) ) ;
#43213=CARTESIAN_POINT ( 'NONE',  ( 3.757989199629905297, -86.09999999999978115, 2.729540522067947173 ) ) ;
#43272=CARTESIAN_POINT ( 'NONE',  ( -0.05183153944128000151, -79.88498827328399443, 3.544331357887999800 ) ) ;
#43294=CARTESIAN_POINT ( 'NONE',  ( -1.296842085168999903, -78.79842549782625838, -3.346922059760999879 ) ) ;
#43299=CARTESIAN_POINT ( 'NONE',  ( 0.2486648094367000239, -85.07919503318798604, -3.538322792724999832 ) ) ;
#43319=CARTESIAN_POINT ( 'NONE',  ( 2.190920801479000257, -85.71183183321298316, 3.550554600649999948 ) ) ;
#43325=CARTESIAN_POINT ( 'NONE',  ( 2.758540696617810983, -78.99078869009431969, -2.352279292788579390 ) ) ;
#43341=CARTESIAN_POINT ( 'NONE',  ( -3.699342691684420537, -79.00321104920828930, 0.06973985258851372881 ) ) ;
#43349=CARTESIAN_POINT ( 'NONE',  ( -3.331633925631045656, -81.84114584730329511, -2.236105189373023272 ) ) ;
#43351=CARTESIAN_POINT ( 'NONE',  ( -1.151390654609000030, -81.41057046129098751, 4.010092854424000208 ) ) ;
#43393=CARTESIAN_POINT ( 'NONE',  ( 3.912590402935000267, -82.39999999999999147, -0.8316467632710000668 ) ) ;
#43413=CARTESIAN_POINT ( 'NONE',  ( -3.131568623105961624, -86.09999999999998010, 1.324114027861469589 ) ) ;
#43434=CARTESIAN_POINT ( 'NONE',  ( -3.380480680714999853, -86.19283349427999497, 0.3694390222027000292 ) ) ;
#43455=CARTESIAN_POINT ( 'NONE',  ( -0.03763201836869552869, -78.62148118236265759, -3.992727109996482060 ) ) ;
#43463=CARTESIAN_POINT ( 'NONE',  ( -3.654181822837000215, -86.09999999943198645, 1.626946589673999854 ) ) ;
#43482=EDGE_LOOP ( 'NONE', ( #25539, #20111, #36717, #31469 ) ) ;
#43526=AXIS2_PLACEMENT_3D ( 'NONE', #45889, #10156, #14564 ) ;
#43556=CARTESIAN_POINT ( 'NONE',  ( 0.000000000000000000, -86.09999999999999432, 0.000000000000000000 ) ) ;
#43558=CARTESIAN_POINT ( 'NONE',  ( 2.110329786959999954, -79.28373615087838289, -2.848065553447999942 ) ) ;
#43583=CARTESIAN_POINT ( 'NONE',  ( 3.534916081315999659, -79.41125264934790096, 0.2633100496122000589 ) ) ;
#43586=CARTESIAN_POINT ( 'NONE',  ( 2.586521478039999877, -84.18624735065199616, 2.423813200681999902 ) ) ;
#43609=CARTESIAN_POINT ( 'NONE',  ( -3.351688600863999667, -82.99100488540000242, 2.489135118475000130 ) ) ;
#43614=CARTESIAN_POINT ( 'NONE',  ( -3.407095545933000569, -78.77851879815550262, -1.429604595782732717E-14 ) ) ;
#43615=EDGE_LOOP ( 'NONE', ( #48201, #53390, #43678, #10753 ) ) ;
#43632=CARTESIAN_POINT ( 'NONE',  ( -0.03211093172565316484, -78.77851879815550262, -3.406944224254369047 ) ) ;
#43646=CARTESIAN_POINT ( 'NONE',  ( -4.005234755443000338, -81.65107046129099899, 1.168177984020000171 ) ) ;
#43678=ORIENTED_EDGE ( 'NONE', *, *, #23990, .T. ) ;
#43688=CARTESIAN_POINT ( 'NONE',  ( 3.699999999670000150, -78.39678895079168797, 0.000000000000000000 ) ) ;
#43709=CARTESIAN_POINT ( 'NONE',  ( -3.131568623105350113, -86.12609999968211127, 1.324114027861438503 ) ) ;
#43732=CARTESIAN_POINT ( 'NONE',  ( -1.507575758304999791, -78.96791748997289062, -3.890205925644000029 ) ) ;
#43798=CARTESIAN_POINT ( 'NONE',  ( -2.764837346328719025, -86.09999999999978115, 3.732097096069707742 ) ) ;
#43830=CARTESIAN_POINT ( 'NONE',  ( -3.242402341787999909, -86.35846544543099412, 2.278681733043999902 ) ) ;
#43857=CARTESIAN_POINT ( 'NONE',  ( -1.778283081280999989, -80.13706584928699783, 3.117924708102000064 ) ) ;
#43868=CARTESIAN_POINT ( 'NONE',  ( 3.184161977317942149, -86.31452042059399332, -1.417680250971129707 ) ) ;
#43875=CARTESIAN_POINT ( 'NONE',  ( 0.9179173133781000082, -81.45982051858098316, 4.026902219962999574 ) ) ;
#43879=CARTESIAN_POINT ( 'NONE',  ( -3.402924446111000201, -81.57575264934799009, 0.9925064726425999462 ) ) ;
#43883=CARTESIAN_POINT ( 'NONE',  ( 2.951758530439000161, -82.31344503318798900, -1.687752529438000026 ) ) ;
#43902=CARTESIAN_POINT ( 'NONE',  ( 4.172307193540000014, -85.46506550819998438, 0.04387830479587000176 ) ) ;
#43907=CARTESIAN_POINT ( 'NONE',  ( -3.699999999670031237, -79.00321104920828930, 7.399999999340018064 ) ) ;
#43924=CARTESIAN_POINT ( 'NONE',  ( -3.893811372584298880, -78.96264283715740362, -2.200139326159465281 ) ) ;
#43932=CARTESIAN_POINT ( 'NONE',  ( 3.979601129954999816, -82.48655496681199395, 0.4014263888467000108 ) ) ;
#43971=CARTESIAN_POINT ( 'NONE',  ( 2.575800521921999930, -83.75017953870899134, -2.439222067143000494 ) ) ;
#43994=CARTESIAN_POINT ( 'NONE',  ( -3.480234241935507900, -86.39318692756698681, 1.471539517285501475 ) ) ;
#44013=CARTESIAN_POINT ( 'NONE',  ( 2.571160684530000129, -82.22094444544498515, -3.286247495836000176 ) ) ;
#44024=ADVANCED_BREP_SHAPE_REPRESENTATION ( '', ( #57583, #43526 ), #13324 ) ;
#44027=CARTESIAN_POINT ( 'NONE',  ( -3.684198380124839023, -86.07389998728979208, 1.557781209248620957 ) ) ;
#44110=CARTESIAN_POINT ( 'NONE',  ( 2.283504659536000236, -82.67419503318798490, 3.492219933351000005 ) ) ;
#44136=CARTESIAN_POINT ( 'NONE',  ( -0.4035306080773887194, -79.04687499584814248, -3.408455983050635130 ) ) ;
#44138=CARTESIAN_POINT ( 'NONE',  ( 3.440333001647999822, -82.42136181958099428, -0.2267620307923000067 ) ) ;
#44152=CARTESIAN_POINT ( 'NONE',  ( -3.597908783441192249, -86.39318692756698681, -2.511058746283273191 ) ) ;
#44153=CARTESIAN_POINT ( 'NONE',  ( 1.604468093511001614, -85.90488784433034652, 3.083698236688781513 ) ) ;
#44159=CARTESIAN_POINT ( 'NONE',  ( -1.390935043183000097, -82.18132306546799271, -3.888936835908999967 ) ) ;
#44162=CARTESIAN_POINT ( 'NONE',  ( -3.180430419197999736, -80.32205496681199008, -1.570485499300999788 ) ) ;
#44165=CARTESIAN_POINT ( 'NONE',  ( -0.6860765926954999205, -83.58499735065198877, -3.477680648429000154 ) ) ;
#44186=CARTESIAN_POINT ( 'NONE',  ( 1.289148685043999931, -84.26882685001099560, 3.967952992048999761 ) ) ;
#44192=CARTESIAN_POINT ( 'NONE',  ( -3.999999999999745093, -78.71311462308116802, -0.4401583980473047220 ) ) ;
#44208=CARTESIAN_POINT ( 'NONE',  ( -2.309341173333539388, -78.96264283715740362, -3.830055274395752551 ) ) ;
#44218=CARTESIAN_POINT ( 'NONE',  ( -3.561950367126999861, -80.01250264934799361, 2.177638482891999683 ) ) ;
#44253=CARTESIAN_POINT ( 'NONE',  ( -3.309179897806000525, -83.26917953870899680, -1.278233535900999973 ) ) ;
#44274=CARTESIAN_POINT ( 'NONE',  ( -2.662296488501999292, -86.36264283715698298, 3.593683008806643375 ) ) ;
#44294=CARTESIAN_POINT ( 'NONE',  ( -2.384769505383999899, -80.41092258374798973, -3.423365290318999943 ) ) ;
#44308=CARTESIAN_POINT ( 'NONE',  ( -3.649946715412256015, -85.94828561723799965, 1.543298655875836367 ) ) ;
#44312=CARTESIAN_POINT ( 'NONE',  ( -0.03769889196560113204, -78.69999999999998863, -3.999822345247804556 ) ) ;
#44389=CARTESIAN_POINT ( 'NONE',  ( 1.269300699276999955, -83.70524735065198740, -3.977244714148000071 ) ) ;
#44421=CARTESIAN_POINT ( 'NONE',  ( -1.861077379058000192, -80.25345679254499487, 3.263090789613000364 ) ) ;
#44432=CARTESIAN_POINT ( 'NONE',  ( -3.523111701668359963, -86.40321104920798234, -2.458856237079841467 ) ) ;
#44443=CARTESIAN_POINT ( 'NONE',  ( -3.502948155309999922, -81.56417549782598542, -0.7830018197964999649 ) ) ;
#44464=CARTESIAN_POINT ( 'NONE',  ( 3.029714949896999965, -83.78155969446399354, -2.868954476365999984 ) ) ;
#44471=CARTESIAN_POINT ( 'NONE',  ( 1.630469595029759189, -78.93919352839404269, -3.527628001382114409 ) ) ;
#44491=CARTESIAN_POINT ( 'NONE',  ( -2.060841138106245474, -78.85171435493610659, -3.417916573713450479 ) ) ;
#44502=CARTESIAN_POINT ( 'NONE',  ( 1.961272738943000027, -79.65175264934788402, 3.685513403684000266 ) ) ;
#44509=CARTESIAN_POINT ( 'NONE',  ( -1.557495164653000197, -85.95233266374599168, 3.187306976996000074 ) ) ;
#44527=CARTESIAN_POINT ( 'NONE',  ( 3.083885533095168885, -85.56041667406407214, 1.532545329980541604 ) ) ;
#44542=CARTESIAN_POINT ( 'NONE',  ( -1.557331793415999810, -85.91467953870898100, 3.187385650886000121 ) ) ;
#44567=CARTESIAN_POINT ( 'NONE',  ( 3.677662896325522457, -86.31452044230000809, 2.671197113342799856 ) ) ;
#44604=CARTESIAN_POINT ( 'NONE',  ( 4.614362421890519705, -86.10000000000000853, 0.5296543453898030496 ) ) ;
#44609=CARTESIAN_POINT ( 'NONE',  ( -2.265513919728744163, -78.40681307243319509, -3.757367528743593699 ) ) ;
#44621=CARTESIAN_POINT ( 'NONE',  ( 3.962812355711000212, -78.54828561723799396, -4.853045467043058701E-16 ) ) ;
#44689=CARTESIAN_POINT ( 'NONE',  ( 3.677265727246999738, -85.38874735065199673, -1.976693371404000255 ) ) ;
#44721=CARTESIAN_POINT ( 'NONE',  ( 1.861913176741999854, -80.01295594358298047, 3.498466738908999840 ) ) ;
#44733=CARTESIAN_POINT ( 'NONE',  ( -3.773359617072352457, -86.25171438276197478, -2.633509696780396592 ) ) ;
#44734=CARTESIAN_POINT ( 'NONE',  ( 3.047513760736739741, -85.83947020242759152, 1.827440418503480490 ) ) ;
#44740=CARTESIAN_POINT ( 'NONE',  ( -3.770453462111999610, -78.81431117999389357, 1.207889202028999964 ) ) ;
#44743=CARTESIAN_POINT ( 'NONE',  ( -2.501232889508999691, -81.45550264934799145, 2.511732025391000267 ) ) ;
#44766=CARTESIAN_POINT ( 'NONE',  ( 0.2051906278595000133, -85.75676443653598824, 4.169824694008999799 ) ) ;
#44773=CARTESIAN_POINT ( 'NONE',  ( 3.548349909811000291, -78.96264282632948550, -4.345475359304840494E-16 ) ) ;
#44803=CARTESIAN_POINT ( 'NONE',  ( 2.777255051931000196, -81.09475264934799554, 3.117122737064000226 ) ) ;
#44810=CARTESIAN_POINT ( 'NONE',  ( -3.302484149747999975, -84.62957809581099866, 1.295437536289999914 ) ) ;
#44825=CARTESIAN_POINT ( 'NONE',  ( 1.160825211897999809, -84.55471544543098616, 3.572652644192999993 ) ) ;
#44831=CARTESIAN_POINT ( 'NONE',  ( 0.5288065283753385915, -84.28854167802401776, 3.403152181769989681 ) ) ;
#44842=CARTESIAN_POINT ( 'NONE',  ( 2.952109282631000031, -82.30717953870899350, -1.687953082055999809 ) ) ;
#44845=ORIENTED_EDGE ( 'NONE', *, *, #31831, .T. ) ;
#44867=CARTESIAN_POINT ( 'NONE',  ( 3.200957065930781997, -86.17851879815599148, 2.324951338795794520 ) ) ;
#44904=CARTESIAN_POINT ( 'NONE',  ( -3.406490272659984164, -78.62148120184446043, 0.06421901112149774882 ) ) ;
#44958=CARTESIAN_POINT ( 'NONE',  ( -3.073513311004000048, -85.74904717229100015, 2.159747950585999998 ) ) ;
#44968=CARTESIAN_POINT ( 'NONE',  ( 3.112536659742000111, -86.17851879815599148, -1.385790604991000041 ) ) ;
#44985=CARTESIAN_POINT ( 'NONE',  ( -4.136841678191000682, -83.22424735065199286, 0.5622640331050000606 ) ) ;
#45018=CARTESIAN_POINT ( 'NONE',  ( 3.481401630171999884, -82.62224128856598782, -0.2294689796840000129 ) ) ;
#45031=CARTESIAN_POINT ( 'NONE',  ( 3.451879464910937667, -86.39318692756698681, -1.536875756006140570 ) ) ;
#45032=CARTESIAN_POINT ( 'NONE',  ( -1.186912087925585668, -86.00353166888481837, 3.216022959499840628 ) ) ;
#45039=CARTESIAN_POINT ( 'NONE',  ( 3.779826505644000356, -82.77871570665098488, 0.3812790984862000077 ) ) ;
#45043=CARTESIAN_POINT ( 'NONE',  ( -3.462036690261000249, -81.77132046129098342, -0.7738570222820000399 ) ) ;
#45067=CARTESIAN_POINT ( 'NONE',  ( 4.045858611978000674, -83.95300820753398341, 1.029872831580999959 ) ) ;
#45075=CARTESIAN_POINT ( 'NONE',  ( -3.914500761937000028, -78.91452044229970397, -1.642509933758750038E-14 ) ) ;
#45107=CARTESIAN_POINT ( 'NONE',  ( -4.005639385872000524, -81.64480496681198929, 1.168295999664000107 ) ) ;
#45131=CARTESIAN_POINT ( 'NONE',  ( 0.2703784039104000225, -82.99532450217398605, 3.579196188411999824 ) ) ;
#45134=CARTESIAN_POINT ( 'NONE',  ( -2.641601459057217660, -84.86666667622432669, -2.210339097018351850 ) ) ;
#45148=CARTESIAN_POINT ( 'NONE',  ( 3.546985177240999931, -82.42742953870899214, -0.05580604480424000702 ) ) ;
#45169=CARTESIAN_POINT ( 'NONE',  ( 3.402340145821570072, -86.39318692614398287, 2.471221923361245576 ) ) ;
#45172=CARTESIAN_POINT ( 'NONE',  ( -3.689614304937916422, -78.79635414669442639, -1.576161069557058703 ) ) ;
#45203=CARTESIAN_POINT ( 'NONE',  ( -0.03239454126609288276, -78.54828564506388489, -3.437034970110011134 ) ) ;
#45214=CARTESIAN_POINT ( 'NONE',  ( 3.548349909811000291, -78.43735717367049176, -4.345475359304840494E-16 ) ) ;
#45257=CARTESIAN_POINT ( 'NONE',  ( -2.881647729895999710, -82.85917773387799912, 2.140058763724999924 ) ) ;
#45286=CARTESIAN_POINT ( 'NONE',  ( 0.2052605617601000187, -85.79442953870898236, 4.167054658242999921 ) ) ;
#45316=CARTESIAN_POINT ( 'NONE',  ( 3.540977845989000006, -81.09906924513698812, -0.5875551853567000382 ) ) ;
#45327=CARTESIAN_POINT ( 'NONE',  ( 3.654181830570063738, -86.12610001270965654, -1.626946572303013872 ) ) ;
#45333=CARTESIAN_POINT ( 'NONE',  ( -0.4362624902269000016, -80.53743850270798532, -4.149668388003999731 ) ) ;
#45337=CARTESIAN_POINT ( 'NONE',  ( -1.194527725498000237, -82.00555496681198520, -3.339861958729000158 ) ) ;
#45362=CARTESIAN_POINT ( 'NONE',  ( 3.031414438364000041, -83.71250737700098909, -2.870563787844999659 ) ) ;
#45370=CARTESIAN_POINT ( 'NONE',  ( 3.851650068367000745, -78.96264283715741783, 7.703300136734033465 ) ) ;
#45390=COLOUR_RGB ( '', 0.66274510, 0.83137255, 0.94901961) ;
#45406=CARTESIAN_POINT ( 'NONE',  ( -3.964990495786999691, -81.44392549782598678, 1.156440230559000026 ) ) ;
#45425=CARTESIAN_POINT ( 'NONE',  ( 3.589195565878999794, -85.64082450217398446, 0.03758747758428000046 ) ) ;
#45429=CARTESIAN_POINT ( 'NONE',  ( -2.505364920882746205, -84.51979167730389975, 2.363564369234580020 ) ) ;
#45444=ORIENTED_EDGE ( 'NONE', *, *, #16172, .T. ) ;
#45463=CARTESIAN_POINT ( 'NONE',  ( -3.407095545933000569, -78.62148121115865251, -2.652612342793000192E-07 ) ) ;
#45466=CARTESIAN_POINT ( 'NONE',  ( -3.960893013548711483, -78.73854164604992434, -0.6456742679201270541 ) ) ;
#45493=CARTESIAN_POINT ( 'NONE',  ( 3.200957065930545742, -86.02148120184399716, 2.324951338796139133 ) ) ;
#45497=CARTESIAN_POINT ( 'NONE',  ( -0.03630073495416798190, -78.43735716284258785, -3.851479002382501182 ) ) ;
#45509=CARTESIAN_POINT ( 'NONE',  ( -0.03630051165549490200, -78.43735716284258785, 3.851479004487115443 ) ) ;
#45552=CARTESIAN_POINT ( 'NONE',  ( -2.845775103139000173, -82.99100488540000242, 2.113417919158000036 ) ) ;
#45565=CARTESIAN_POINT ( 'NONE',  ( -3.647699722740957995, -86.02148118236289065, 1.624060551956000520 ) ) ;
#45580=CARTESIAN_POINT ( 'NONE',  ( -1.831549031511999770, -85.91467953870898100, 3.748625133460000036 ) ) ;
#45612=CARTESIAN_POINT ( 'NONE',  ( -2.650649970517000131, -81.81671231080099460, 2.661846198621000248 ) ) ;
#45629=CARTESIAN_POINT ( 'NONE',  ( -3.741325830153999998, -80.29693765374598513, -1.847309861237000028 ) ) ;
#45633=CARTESIAN_POINT ( 'NONE',  ( -2.658539373363999925, -81.89157046129098205, -2.348769664634999810 ) ) ;
#45657=CARTESIAN_POINT ( 'NONE',  ( 2.266606191906000323, -85.15551236020199610, -3.506010019137000278 ) ) ;
#45665=CARTESIAN_POINT ( 'NONE',  ( 3.778552491321000240, -78.99318692756679638, -4.627392213906519702E-16 ) ) ;
#45666=ORIENTED_EDGE ( 'NONE', *, *, #23990, .F. ) ;
#45685=CARTESIAN_POINT ( 'NONE',  ( 3.914500761937000028, -78.91452044229970397, -1.429791614965258972E-15 ) ) ;
#45699=CARTESIAN_POINT ( 'NONE',  ( -4.030725660649999931, -81.56417549782598542, -0.9009740902403999829 ) ) ;
#45723=CARTESIAN_POINT ( 'NONE',  ( 1.109183238629000146, -84.43832450217399810, 3.413714993235999806 ) ) ;
#45763=CARTESIAN_POINT ( 'NONE',  ( -2.775612516598270130, -78.89270831443518261, -2.898029264795531024 ) ) ;
#45791=CARTESIAN_POINT ( 'NONE',  ( 3.922208058606372116, -86.07390000031791999, 0.4502061935818455485 ) ) ;
#45795=CARTESIAN_POINT ( 'NONE',  ( -3.587191200520567502, -78.43735717367049176, -2.026888227377177998 ) ) ;
#45806=CARTESIAN_POINT ( 'NONE',  ( -3.620804152519746300, -78.40681307385639798, -0.06825882735791576061 ) ) ;
#45823=CARTESIAN_POINT ( 'NONE',  ( 1.845937214730200226, -83.71041667982382251, -2.906560619503415044 ) ) ;
#45848=CARTESIAN_POINT ( 'NONE',  ( 3.435165100308000152, -83.95300820753398341, 0.8744208703508999925 ) ) ;
#45860=CARTESIAN_POINT ( 'NONE',  ( -5.871863728899527679, -86.07390000031791999, -4.829204525511850754 ) ) ;
#45875=CARTESIAN_POINT ( 'NONE',  ( 3.044637772279000121, -84.11719503318798274, 2.853111132616000134 ) ) ;
#45889=CARTESIAN_POINT ( 'NONE',  ( 0.000000000000000000, 0.000000000000000000, 0.000000000000000000 ) ) ;
#45914=CARTESIAN_POINT ( 'NONE',  ( 2.352936540351114658, -85.88541304819187872, 3.122209706914203409 ) ) ;
#45922=CARTESIAN_POINT ( 'NONE',  ( 3.496672618083999762, -79.64448742432209372, 2.280984592505000297 ) ) ;
#45927=CARTESIAN_POINT ( 'NONE',  ( 3.499218162531000154, -80.92330496681199747, -0.5805468162371000274 ) ) ;
#45949=CARTESIAN_POINT ( 'NONE',  ( 4.174647607761000856, -85.39601319073598518, 0.04390291789455000315 ) ) ;
#45958=CARTESIAN_POINT ( 'NONE',  ( 3.851650068366999857, -78.96264283715740362, -4.716910927661330529E-16 ) ) ;
#45974=CARTESIAN_POINT ( 'NONE',  ( 2.111723220701999804, -79.21468383341469632, -2.849946108166999892 ) ) ;
#45981=CARTESIAN_POINT ( 'NONE',  ( 3.914500761936999140, -78.91452044229970397, -2.310234204170795280 ) ) ;
#45994=CARTESIAN_POINT ( 'NONE',  ( -0.05809966506197000030, -79.52378455456849338, 3.962651287612999784 ) ) ;
#45999=CARTESIAN_POINT ( 'NONE',  ( -3.914500761937000028, -78.91452044229970397, -1.642509933758750038E-14 ) ) ;
#46018=CARTESIAN_POINT ( 'NONE',  ( -2.881626843934999904, -83.23582450217399753, 2.140085129360999705 ) ) ;
#46054=CARTESIAN_POINT ( 'NONE',  ( 3.620209227049822953, -86.25171438276198899, -1.611820994701397725 ) ) ;
#46057=CARTESIAN_POINT ( 'NONE',  ( 0.2238869547411186378, -80.58854166667283891, -4.045564205103767463 ) ) ;
#46083=CARTESIAN_POINT ( 'NONE',  ( -2.350111744379518086, -86.07390000031791999, 3.172282531658503046 ) ) ;
#46099=CARTESIAN_POINT ( 'NONE',  ( -0.03561159147831179095, -78.40681307243319509, 3.778384673934156002 ) ) ;
#46117=CARTESIAN_POINT ( 'NONE',  ( 2.064266695395271967, -82.66979168306330905, 2.715591382896376249 ) ) ;
#46142=CARTESIAN_POINT ( 'NONE',  ( 3.270705966882999860, -85.26804551122299358, 1.847660810087999872 ) ) ;
#46154=CARTESIAN_POINT ( 'NONE',  ( 3.184161977317978565, -85.88547957940599531, -1.417680250971047773 ) ) ;
#46165=CARTESIAN_POINT ( 'NONE',  ( 1.298082172566151549, -82.74687498353479498, 3.823617033396692122 ) ) ;
#46168=CARTESIAN_POINT ( 'NONE',  ( 4.043204716307999824, -83.99067953870898862, 1.029097049655000040 ) ) ;
#46198=CARTESIAN_POINT ( 'NONE',  ( -2.442701056171530105, -81.51354165288981335, 2.427965435584034104 ) ) ;
#46210=CARTESIAN_POINT ( 'NONE',  ( 3.326798747144231516, -85.83867307182441664, 1.964420495601435057 ) ) ;
#46215=CARTESIAN_POINT ( 'NONE',  ( 2.485497987250000040, -79.28373615087838289, -3.354386240666999974 ) ) ;
#46221=CARTESIAN_POINT ( 'NONE',  ( 0.5658835715479000328, -82.12580496681198383, -3.501612269639000186 ) ) ;
#46242=CARTESIAN_POINT ( 'NONE',  ( -3.722292034697000318, -82.86303720588698241, 0.5058778948779999451 ) ) ;
#46250=CARTESIAN_POINT ( 'NONE',  ( -3.778552491321031770, -78.99318692756679638, 7.557104982642018243 ) ) ;
#46266=CARTESIAN_POINT ( 'NONE',  ( -3.238101123710000362, -78.61343171100860161, 1.037346680369000129 ) ) ;
#46287=CARTESIAN_POINT ( 'NONE',  ( -3.095242434087999595, -81.68442549782599826, -2.734588626640999998 ) ) ;
#46309=CARTESIAN_POINT ( 'NONE',  ( -3.315791941328000370, -83.23582450217399753, 2.462524611965999810 ) ) ;
#46362=COLOUR_RGB ( '', 0.66274510, 0.83137255, 0.94901961) ;
#46374=CARTESIAN_POINT ( 'NONE',  ( 1.441729589604688666, -85.80681307385599155, 3.322092378136410229 ) ) ;
#46391=CARTESIAN_POINT ( 'NONE',  ( 3.437187628289000596, -78.54828564506389910, 2.028536598677995073 ) ) ;
#46426=CARTESIAN_POINT ( 'NONE',  ( 4.160588626246000565, -79.48657046129088144, 0.3099153621731999819 ) ) ;
#46432=CARTESIAN_POINT ( 'NONE',  ( 3.546986249139000069, -82.46507062100899077, -0.05580368944623999988 ) ) ;
#46455=CARTESIAN_POINT ( 'NONE',  ( 0.5575394168558645003, -85.79166668297689569, 3.974010456388519685 ) ) ;
#46458=CARTESIAN_POINT ( 'NONE',  ( 4.171886442359999947, -85.43367953870898646, 0.04368964723657999677 ) ) ;
#46490=CARTESIAN_POINT ( 'NONE',  ( -1.031249463432703406, -81.39791665334102788, 3.286199682045575887 ) ) ;
#46503=CARTESIAN_POINT ( 'NONE',  ( -3.654181822837000215, -86.09999999943198645, 1.626946589673999854 ) ) ;
#46508=CARTESIAN_POINT ( 'NONE',  ( 2.484104553507999746, -79.21468383341469632, -3.352505685947999581 ) ) ;
#46539=CARTESIAN_POINT ( 'NONE',  ( 0.2829448620830999905, -82.50228596008699355, 3.745841164862000028 ) ) ;
#46559=CARTESIAN_POINT ( 'NONE',  ( 3.344859295621999795, -81.01844020063299467, 1.180460146152999990 ) ) ;
#46581=CARTESIAN_POINT ( 'NONE',  ( 1.861773376307000127, -79.40353455456848053, 3.498539798548999880 ) ) ;
#46586=CARTESIAN_POINT ( 'NONE',  ( -3.485499217011999828, -78.91452042059380290, -1.462502484024984119E-14 ) ) ;
#46601=CARTESIAN_POINT ( 'NONE',  ( -1.649098995971000070, -86.23821544543099549, 3.375205270238999411 ) ) ;
#46609=CARTESIAN_POINT ( 'NONE',  ( -4.134112256334000257, -83.18657311260999165, 0.5618462995190999232 ) ) ;
#46610=CARTESIAN_POINT ( 'NONE',  ( 3.621447497675000182, -78.99318692614357929, 0.000000000000000000 ) ) ;
#46615=CARTESIAN_POINT ( 'NONE',  ( 2.732978708635966925, -78.98334398719974558, -2.638764568140384181 ) ) ;
#46667=CARTESIAN_POINT ( 'NONE',  ( 3.184161977317979897, -85.88547957940599531, -1.417680250971043998 ) ) ;
#46731=CARTESIAN_POINT ( 'NONE',  ( -1.489945701322999971, -84.98406384713199202, -3.218948819672999839 ) ) ;
#46742=CARTESIAN_POINT ( 'NONE',  ( -3.576074390005993475, -85.88547955769999476, 1.592170899228015024 ) ) ;
#46755=CARTESIAN_POINT ( 'NONE',  ( 2.217082214997963874, -85.21354167675372082, -3.391499533005605915 ) ) ;
#46829=CARTESIAN_POINT ( 'NONE',  ( 3.962859227717999921, -85.14779509595699380, 0.04167563340643000436 ) ) ;
#46848=CARTESIAN_POINT ( 'NONE',  ( 3.440741810271999768, -82.41509632510098982, -0.2267889765191999918 ) ) ;
#46872=CARTESIAN_POINT ( 'NONE',  ( -1.778395558963000056, -79.76042549782599167, 3.117859321502000292 ) ) ;
#46892=CARTESIAN_POINT ( 'NONE',  ( 3.308763867269000070, -85.63696544543098810, -1.778607282991000016 ) ) ;
#46901=CARTESIAN_POINT ( 'NONE',  ( 3.044259723400999817, -84.14857643474398685, 2.852899930898999958 ) ) ;
#46907=CARTESIAN_POINT ( 'NONE',  ( 2.589388593803659600, -78.97650220697799739, -2.803363233735876481 ) ) ;
#46927=CARTESIAN_POINT ( 'NONE',  ( 1.974456364585935431, -78.69999999999998863, -3.418760544058775164 ) ) ;
#46934=EDGE_CURVE ( 'NONE', #3531, #9865, #50212, .T. ) ;
#46937=CARTESIAN_POINT ( 'NONE',  ( 0.7265058034139308951, -81.28229167440642300, 3.986460672241819214 ) ) ;
#46975=CARTESIAN_POINT ( 'NONE',  ( 3.400000000000109601, -78.67390000031815589, 2.006589450846672840 ) ) ;
#46998=CARTESIAN_POINT ( 'NONE',  ( 1.353569424327082826, -86.12609999968211127, 3.118950113984548800 ) ) ;
#47017=CARTESIAN_POINT ( 'NONE',  ( -3.315867686165999917, -86.07743221058099437, 0.9362964062973999635 ) ) ;
#47041=CARTESIAN_POINT ( 'NONE',  ( 3.973714814374760262, -85.48333334632451397, 0.5577315370174421583 ) ) ;
#47089=CARTESIAN_POINT ( 'NONE',  ( 2.570900958241000289, -82.21467895096598966, -3.285915534916000080 ) ) ;
#47123=CARTESIAN_POINT ( 'NONE',  ( -3.193873729499000280, -84.54654301962300167, -2.346307860450000060 ) ) ;
#47140=CARTESIAN_POINT ( 'NONE',  ( 3.499622226389000001, -80.89192428167199012, -0.5806930388547999478 ) ) ;
#47164=CARTESIAN_POINT ( 'NONE',  ( 2.387772752419999645, -80.96292549782599224, 2.679977387145999757 ) ) ;
#47184=CARTESIAN_POINT ( 'NONE',  ( -3.926971269994000480, -83.47246544543099844, 0.5337392329503000132 ) ) ;
#47198=CARTESIAN_POINT ( 'NONE',  ( 0.8262517789086295528, -78.91601566066201201, -3.392806836647565216 ) ) ;
#47252=CARTESIAN_POINT ( 'NONE',  ( 3.399999999999979927, -78.70000000000000284, -2.006589542798784986 ) ) ;
#47306=CARTESIAN_POINT ( 'NONE',  ( 3.124342397322000586, -85.34481509293298984, -1.679301754202999986 ) ) ;
#47329=ADVANCED_FACE ( 'NONE', ( #38108 ), #5631, .F. ) ;
#47333=CARTESIAN_POINT ( 'NONE',  ( 3.991454038972588325, -85.42552084570225190, -0.4111825025862656524 ) ) ;
#47430=CARTESIAN_POINT ( 'NONE',  ( 0.5658688935430999933, -82.10069402096399926, -3.501615713813999609 ) ) ;
#47445=CARTESIAN_POINT ( 'NONE',  ( 2.389814808304494775, -86.36264282632902223, -3.356337498275545173 ) ) ;
#47458=CARTESIAN_POINT ( 'NONE',  ( 3.540989726729000253, -80.72242549782599497, -0.5874770353539999768 ) ) ;
#47464=CARTESIAN_POINT ( 'NONE',  ( -2.265198070799999908, -84.54699735065199206, 2.726507195704999997 ) ) ;
#47479=CARTESIAN_POINT ( 'NONE',  ( 3.654181830570000233, -86.09999999999999432, -1.626946572303000105 ) ) ;
#47490=CARTESIAN_POINT ( 'NONE',  ( 0.7962146461373009743, -78.91497093336721491, -3.398928107770800455 ) ) ;
#47520=CARTESIAN_POINT ( 'NONE',  ( 3.696996952934347824, -81.05104167182884112, 1.659147455894784295 ) ) ;
#47522=CARTESIAN_POINT ( 'NONE',  ( 1.620786422037999941, -80.68907046129099569, -3.844424077763000103 ) ) ;
#47604=CARTESIAN_POINT ( 'NONE',  ( -3.517172751179999945, -84.74356301659899771, -0.4594186973889000103 ) ) ;
#47624=CARTESIAN_POINT ( 'NONE',  ( -0.03769889196559850220, -78.67389998729011324, -3.999822345247525224 ) ) ;
#47628=CARTESIAN_POINT ( 'NONE',  ( -3.961164824809206841, -84.75104167177519798, -0.8542422772179285584 ) ) ;
#47644=( NAMED_UNIT ( * ) SI_UNIT ( $, .STERADIAN. ) SOLID_ANGLE_UNIT ( ) );
#47695=CARTESIAN_POINT ( 'NONE',  ( -2.398287285837117810, -78.69999999999998863, 3.977573602256943008 ) ) ;
#47717=CARTESIAN_POINT ( 'NONE',  ( -1.297011388420000078, -79.17506245343760440, -3.346857603051000218 ) ) ;
#47730=CARTESIAN_POINT ( 'NONE',  ( -3.929996950241438913, -86.09999999999996589, -0.3761983785358135046 ) ) ;
#47741=CARTESIAN_POINT ( 'NONE',  ( 3.146181864693999852, -79.28328455456849611, 2.052535432853999975 ) ) ;
#47745=CARTESIAN_POINT ( 'NONE',  ( -1.489081774397999824, -85.02799735065198661, -3.216768448715999984 ) ) ;
#47764=CARTESIAN_POINT ( 'NONE',  ( -3.976122264605000733, -86.18656799980000471, 0.4345342749550000216 ) ) ;
#47772=CARTESIAN_POINT ( 'NONE',  ( 2.428538520610905138, -78.97637148647436334, -2.635006473292730966 ) ) ;
#47791=CARTESIAN_POINT ( 'NONE',  ( -3.474812103689401965, -78.85171435493610659, -1.963390115445670991 ) ) ;
#47799=CARTESIAN_POINT ( 'NONE',  ( 3.758258207583866195, -80.85833333634744235, -1.512211360522490722 ) ) ;
#47803=CARTESIAN_POINT ( 'NONE',  ( 3.793820962314999878, -79.36005496681158888, -1.736947023676999935 ) ) ;
#47908=CARTESIAN_POINT ( 'NONE',  ( -0.03689308533088261205, -78.48547955770028750, -3.914326904521404860 ) ) ;
#47952=CARTESIAN_POINT ( 'NONE',  ( -3.684198380124665828, -86.09999999999978115, 1.557781209248828347 ) ) ;
#48006=CARTESIAN_POINT ( 'NONE',  ( 3.342652169347999802, -81.08749251809699388, 1.179681212160999859 ) ) ;
#48020=CARTESIAN_POINT ( 'NONE',  ( 3.308356911591940008, -86.39318692614399708, -1.472975398279134485 ) ) ;
#48031=CARTESIAN_POINT ( 'NONE',  ( -3.453033859651000181, -78.47775883115959061, 0.4993677312671000457 ) ) ;
#48036=CARTESIAN_POINT ( 'NONE',  ( -0.6682991597444000176, -84.35769503318799423, 3.483523875034000294 ) ) ;
#48057=CARTESIAN_POINT ( 'NONE',  ( 2.284771741974000125, -82.63025363959900460, 3.494189356575999827 ) ) ;
#48064=CARTESIAN_POINT ( 'NONE',  ( -3.671083419894561217, -78.75032998289347574, -1.629121246791012778 ) ) ;
#48081=CARTESIAN_POINT ( 'NONE',  ( 3.778552491320999795, -78.99318692756679638, -2.230001151765018008 ) ) ;
#48114=EDGE_CURVE ( 'NONE', #36712, #3531, #55930, .T. ) ;
#48173=CARTESIAN_POINT ( 'NONE',  ( 1.925977698187999909, -85.23083017214499080, -2.979122324201999739 ) ) ;
#48184=CARTESIAN_POINT ( 'NONE',  ( -5.871863728900494905, -86.10000000000019327, -4.829204525511367585 ) ) ;
#48201=ORIENTED_EDGE ( 'NONE', *, *, #14831, .F. ) ;
#48215=SHAPE_REPRESENTATION_RELATIONSHIP ( 'NONE' , 'NONE' ,  #52046, #44024 ) ;
#48267=CARTESIAN_POINT ( 'NONE',  ( 3.270789807158999807, -85.87746544543099958, 1.847510159297000021 ) ) ;
#48290=CARTESIAN_POINT ( 'NONE',  ( -3.478405327321000051, -78.80273445295348722, -0.6821537367355999804 ) ) ;
#48300=CARTESIAN_POINT ( 'NONE',  ( -3.929996950240798093, -86.12609999968209706, -0.3761983785355073051 ) ) ;
#48308=CARTESIAN_POINT ( 'NONE',  ( 2.442089561480999649, -82.53821485768798993, -3.121279332836000009 ) ) ;
#48312=CARTESIAN_POINT ( 'NONE',  ( 2.211827365938999979, -82.04517549782597996, -2.826962668278000024 ) ) ;
#48314=CARTESIAN_POINT ( 'NONE',  ( -3.514734140608999802, -83.15519503318799366, 0.4777095056862999400 ) ) ;
#48319=ADVANCED_FACE ( 'NONE', ( #10825 ), #9939, .T. ) ;
#48334=CARTESIAN_POINT ( 'NONE',  ( 2.265335474502999880, -85.22456467766599530, -3.504044460248999737 ) ) ;
#48341=CARTESIAN_POINT ( 'NONE',  ( 3.699999999670000150, -79.00321104920828930, -4.531193156441073745E-16 ) ) ;
#48352=CARTESIAN_POINT ( 'NONE',  ( -3.308356910955999819, -86.39318692608898687, 1.472975399707999955 ) ) ;
#48358=CARTESIAN_POINT ( 'NONE',  ( -3.587191200520567502, -78.96264282632948550, -2.026888227377177998 ) ) ;
#48370=CARTESIAN_POINT ( 'NONE',  ( 3.837977402148000206, -82.36630496681199531, -1.636926709757999809 ) ) ;
#48429=CARTESIAN_POINT ( 'NONE',  ( -2.611770760766960464, -86.39318692756700102, 3.525481195052141192 ) ) ;
#48448=CARTESIAN_POINT ( 'NONE',  ( -3.126681305892000218, -81.85392767752199461, -2.762320878000999791 ) ) ;
#48462=CARTESIAN_POINT ( 'NONE',  ( 4.443227334435270848, -85.83735716284300565, 0.5100107989082148796 ) ) ;
#48508=CARTESIAN_POINT ( 'NONE',  ( -2.764837346328296253, -86.12610001270964233, 3.732097096069109554 ) ) ;
#48542=CARTESIAN_POINT ( 'NONE',  ( 3.685513155162999599, -82.55394503318800048, 1.956341549149999581 ) ) ;
#48575=CARTESIAN_POINT ( 'NONE',  ( -2.751373484785000212, -79.05481202895639115, -2.305178922514000028 ) ) ;
#48585=CARTESIAN_POINT ( 'NONE',  ( -3.318865696948021693, -86.31452042059397911, -2.316308510770335172 ) ) ;
#48586=CARTESIAN_POINT ( 'NONE',  ( 2.090460633792530221, -85.88583664465505763, 2.794791628714064391 ) ) ;
#48592=CARTESIAN_POINT ( 'NONE',  ( 0.5517604069303000403, -79.29531287791878924, -4.093176084825000061 ) ) ;
#48595=CARTESIAN_POINT ( 'NONE',  ( -1.281543785372999844, -78.99930496681159298, -3.307439830080999510 ) ) ;
#48599=CARTESIAN_POINT ( 'NONE',  ( 2.573795024414000210, -83.82549735065198604, -2.437322908517999931 ) ) ;
#48618=CARTESIAN_POINT ( 'NONE',  ( 3.675289024537000238, -85.34481509293298984, -1.975429873306999928 ) ) ;
#48624=FACE_OUTER_BOUND ( 'NONE', #17911, .T. ) ;
#48645=CARTESIAN_POINT ( 'NONE',  ( -0.03204405817075896279, -78.72609999968184979, -3.399848993460421465 ) ) ;
#48654=CARTESIAN_POINT ( 'NONE',  ( -4.007886309445000350, -81.57575264934799009, 1.168951343685000088 ) ) ;
#48691=CARTESIAN_POINT ( 'NONE',  ( -1.490242064849000014, -84.95267953870899191, -3.219274950222999809 ) ) ;
#48716=CARTESIAN_POINT ( 'NONE',  ( 3.451879464910831974, -86.39318692756698681, -1.536875756006378824 ) ) ;
#48734=CARTESIAN_POINT ( 'NONE',  ( -1.405194841723999888, -81.98044359648298496, -3.928806027564999859 ) ) ;
#48748=CARTESIAN_POINT ( 'NONE',  ( -2.739132899391135911, -85.94828561723799965, 3.697400121254065919 ) ) ;
#48829=CARTESIAN_POINT ( 'NONE',  ( -0.7865880339533001253, -84.42674735065199343, 4.100107199207999820 ) ) ;
#48857=CARTESIAN_POINT ( 'NONE',  ( 0.6938652518923514867, -79.12395832888063296, -3.339787257827266043 ) ) ;
#48860=CARTESIAN_POINT ( 'NONE',  ( -3.617892441770000023, -78.93070212325169166, 1.159015290449999958 ) ) ;
#48872=CARTESIAN_POINT ( 'NONE',  ( 2.544856321172368485, -86.39318692756700102, -3.574083091624765007 ) ) ;
#48878=CARTESIAN_POINT ( 'NONE',  ( 1.539486242883999934, -80.97495933943199020, -3.651845052344000031 ) ) ;
#48881=CARTESIAN_POINT ( 'NONE',  ( -0.3707676657765999750, -80.56255496681198736, -3.527618700040000110 ) ) ;
#48906=CARTESIAN_POINT ( 'NONE',  ( 3.674917764513000229, -85.35108058741198533, -1.975230324880000277 ) ) ;
#48912=CARTESIAN_POINT ( 'NONE',  ( 0.8935345625127607549, -78.91502747134597939, -3.805630735094382988 ) ) ;
#48927=ORIENTED_EDGE ( 'NONE', *, *, #16172, .F. ) ;
#48929=CARTESIAN_POINT ( 'NONE',  ( 3.548349909811000735, -78.96264282632948550, -1.307818870560639724E-15 ) ) ;
#48939=CARTESIAN_POINT ( 'NONE',  ( -4.168307155918999918, -80.20180496681199145, 0.1878237294363000187 ) ) ;
#48978=CARTESIAN_POINT ( 'NONE',  ( 3.399999999999999911, -78.69999999999998863, 0.000000000000000000 ) ) ;
#48979=CARTESIAN_POINT ( 'NONE',  ( 1.078548557676999975, -83.62992953870899271, -3.379539263167000041 ) ) ;
#49001=CARTESIAN_POINT ( 'NONE',  ( 3.518657424384828758, -86.36264283715698298, -1.566607219110386140 ) ) ;
#49036=CARTESIAN_POINT ( 'NONE',  ( 1.592434616855321838, -86.07389998728979208, 3.669353075276816423 ) ) ;
#49042=CARTESIAN_POINT ( 'NONE',  ( -2.089807409446279074, -78.48547957940618858, -3.465957297018673611 ) ) ;
#49053=CARTESIAN_POINT ( 'NONE',  ( -2.394032993764998452, -78.62148118236264338, 3.970517833774876326 ) ) ;
#49090=ORIENTED_EDGE ( 'NONE', *, *, #25505, .F. ) ;
#49117=CARTESIAN_POINT ( 'NONE',  ( 3.807751541924000005, -82.42258068398498949, -1.403160745109000018 ) ) ;
#49145=CARTESIAN_POINT ( 'NONE',  ( 2.193927587745784891, -79.23958332842951791, -2.654379237460795071 ) ) ;
#49148=CARTESIAN_POINT ( 'NONE',  ( 3.319279290813000216, -79.89270551910098561, 2.165265596042999618 ) ) ;
#49159=CARTESIAN_POINT ( 'NONE',  ( 3.576074390005934855, -86.31452044229999387, -1.592170899228145586 ) ) ;
#49165=CARTESIAN_POINT ( 'NONE',  ( -3.381175124639000273, -80.37370721702599496, 2.067279602469000110 ) ) ;
#49169=CARTESIAN_POINT ( 'NONE',  ( -2.656469456053000222, -81.81625264934800157, -2.346940931520999918 ) ) ;
#49192=CARTESIAN_POINT ( 'NONE',  ( 3.614576214518000263, -82.06136777077499289, -1.331977498170999974 ) ) ;
#49200=CARTESIAN_POINT ( 'NONE',  ( 1.792077181278651565, -78.94486059145259560, -3.438065020606960065 ) ) ;
#49231=CARTESIAN_POINT ( 'NONE',  ( 4.047000891220999819, -82.44647163347798369, -0.2667513232904999421 ) ) ;
#49238=CARTESIAN_POINT ( 'NONE',  ( -0.6684780613089000845, -84.38907726527799014, 3.483919782562000300 ) ) ;
#49253=CARTESIAN_POINT ( 'NONE',  ( 1.142103019466000013, -83.95346544543099299, -3.578681710149999695 ) ) ;
#49257=CARTESIAN_POINT ( 'NONE',  ( -0.07384301375007251700, -85.83020833989095877, 3.410305331954705643 ) ) ;
#49297=CARTESIAN_POINT ( 'NONE',  ( 4.515731304085743858, -86.31452044230000809, 0.5183330846476985609 ) ) ;
#49339=CARTESIAN_POINT ( 'NONE',  ( -3.661088936265289195, -78.40681307385639798, -2.068643027229794651 ) ) ;
#49391=CARTESIAN_POINT ( 'NONE',  ( 3.756302695449999618, -85.14779509595699380, 0.03950336994162999965 ) ) ;
#49419=CARTESIAN_POINT ( 'NONE',  ( -4.095422038743000925, -84.91932450217399264, -0.5348100902707000337 ) ) ;
#49453=CARTESIAN_POINT ( 'NONE',  ( -0.05492852729254000393, -80.13320636806399477, 3.756108806030999947 ) ) ;
#49473=CARTESIAN_POINT ( 'NONE',  ( -1.194669669092999875, -82.01182046129099490, -3.340258828557999493 ) ) ;
#49495=CARTESIAN_POINT ( 'NONE',  ( 3.637992502009999463, -85.14393562394799631, -1.955383377840000048 ) ) ;
#49535=CARTESIAN_POINT ( 'NONE',  ( 2.572610278691000119, -82.17700264934799748, -3.288083568311999993 ) ) ;
#49542=CARTESIAN_POINT ( 'NONE',  ( 1.096138950756000208, -84.26882685001099560, 3.373876015865000078 ) ) ;
#49559=CARTESIAN_POINT ( 'NONE',  ( 3.426173589824000221, -82.67079877876498983, -1.262548838661999850 ) ) ;
#49564=CARTESIAN_POINT ( 'NONE',  ( 2.052407343088218816, -84.17291667838408387, 2.765357313056269639 ) ) ;
#49599=CARTESIAN_POINT ( 'NONE',  ( 1.441729589605054818, -86.39318692614399708, 3.322092378136251689 ) ) ;
#49603=CARTESIAN_POINT ( 'NONE',  ( 3.403319483155256009, -79.31666665249466064, -2.125768741672802609 ) ) ;
#49633=CARTESIAN_POINT ( 'NONE',  ( -2.038544480927684255, -78.67390000031812747, -3.380937442862520292 ) ) ;
#49645=CARTESIAN_POINT ( 'NONE',  ( 2.103056013418682646, -78.40681307385641219, 3.641429823450980763 ) ) ;
#49687=CARTESIAN_POINT ( 'NONE',  ( 1.939901737288000083, -82.63025363959900460, 2.966766385765999825 ) ) ;
#49717=CARTESIAN_POINT ( 'NONE',  ( -3.935749424346000058, -86.36232450217399048, 0.4303395207149999790 ) ) ;
#49748=CARTESIAN_POINT ( 'NONE',  ( -1.036641179982999983, -81.69646188631999451, 3.610643376931000237 ) ) ;
#49762=CARTESIAN_POINT ( 'NONE',  ( 1.826169837773488069, -85.89642030789714511, 2.963197235734413848 ) ) ;
#49767=CARTESIAN_POINT ( 'NONE',  ( -1.507728061743999870, -78.97418298445228402, -3.890598935239999889 ) ) ;
#49793=CARTESIAN_POINT ( 'NONE',  ( -2.639441014136000074, -84.30218271708000088, 3.176769522894000275 ) ) ;
#49831=CARTESIAN_POINT ( 'NONE',  ( 1.940281527255000027, -79.51992549782627862, 3.646067899498000031 ) ) ;
#49855=CARTESIAN_POINT ( 'NONE',  ( -1.575735042988000156, -86.12182450217399321, 3.225051518789999960 ) ) ;
#49888=ORIENTED_EDGE ( 'NONE', *, *, #20004, .F. ) ;
#49925=CARTESIAN_POINT ( 'NONE',  ( 3.140027144888980271, -85.94828564506399005, -1.398030157552043740 ) ) ;
#49928=CARTESIAN_POINT ( 'NONE',  ( -3.740501297249256396, -78.39678895079168797, -2.113513782812399544 ) ) ;
#49940=CARTESIAN_POINT ( 'NONE',  ( 3.778552491321000240, -78.40681307243319509, -4.627392213906519702E-16 ) ) ;
#49981=CARTESIAN_POINT ( 'NONE',  ( 3.478467325896999807, -83.82118105601298907, 0.8854434467574999745 ) ) ;
#49994=CARTESIAN_POINT ( 'NONE',  ( 3.241578942234978111, -85.83735717367099483, -1.443243930775048645 ) ) ;
#50005=CARTESIAN_POINT ( 'NONE',  ( -2.651434666701682374, -82.99739581956490042, 3.011249467861417450 ) ) ;
#50009=CARTESIAN_POINT ( 'NONE',  ( 0.3142732060366000280, -82.78817953870900226, 4.160263707816999279 ) ) ;
#50037=CARTESIAN_POINT ( 'NONE',  ( 2.211821066349999754, -82.42182391443098766, -2.826968957741000210 ) ) ;
#50055=CARTESIAN_POINT ( 'NONE',  ( 4.049271546212999340, -82.49041413704399872, -0.2668988840931000306 ) ) ;
#50059=CARTESIAN_POINT ( 'NONE',  ( -2.719119925748999744, -78.88532046129088826, -2.278397777311000016 ) ) ;
#50085=CARTESIAN_POINT ( 'NONE',  ( 3.962535311936000060, -82.14153471428599573, -0.06234140039890999352 ) ) ;
#50111=CARTESIAN_POINT ( 'NONE',  ( -4.036611966185642331, -78.77851881763733388, -2.280826645528176488 ) ) ;
#50125=CARTESIAN_POINT ( 'NONE',  ( -1.093701836234999947, -81.08703455456799247, 3.809172760610000097 ) ) ;
#50146=( BOUNDED_SURFACE ( )  B_SPLINE_SURFACE ( 3, 3, ( 
 ( #8291, #26002, #40468, #21582, #53169, #44604, #8583 ),
 ( #44027, #3864, #39587, #49036, #60, #3578, #21864 ),
 ( #4157, #57592, #40758, #26571, #58178, #39871, #352 ),
 ( #44308, #48748, #18035, #22157, #17743, #17152, #35138 ),
 ( #57884, #17440, #35426, #36028, #35731, #12718, #34854 ),
 ( #12437, #31584, #8005, #53456, #26295, #48462, #54054 ),
 ( #54348, #51091, #18624, #50798, #928, #14750, #15052 ),
 ( #55504, #36615, #28038, #27455, #13887, #6194, #14173 ),
 ( #32750, #36901, #5898, #46374, #19488, #32170, #27744 ),
 ( #10640, #55207, #5608, #36324, #37481, #23908, #54914 ),
 ( #24207, #41926, #23038, #1498, #33044, #1210, #46667 ),
 ( #14466, #28622, #50502, #42225, #18331, #31882, #49925 ),
 ( #54637, #28322, #9470, #10343, #45493, #5036, #41054 ),
 ( #23334, #46083, #641, #50209, #9759, #45791, #5327 ),
 ( #41344, #18908, #32457, #10056, #23617, #41630, #19202 ) ),
 .UNSPECIFIED., .F., .F., .T. ) 
 B_SPLINE_SURFACE_WITH_KNOTS ( ( 4, 1, 1, 1, 1, 1, 1, 1, 1, 1, 1, 1, 4 ),
 ( 4, 3, 4 ),
 ( 0.009836358966825000175, 0.09153389967814999639, 0.1732269073519000224, 0.2549246240467999969, 0.3366128957582000258, 0.4183102327763000283, 0.5000049915180999616, 0.5816997512343000665, 0.6633971206824998967, 0.7450853986059999823, 0.8267830947368000061, 0.9084761241232000017, 0.9901736480482069558 ),
 ( 0.000000000000000000, 0.5000000000000000000, 1.000000000000000000 ),
 .UNSPECIFIED. ) 
 GEOMETRIC_REPRESENTATION_ITEM ( )  RATIONAL_B_SPLINE_SURFACE ( (
 ( 1.000000000000000000, 0.8025111637939374987, 0.8025111637939374987, 1.000000000000000000, 0.8025111637939374987, 0.8025111637939374987, 1.000000000000000000),
 ( 1.000000000000000000, 0.8025111637939374987, 0.8025111637939374987, 1.000000000000000000, 0.8025111637939374987, 0.8025111637939374987, 1.000000000000000000),
 ( 1.000000000000000000, 0.8025111637939374987, 0.8025111637939374987, 1.000000000000000000, 0.8025111637939374987, 0.8025111637939374987, 1.000000000000000000),
 ( 1.000000000000000000, 0.8025111637939374987, 0.8025111637939374987, 1.000000000000000000, 0.8025111637939374987, 0.8025111637939374987, 1.000000000000000000),
 ( 1.000000000000000000, 0.8025111637939374987, 0.8025111637939374987, 1.000000000000000000, 0.8025111637939374987, 0.8025111637939374987, 1.000000000000000000),
 ( 1.000000000000000000, 0.8025111637939374987, 0.8025111637939374987, 1.000000000000000000, 0.8025111637939374987, 0.8025111637939374987, 1.000000000000000000),
 ( 1.000000000000000000, 0.8025111637939374987, 0.8025111637939374987, 1.000000000000000000, 0.8025111637939374987, 0.8025111637939374987, 1.000000000000000000),
 ( 1.000000000000000000, 0.8025111637939374987, 0.8025111637939374987, 1.000000000000000000, 0.8025111637939374987, 0.8025111637939374987, 1.000000000000000000),
 ( 1.000000000000000000, 0.8025111637939374987, 0.8025111637939374987, 1.000000000000000000, 0.8025111637939374987, 0.8025111637939374987, 1.000000000000000000),
 ( 1.000000000000000000, 0.8025111637939374987, 0.8025111637939374987, 1.000000000000000000, 0.8025111637939374987, 0.8025111637939374987, 1.000000000000000000),
 ( 1.000000000000000000, 0.8025111637939374987, 0.8025111637939374987, 1.000000000000000000, 0.8025111637939374987, 0.8025111637939374987, 1.000000000000000000),
 ( 1.000000000000000000, 0.8025111637939374987, 0.8025111637939374987, 1.000000000000000000, 0.8025111637939374987, 0.8025111637939374987, 1.000000000000000000),
 ( 1.000000000000000000, 0.8025111637939374987, 0.8025111637939374987, 1.000000000000000000, 0.8025111637939374987, 0.8025111637939374987, 1.000000000000000000),
 ( 1.000000000000000000, 0.8025111637939374987, 0.8025111637939374987, 1.000000000000000000, 0.8025111637939374987, 0.8025111637939374987, 1.000000000000000000),
 ( 1.000000000000000000, 0.8025111637939374987, 0.8025111637939374987, 1.000000000000000000, 0.8025111637939374987, 0.8025111637939374987, 1.000000000000000000) ) ) 
 REPRESENTATION_ITEM ( '' )  SURFACE ( )  );
#50148=CARTESIAN_POINT ( 'NONE',  ( -3.420407972780000083, -86.36232450217399048, 0.3739914737839999948 ) ) ;
#50151=CARTESIAN_POINT ( 'NONE',  ( -2.535599314688579575, -86.02291667262494457, 2.329467182686746352 ) ) ;
#50185=CARTESIAN_POINT ( 'NONE',  ( 3.716963287104071867, -79.54791665507261200, 1.610115688683979585 ) ) ;
#50209=CARTESIAN_POINT ( 'NONE',  ( 1.353569424326575898, -86.07390000031791999, 3.118950113984900518 ) ) ;
#50212=CIRCLE ( 'NONE', #6834, 4.000000000000000000 ) ;
#50213=CARTESIAN_POINT ( 'NONE',  ( -3.819913647775994292, -78.40681307243319509, -2.158384532486305574 ) ) ;
#50227=CARTESIAN_POINT ( 'NONE',  ( 2.060606600077061756, -78.43735717367052018, 3.567928899679150057 ) ) ;
#50246=CARTESIAN_POINT ( 'NONE',  ( 0.5623895165579090305, -82.78541668270349874, 3.364310149638601199 ) ) ;
#50270=CARTESIAN_POINT ( 'NONE',  ( 3.273752094640999921, -82.17775871403298993, -1.206383228866000135 ) ) ;
#50281=CARTESIAN_POINT ( 'NONE',  ( -5.936087459992990922, -85.94828564506399005, -4.882024132225906143 ) ) ;
#50296=CARTESIAN_POINT ( 'NONE',  ( 4.171543465321999378, -82.42742953870899214, -0.06563245401257999934 ) ) ;
#50324=CARTESIAN_POINT ( 'NONE',  ( 0.05530789208431366455, -81.32083332030849476, 3.442645786192767510 ) ) ;
#50337=CARTESIAN_POINT ( 'NONE',  ( 3.513385375869528371, -85.82276001101435270, 1.485411387532208582 ) ) ;
#50343=CARTESIAN_POINT ( 'NONE',  ( -0.06104599752768998661, -79.88498827328399443, 4.174432124594999571 ) ) ;
#50374=CARTESIAN_POINT ( 'NONE',  ( 2.998969658540000083, -83.58068022547898579, -2.839840568714000035 ) ) ;
#50382=CARTESIAN_POINT ( 'NONE',  ( -3.778552491321000240, -78.99318692756679638, -1.585466545969598184E-14 ) ) ;
#50387=( NAMED_UNIT ( * ) PLANE_ANGLE_UNIT ( ) SI_UNIT ( $, .RADIAN. ) );
#50395=CARTESIAN_POINT ( 'NONE',  ( -0.05187192650483000295, -79.80967046134098553, 3.547093095958999687 ) ) ;
#50414=CARTESIAN_POINT ( 'NONE',  ( 3.894733971054000321, -80.84267549782599360, 1.374609327336000053 ) ) ;
#50437=CARTESIAN_POINT ( 'NONE',  ( -0.6762769136191999486, -84.55857450217399673, 3.525108090257000004 ) ) ;
#50440=CARTESIAN_POINT ( 'NONE',  ( 3.242204976606303912, -85.36770834133103847, -1.159067530704637194 ) ) ;
#50477=CARTESIAN_POINT ( 'NONE',  ( -1.685420276471391254, -80.47291666538409061, -3.684289950626761012 ) ) ;
#50487=CARTESIAN_POINT ( 'NONE',  ( -3.647699722740957995, -86.02148118236289065, 1.624060551956000520 ) ) ;
#50502=CARTESIAN_POINT ( 'NONE',  ( -0.4924802140958408625, -85.94828564506400426, 3.960641768741219870 ) ) ;
#50537=CARTESIAN_POINT ( 'NONE',  ( -3.418851969608866170, -83.17083334817002083, 0.4151850122235886120 ) ) ;
#50555=CARTESIAN_POINT ( 'NONE',  ( 3.837589708125999977, -82.37257046129099081, -1.636761355292999820 ) ) ;
#50559=CARTESIAN_POINT ( 'NONE',  ( 0.2634948857500000186, -84.78704385015599598, -3.747257769858999943 ) ) ;
#50571=CARTESIAN_POINT ( 'NONE',  ( 0.3439668297849150513, -85.94828564506399005, -7.678084447329936779 ) ) ;
#50589=CARTESIAN_POINT ( 'NONE',  ( -4.134104809361999422, -83.14892953870898396, 0.5618920481403999467 ) ) ;
#50618=CARTESIAN_POINT ( 'NONE',  ( 3.433336739787663294, -79.43229166101083649, -0.2598626512273453648 ) ) ;
#50631=CARTESIAN_POINT ( 'NONE',  ( 0.1290952183515442220, -85.95735607754586738, 3.973009594863323279 ) ) ;
#50639=CARTESIAN_POINT ( 'NONE',  ( 2.572602951542000138, -82.28999676290898435, -3.288090883683000065 ) ) ;
#50644=CARTESIAN_POINT ( 'NONE',  ( 3.499633968373000226, -80.92957046129099297, -0.5806158015779000481 ) ) ;
#50668=CARTESIAN_POINT ( 'NONE',  ( 2.891731347767999782, -83.82504052802198657, 2.709959370028000247 ) ) ;
#50685=VERTEX_POINT ( 'NONE', #18489 ) ;
#50689=CARTESIAN_POINT ( 'NONE',  ( 3.263030582009000202, -82.33492937544698975, -1.391710130416999869 ) ) ;
#50712=CARTESIAN_POINT ( 'NONE',  ( 2.636359243785999951, -80.84653455456798099, 2.958984748685999921 ) ) ;
#50734=CARTESIAN_POINT ( 'NONE',  ( 3.962859907113000180, -85.75721544543100094, 0.04150063856765000281 ) ) ;
#50768=CARTESIAN_POINT ( 'NONE',  ( 3.715423405847853466, -82.70470561765866080, -0.7897406471633323655 ) ) ;
#50774=CARTESIAN_POINT ( 'NONE',  ( -3.206845790991853740, -80.35729166409527124, -2.475673254574849214 ) ) ;
#50798=CARTESIAN_POINT ( 'NONE',  ( 1.504274447196337405, -85.80681307243298761, 3.466210801031209154 ) ) ;
#50813=CARTESIAN_POINT ( 'NONE',  ( -2.218415739201539338, -78.39678895079168797, 3.679255581759628413 ) ) ;
#50830=CARTESIAN_POINT ( 'NONE',  ( -3.304281735504577266, -83.13229168162348515, 0.9680142999968018858 ) ) ;
#50848=CARTESIAN_POINT ( 'NONE',  ( -3.809176057898999712, -78.63855496681158286, 1.220059858830999877 ) ) ;
#50855=CARTESIAN_POINT ( 'NONE',  ( 2.588169404531000417, -84.14231094026499136, 2.425479093844999934 ) ) ;
#50866=CARTESIAN_POINT ( 'NONE',  ( 3.106054555984663956, -86.07390000031791999, -1.382904586457472496 ) ) ;
#50877=CARTESIAN_POINT ( 'NONE',  ( 3.591098859228397444, -85.56041668048763427, 1.791456720771969824 ) ) ;
#50882=CARTESIAN_POINT ( 'NONE',  ( 1.289384742053000021, -84.23744503318798138, 3.968318193697000673 ) ) ;
#50907=CARTESIAN_POINT ( 'NONE',  ( 0.7501952194293379783, -80.62708332301558301, -3.361068624121959392 ) ) ;
#50920=CARTESIAN_POINT ( 'NONE',  ( 0.4075231696620134625, -85.94906435298663894, 3.946922339886002273 ) ) ;
#50926=CARTESIAN_POINT ( 'NONE',  ( 3.277187423977000247, -80.84699166913398471, -2.586436307216999797 ) ) ;
#50953=CARTESIAN_POINT ( 'NONE',  ( -2.400634063566000176, -84.18579177382198964, 2.889347057923999706 ) ) ;
#50958=EDGE_CURVE ( 'NONE', #35853, #50685, #32183, .T. ) ;
#50975=CARTESIAN_POINT ( 'NONE',  ( -3.543871218327000250, -80.17042173478499478, 0.1598027556938000082 ) ) ;
#51001=CARTESIAN_POINT ( 'NONE',  ( -1.390911224239000044, -81.80467549782599690, -3.888944045958999673 ) ) ;
#51006=CARTESIAN_POINT ( 'NONE',  ( -3.699999999670000150, -79.00321104920828930, -1.552506213169860872E-14 ) ) ;
#51022=CARTESIAN_POINT ( 'NONE',  ( -1.664832167514000094, -85.27621544543099219, -3.596430821289000157 ) ) ;
#51030=CARTESIAN_POINT ( 'NONE',  ( 4.000000000000000000, -78.72610001270986402, 0.000000000000000000 ) ) ;
#51036=CARTESIAN_POINT ( 'NONE',  ( 2.887050208512827787, -78.99159464002811148, -2.426921481828515859 ) ) ;
#51060=CARTESIAN_POINT ( 'NONE',  ( 3.365092916910764398, -82.58831665972199687, -0.7152753179581305965 ) ) ;
#51063=CARTESIAN_POINT ( 'NONE',  ( -0.5677917205621726415, -86.25171438276198899, 4.566314625519950710 ) ) ;
#51067=CARTESIAN_POINT ( 'NONE',  ( 2.081936059911246861, -80.70416666796184302, -3.476221075145997208 ) ) ;
#51091=CARTESIAN_POINT ( 'NONE',  ( -2.611770760767388566, -85.80681307243297340, 3.525481195051840100 ) ) ;
#51147=CARTESIAN_POINT ( 'NONE',  ( 3.086296569003000201, -85.51626360600299392, 1.743485741791999999 ) ) ;
#51158=FACE_OUTER_BOUND ( 'NONE', #43482, .T. ) ;
#51171=CARTESIAN_POINT ( 'NONE',  ( -3.522477044106106181, -86.08072918608876023, 1.921747906583619159 ) ) ;
#51174=CARTESIAN_POINT ( 'NONE',  ( -2.682899408521000062, -83.38942953870899544, -3.195089342158999646 ) ) ;
#51203=CARTESIAN_POINT ( 'NONE',  ( 0.2387542509232137289, -82.09166665063389701, -3.402624595228084026 ) ) ;
#51251=CARTESIAN_POINT ( 'NONE',  ( 3.426173274723999906, -82.06136777077499289, -1.262550693616000030 ) ) ;
#51271=CARTESIAN_POINT ( 'NONE',  ( 3.537262634168000019, -79.45518468237709442, 0.2633306235646999949 ) ) ;
#51293=CARTESIAN_POINT ( 'NONE',  ( 1.686223813997999921, -79.51992549782627862, 3.168656936234999666 ) ) ;
#51312=CARTESIAN_POINT ( 'NONE',  ( 2.081307824277000229, -85.99771544543098400, 3.372558905200000456 ) ) ;
#51326=CARTESIAN_POINT ( 'NONE',  ( 0.2350766928662207378, -78.89591687295829558, -3.468875016500294173 ) ) ;
#51347=CARTESIAN_POINT ( 'NONE',  ( 3.325196253812411573, -82.46277143088778416, -0.7067949879676419522 ) ) ;
#51354=CARTESIAN_POINT ( 'NONE',  ( 0.9191423324976545350, -82.13020835052557800, -3.906387138476612009 ) ) ;
#51394=CARTESIAN_POINT ( 'NONE',  ( 1.974456470848767298, -78.70000000000000284, 3.418760428718595090 ) ) ;
#51440=CARTESIAN_POINT ( 'NONE',  ( -3.377848665726999933, -86.11751568233700027, 0.3691513799601000012 ) ) ;
#51463=CARTESIAN_POINT ( 'NONE',  ( -0.9577436045183314040, -83.51770832516572796, -3.937309471672632455 ) ) ;
#51541=CARTESIAN_POINT ( 'NONE',  ( -3.181650608227999832, -82.74278679062099684, 2.362856221671000068 ) ) ;
#51553=ORIENTED_EDGE ( 'NONE', *, *, #19022, .F. ) ;
#51561=CARTESIAN_POINT ( 'NONE',  ( -3.238485901480999907, -78.60716621652929348, 1.037469946420999989 ) ) ;
#51586=CARTESIAN_POINT ( 'NONE',  ( 1.394409823850000008, -80.48192549782599770, -3.307470144239999854 ) ) ;
#51605=CARTESIAN_POINT ( 'NONE',  ( -3.027477083952000214, -85.15596544543099355, -2.223903009527000041 ) ) ;
#51620=CARTESIAN_POINT ( 'NONE',  ( -3.336363063059238687, -78.72637457323575916, -0.7471181105293197566 ) ) ;
#51730=CARTESIAN_POINT ( 'NONE',  ( 3.432844757780000311, -83.90181010973100229, -0.8928306503459999544 ) ) ;
#51753=CARTESIAN_POINT ( 'NONE',  ( 4.048411298789319268, -83.94166666306279012, -0.1471474844110896574 ) ) ;
#51847=CARTESIAN_POINT ( 'NONE',  ( -3.522252620761999964, -78.93456160447509262, -0.6907526756895999709 ) ) ;
#51861=CARTESIAN_POINT ( 'NONE',  ( 0.4132205903738334074, -86.09999999999998010, -3.926276861431333920 ) ) ;
#51871=CARTESIAN_POINT ( 'NONE',  ( 2.498944011016999589, -80.84653455456798099, 2.804753272470999814 ) ) ;
#51876=CARTESIAN_POINT ( 'NONE',  ( 3.430559350187999623, -83.94574735065199889, -0.8923151533959999826 ) ) ;
#51902=CARTESIAN_POINT ( 'NONE',  ( 0.4866655842918644614, -78.90438882479159588, -3.447293470213554034 ) ) ;
#51932=CARTESIAN_POINT ( 'NONE',  ( 3.845056324898657785, -82.38072918665125144, -1.147388926672712639 ) ) ;
#52014=CARTESIAN_POINT ( 'NONE',  ( 2.952107475776000189, -82.34482020574199623, -1.687956242112000016 ) ) ;
#52035=CARTESIAN_POINT ( 'NONE',  ( -4.006190475301194098, -78.54828561723799396, -2.263637441416614493 ) ) ;
#52039=CARTESIAN_POINT ( 'NONE',  ( 2.343872625036407698, -85.67604168173227208, 3.257443233898490664 ) ) ;
#52046=SHAPE_REPRESENTATION ( 'Spring', ( #43526 ), #13324 ) ;
#52057=( LENGTH_UNIT ( ) NAMED_UNIT ( * ) SI_UNIT ( .MILLI., .METRE. ) );
#52134=CARTESIAN_POINT ( 'NONE',  ( -3.276755629569999773, -78.81431117999389357, 1.049729901832000101 ) ) ;
#52147=CARTESIAN_POINT ( 'NONE',  ( 3.380118192975939184, -86.40321104920799655, -1.504925579246137568 ) ) ;
#52158=CARTESIAN_POINT ( 'NONE',  ( -3.613802140370000249, -78.36136788790179253, 0.5226175732511999517 ) ) ;
#52163=CARTESIAN_POINT ( 'NONE',  ( 3.130966520949999943, -82.62299735065199968, 1.661977487544999965 ) ) ;
#52183=CARTESIAN_POINT ( 'NONE',  ( 4.171885727129999388, -85.47133100267899408, 0.04387387242050999614 ) ) ;
#52188=CARTESIAN_POINT ( 'NONE',  ( 2.332848451437957937, -78.97236559110959320, -2.708295505596481689 ) ) ;
#52192=FILL_AREA_STYLE ('',( #34153 ) ) ;
#52214=CARTESIAN_POINT ( 'NONE',  ( 3.281285156496776878, -82.30364585245855835, -2.308832152369716173 ) ) ;
#52221=CARTESIAN_POINT ( 'NONE',  ( 3.654181830570000233, -86.09999999999999432, -1.626946572303000105 ) ) ;
#52252=CARTESIAN_POINT ( 'NONE',  ( -0.03204386105641582327, -78.67390000031814168, 3.399848995318665246 ) ) ;
#52277=CARTESIAN_POINT ( 'NONE',  ( 3.106054555984329113, -86.12609999968211127, -1.382904586457928353 ) ) ;
#52382=( BOUNDED_SURFACE ( )  B_SPLINE_SURFACE ( 3, 3, ( 
 ( #16379, #12234, #11951, #20519, #47695, #26587, #2234 ),
 ( #53776, #33785, #7518, #38517, #20232, #56532, #16091 ),
 ( #11381, #34073, #31015, #25515, #49053, #11668, #29642 ),
 ( #44621, #7225, #25228, #4177, #22174, #75, #27472 ),
 ( #5624, #18054, #23348, #40773, #54070, #54362, #32766 ),
 ( #22763, #13606, #32473, #45509, #367, #55221, #36919 ),
 ( #49940, #4762, #28053, #46099, #13902, #27176, #14768 ),
 ( #23635, #18640, #41648, #19217, #50813, #36046, #41360 ),
 ( #54930, #31602, #49645, #18347, #41069, #9191, #45806 ),
 ( #45214, #5341, #50227, #18924, #36337, #36632, #5055 ),
 ( #31896, #942, #9485, #23053, #655, #9774, #27763 ),
 ( #2097, #46391, #6503, #10950, #19801, #24512, #2381 ),
 ( #15368, #37795, #56107, #33059, #56681, #1513, #16237 ),
 ( #42239, #46975, #28638, #52252, #38661, #15653, #33650 ),
 ( #55518, #20094, #51394, #55815, #28931, #5916, #42528 ) ),
 .UNSPECIFIED., .F., .F., .T. ) 
 B_SPLINE_SURFACE_WITH_KNOTS ( ( 4, 1, 1, 1, 1, 1, 1, 1, 1, 1, 1, 1, 4 ),
 ( 4, 3, 4 ),
 ( 0.009836358966825000175, 0.09153389967814999639, 0.1732269073519000224, 0.2549246240467999969, 0.3366128957582000258, 0.4183102327763000283, 0.5000049915179999305, 0.5816997512343000665, 0.6633971206824998967, 0.7450853986059999823, 0.8267830947368000061, 0.9084761241232000017, 0.9901736240545999657 ),
 ( 0.000000000000000000, 0.5000000000000000000, 1.000000000000000000 ),
 .UNSPECIFIED. ) 
 GEOMETRIC_REPRESENTATION_ITEM ( )  RATIONAL_B_SPLINE_SURFACE ( (
 ( 1.000000000000000000, 0.8025111804430778983, 0.8025111804430778983, 1.000000000000000000, 0.8025111804430778983, 0.8025111804430778983, 1.000000000000000000),
 ( 1.000000000000000000, 0.8025111804430778983, 0.8025111804430778983, 1.000000000000000000, 0.8025111804430778983, 0.8025111804430778983, 1.000000000000000000),
 ( 1.000000000000000000, 0.8025111804430778983, 0.8025111804430778983, 1.000000000000000000, 0.8025111804430778983, 0.8025111804430778983, 1.000000000000000000),
 ( 1.000000000000000000, 0.8025111804430778983, 0.8025111804430778983, 1.000000000000000000, 0.8025111804430778983, 0.8025111804430778983, 1.000000000000000000),
 ( 1.000000000000000000, 0.8025111804430778983, 0.8025111804430778983, 1.000000000000000000, 0.8025111804430778983, 0.8025111804430778983, 1.000000000000000000),
 ( 1.000000000000000000, 0.8025111804430778983, 0.8025111804430778983, 1.000000000000000000, 0.8025111804430778983, 0.8025111804430778983, 1.000000000000000000),
 ( 1.000000000000000000, 0.8025111804430778983, 0.8025111804430778983, 1.000000000000000000, 0.8025111804430778983, 0.8025111804430778983, 1.000000000000000000),
 ( 1.000000000000000000, 0.8025111804430778983, 0.8025111804430778983, 1.000000000000000000, 0.8025111804430778983, 0.8025111804430778983, 1.000000000000000000),
 ( 1.000000000000000000, 0.8025111804430778983, 0.8025111804430778983, 1.000000000000000000, 0.8025111804430778983, 0.8025111804430778983, 1.000000000000000000),
 ( 1.000000000000000000, 0.8025111804430778983, 0.8025111804430778983, 1.000000000000000000, 0.8025111804430778983, 0.8025111804430778983, 1.000000000000000000),
 ( 1.000000000000000000, 0.8025111804430778983, 0.8025111804430778983, 1.000000000000000000, 0.8025111804430778983, 0.8025111804430778983, 1.000000000000000000),
 ( 1.000000000000000000, 0.8025111804430778983, 0.8025111804430778983, 1.000000000000000000, 0.8025111804430778983, 0.8025111804430778983, 1.000000000000000000),
 ( 1.000000000000000000, 0.8025111804430778983, 0.8025111804430778983, 1.000000000000000000, 0.8025111804430778983, 0.8025111804430778983, 1.000000000000000000),
 ( 1.000000000000000000, 0.8025111804430778983, 0.8025111804430778983, 1.000000000000000000, 0.8025111804430778983, 0.8025111804430778983, 1.000000000000000000),
 ( 1.000000000000000000, 0.8025111804430778983, 0.8025111804430778983, 1.000000000000000000, 0.8025111804430778983, 0.8025111804430778983, 1.000000000000000000) ) ) 
 REPRESENTATION_ITEM ( '' )  SURFACE ( )  );
#52419=CARTESIAN_POINT ( 'NONE',  ( -1.194548181431000167, -81.98044359648298496, -3.339855766669999948 ) ) ;
#52431=CARTESIAN_POINT ( 'NONE',  ( 3.112536659741943268, -86.17851879815597727, -1.385790604991126607 ) ) ;
#52440=CARTESIAN_POINT ( 'NONE',  ( -2.879346558283000235, -78.56178455456850429, -2.412654453515000075 ) ) ;
#52444=CARTESIAN_POINT ( 'NONE',  ( 3.122208683565999898, -85.38874735065199673, -1.678325600246000082 ) ) ;
#52459=CARTESIAN_POINT ( 'NONE',  ( 3.518657424385000176, -85.83735716284299144, -1.566607219110000004 ) ) ;
#52464=CARTESIAN_POINT ( 'NONE',  ( 4.038192700013000014, -83.90181010973100229, -1.050272432624000052 ) ) ;
#52490=CARTESIAN_POINT ( 'NONE',  ( -2.265513919728744163, -78.99318692756679638, -3.757367528743593699 ) ) ;
#52500=CARTESIAN_POINT ( 'NONE',  ( 0.9271659294403999940, -81.29032046129098887, 4.067789135191000049 ) ) ;
#52563=CARTESIAN_POINT ( 'NONE',  ( 3.194290819685381866, -86.09999999999998010, 2.320109443757771395 ) ) ;
#52606=CARTESIAN_POINT ( 'NONE',  ( -4.043785186575957091, -78.69999999999998863, -2.284879765406314878 ) ) ;
#52676=CARTESIAN_POINT ( 'NONE',  ( 1.224658201351000120, -84.55471544543098616, 3.769110384959000193 ) ) ;
#52705=CARTESIAN_POINT ( 'NONE',  ( 3.006299185876999847, -79.77631457584399755, 1.961099271341999684 ) ) ;
#52719=CARTESIAN_POINT ( 'NONE',  ( -3.972981440171656331, -86.25171435493597016, -0.3803130624956269634 ) ) ;
#52729=CARTESIAN_POINT ( 'NONE',  ( -3.478367431019000033, -78.68975264934786651, -0.6823414571583998889 ) ) ;
#52733=CARTESIAN_POINT ( 'NONE',  ( -3.306603397031000036, -83.34449735065199150, -1.277238313581000151 ) ) ;
#52751=CARTESIAN_POINT ( 'NONE',  ( -4.136849130093000149, -83.11125530066698275, 0.5622182541971000314 ) ) ;
#52757=CARTESIAN_POINT ( 'NONE',  ( -3.621447497675000182, -78.99318692614357929, -1.519545876029819695E-14 ) ) ;
#52769=CARTESIAN_POINT ( 'NONE',  ( -3.654181822837000215, -86.09999999943198645, 1.626946589673999854 ) ) ;
#52777=CARTESIAN_POINT ( 'NONE',  ( -2.171318179221914058, -78.99318692614359350, -3.601143365367586835 ) ) ;
#52786=CARTESIAN_POINT ( 'NONE',  ( 4.163343027946999619, -79.41125264934790096, 0.3101205329980999403 ) ) ;
#52849=CARTESIAN_POINT ( 'NONE',  ( 3.476140009347202131, -86.40321104920798234, 2.524824982687337016 ) ) ;
#52869=CARTESIAN_POINT ( 'NONE',  ( 2.775476009882999584, -81.13242513063499928, 3.115010180492999936 ) ) ;
#52915=AXIS2_PLACEMENT_3D ( 'NONE', #1449, #2604, #10294 ) ;
#52966=CARTESIAN_POINT ( 'NONE',  ( -3.415687109163000112, -86.11024735065198854, 2.400462065159000069 ) ) ;
#52992=CARTESIAN_POINT ( 'NONE',  ( -2.377882521816736539, -78.89270832978301939, -2.490427524875605592 ) ) ;
#52994=CARTESIAN_POINT ( 'NONE',  ( 1.686350432428000090, -79.89656500032499764, 3.168590765505000295 ) ) ;
#53004=CARTESIAN_POINT ( 'NONE',  ( -3.156875167770065271, -86.31452042059396490, 1.477445080843142300 ) ) ;
#53005=CARTESIAN_POINT ( 'NONE',  ( -2.277808299861439512, -86.04892729347230329, 2.553837542456823595 ) ) ;
#53010=CARTESIAN_POINT ( 'NONE',  ( -3.973259589201000530, -78.85439465482099308, 0.5748252895958999575 ) ) ;
#53014=CARTESIAN_POINT ( 'NONE',  ( 2.110462767538999973, -79.17075264934788947, -2.847965697444999833 ) ) ;
#53016=CARTESIAN_POINT ( 'NONE',  ( -3.308786720591999853, -83.27544503318799229, -1.278081663740999963 ) ) ;
#53041=CARTESIAN_POINT ( 'NONE',  ( 1.289278921801000122, -84.26256135553198590, 3.968353856072999619 ) ) ;
#53062=CARTESIAN_POINT ( 'NONE',  ( 3.437187628289001040, -78.85171435493609238, -1.267161289092433307E-15 ) ) ;
#53074=CARTESIAN_POINT ( 'NONE',  ( -1.405958995161999958, -81.93650264934798599, -3.931017140282999645 ) ) ;
#53115=CARTESIAN_POINT ( 'NONE',  ( -3.517605154487999819, -84.71217953870899464, -0.4593545457370999952 ) ) ;
#53131=EDGE_CURVE ( 'NONE', #50685, #26598, #5661, .T. ) ;
#53137=CARTESIAN_POINT ( 'NONE',  ( -3.335532751159751452, -86.39318692614399708, 1.410355715539307830 ) ) ;
#53156=CARTESIAN_POINT ( 'NONE',  ( -0.4362184210878999879, -80.53117300822900404, -4.149249208457999494 ) ) ;
#53169=CARTESIAN_POINT ( 'NONE',  ( 3.757989199629945709, -86.10000000000000853, 2.729540522067831265 ) ) ;
#53174=CARTESIAN_POINT ( 'NONE',  ( 3.999999999999606093, -78.67389998729011324, -1.484001723589534194E-15 ) ) ;
#53232=CARTESIAN_POINT ( 'NONE',  ( 3.654181830570000233, -86.12610001270999760, -1.626946572303000105 ) ) ;
#53248=CARTESIAN_POINT ( 'NONE',  ( 3.474219449940000537, -82.38249735065198820, -1.986484532523000279 ) ) ;
#53280=CARTESIAN_POINT ( 'NONE',  ( -3.445809878667000170, -81.82057179202399766, 1.005057003444999930 ) ) ;
#53291=CARTESIAN_POINT ( 'NONE',  ( -4.615324208696027775, -86.17851881763698429, -0.4418012292915585171 ) ) ;
#53292=CARTESIAN_POINT ( 'NONE',  ( 3.572165910270233891, -85.80175210208024339, 0.8161875824647534250 ) ) ;
#53300=CARTESIAN_POINT ( 'NONE',  ( 4.005932792494999894, -82.62224128856598782, -0.2640423048605999856 ) ) ;
#53304=CARTESIAN_POINT ( 'NONE',  ( 3.380804078035000160, -82.41750264934799475, 0.3410251249121999950 ) ) ;
#53323=CARTESIAN_POINT ( 'NONE',  ( 4.171966157921000118, -82.45880512652999528, -0.06563631418457001321 ) ) ;
#53329=CARTESIAN_POINT ( 'NONE',  ( -3.407095545933028991, -78.77851879815550262, 6.814191091866018013 ) ) ;
#53349=CARTESIAN_POINT ( 'NONE',  ( 2.103055900234938491, -78.99318692614359350, -3.641429946303727405 ) ) ;
#53358=CARTESIAN_POINT ( 'NONE',  ( -4.170645326359000649, -80.13275264934799225, 0.1879290872891999920 ) ) ;
#53390=ORIENTED_EDGE ( 'NONE', *, *, #22230, .T. ) ;
#53394=CARTESIAN_POINT ( 'NONE',  ( 3.485499217011999828, -78.48547957940618858, 0.000000000000000000 ) ) ;
#53395=CARTESIAN_POINT ( 'NONE',  ( 0.1745292062968000213, -85.79442953870898236, 3.543168428762999866 ) ) ;
#53421=CARTESIAN_POINT ( 'NONE',  ( 4.268285239867531722, -86.40321104920798234, 0.4899302694419261917 ) ) ;
#53456=CARTESIAN_POINT ( 'NONE',  ( 1.533375225219753890, -85.83735716284299144, 3.533266005812401023 ) ) ;
#53461=CARTESIAN_POINT ( 'NONE',  ( -2.218416052576314801, -78.39678895079168797, -3.679255452198593179 ) ) ;
#53471=ADVANCED_FACE ( 'NONE', ( #1468 ), #15819, .T. ) ;
#53543=CARTESIAN_POINT ( 'NONE',  ( 3.635062440651000149, -85.62924735065199400, 2.053270061586999873 ) ) ;
#53572=CARTESIAN_POINT ( 'NONE',  ( -2.753094546102373918, -78.85416666326673862, -2.068686224605921442 ) ) ;
#53576=CARTESIAN_POINT ( 'NONE',  ( -3.502956697134000041, -81.94082221650599251, -0.7829685155521000084 ) ) ;
#53587=CARTESIAN_POINT ( 'NONE',  ( 1.992133063105471891, -85.88985440391550696, 2.860955247882542629 ) ) ;
#53592=CARTESIAN_POINT ( 'NONE',  ( -2.796407410894000023, -81.81671231080099460, 2.808219311970999943 ) ) ;
#53595=CARTESIAN_POINT ( 'NONE',  ( 3.438062426372999969, -82.37741931601499346, -0.2266141585933000024 ) ) ;
#53619=CARTESIAN_POINT ( 'NONE',  ( -0.7867051183105999712, -84.31375945333499544, 4.100085976432000123 ) ) ;
#53626=CARTESIAN_POINT ( 'NONE',  ( 3.437187628289001040, -78.85171435493609238, 6.874375256578030502 ) ) ;
#53642=B_SPLINE_CURVE_WITH_KNOTS ( 'NONE', 3,
 ( #16978, #57996, #34962, #53572, #52992, #17551, #30823, #30538, #44136, #17256, #48857, #8399, #35543, #49145, #26686, #14576, #50618, #55321, #1321, #55616, #23442, #14865, #42038, #9874, #23152, #32862, #10455, #14284, #5432, #18443, #4864, #36433, #9582, #41453, #5723, #464, #50907, #19315, #41157, #28442, #32280, #32570, #751, #22862, #23733, #1607, #41745, #1038, #50324, #46490, #18731, #46198, #19023, #37014, #36724, #6015, #24023, #40872, #54739, #27855, #54460, #28735, #10169, #51203, #37305, #15163, #28143, #19599, #33159, #13996, #37599 ),
 .UNSPECIFIED., .F., .F.,
 ( 4, 2, 2, 2, 1, 2, 2, 2, 2, 2, 2, 2, 2, 2, 2, 2, 2, 2, 1, 2, 2, 2, 2, 2, 2, 2, 2, 2, 2, 2, 2, 2, 1, 2, 2, 2, 4 ),
 ( 0.000000000000000000, 0.03124999999999998612, 0.06249999999999997224, 0.07812499999999995837, 0.09374999999999993061, 0.1093749999999999167, 0.1249999999999998890, 0.1562499999999999445, 0.1874999999999999445, 0.2187499999999999445, 0.2500000000000000000, 0.2812500000000000555, 0.3125000000000000555, 0.3437500000000001110, 0.3750000000000001665, 0.4062500000000001665, 0.4375000000000001110, 0.4687500000000001110, 0.5000000000000001110, 0.5312500000000001110, 0.5625000000000001110, 0.5937500000000001110, 0.6250000000000000000, 0.6562500000000000000, 0.6875000000000000000, 0.7187500000000000000, 0.7500000000000000000, 0.7812500000000000000, 0.8125000000000000000, 0.8437500000000000000, 0.8749999999999998890, 0.8906249999999998890, 0.9062499999999998890, 0.9218749999999998890, 0.9374999999999998890, 0.9687499999999998890, 1.000000000000000000 ),
 .UNSPECIFIED. ) ;
#53646=CARTESIAN_POINT ( 'NONE',  ( -3.547719542586254882, -78.96264282632948550, 0.06688145936885296627 ) ) ;
#53657=CARTESIAN_POINT ( 'NONE',  ( 3.275410689762999983, -80.80305496681198463, -2.584907563698999766 ) ) ;
#53664=CARTESIAN_POINT ( 'NONE',  ( -2.267046284475000117, -84.50932768054498467, 2.728563928855000320 ) ) ;
#53681=CARTESIAN_POINT ( 'NONE',  ( -1.560185313921000017, -83.23196544543098696, 3.417189128149000332 ) ) ;
#53726=CARTESIAN_POINT ( 'NONE',  ( -0.5084075448448571732, -86.36264282632899381, 4.088733110535507365 ) ) ;
#53764=CARTESIAN_POINT ( 'NONE',  ( 3.851650068367000301, -78.43735716284257364, -2.273141396972203854 ) ) ;
#53776=CARTESIAN_POINT ( 'NONE',  ( 3.999999999999605649, -78.67389998729011324, -4.898587196588929651E-16 ) ) ;
#53815=CARTESIAN_POINT ( 'NONE',  ( 3.125201106736000156, -85.38443645448099062, 1.765463379168000113 ) ) ;
#53825=CARTESIAN_POINT ( 'NONE',  ( 3.184161977317999881, -86.31452042059399332, -1.417680250971000033 ) ) ;
#53843=CARTESIAN_POINT ( 'NONE',  ( -4.134522458939999368, -83.15519503318799366, 0.5619488135074000024 ) ) ;
#53877=CARTESIAN_POINT ( 'NONE',  ( -1.265088337640000171, -82.29771400872598974, -3.537080082236999878 ) ) ;
#53889=CARTESIAN_POINT ( 'NONE',  ( -1.536715235503818278, -86.40321104920798234, -3.365784645892647919 ) ) ;
#53890=CARTESIAN_POINT ( 'NONE',  ( 3.645504569144430551, -85.80231680694522822, 0.8496922539149652787 ) ) ;
#53896=STYLED_ITEM ( 'NONE', ( #34309 ), #44024 ) ;
#53897=CARTESIAN_POINT ( 'NONE',  ( 3.645312667415999908, -82.65846528216999900, -1.554756671834999882 ) ) ;
#53900=CARTESIAN_POINT ( 'NONE',  ( -2.026060677209999827, -80.37325264934800373, -2.908615120711000035 ) ) ;
#53925=CARTESIAN_POINT ( 'NONE',  ( -1.753665918641999832, -84.91501152966898758, -3.788702389557000227 ) ) ;
#53950=CARTESIAN_POINT ( 'NONE',  ( -4.043785186575886925, -78.72610001270986402, -2.284879765406275354 ) ) ;
#53960=CARTESIAN_POINT ( 'NONE',  ( -0.4361488465060999742, -80.56255496681198736, -4.149679081948000281 ) ) ;
#53966=CARTESIAN_POINT ( 'NONE',  ( 2.588476952076999904, -84.14857643474398685, 2.425767309192000454 ) ) ;
#53980=CARTESIAN_POINT ( 'NONE',  ( 3.588900492731000202, -82.63457450217399014, -0.05646551414434999860 ) ) ;
#53998=CARTESIAN_POINT ( 'NONE',  ( 3.235517742858999846, -82.34726287204199480, -1.192291943657000086 ) ) ;
#54020=CARTESIAN_POINT ( 'NONE',  ( 3.140027144888846156, -86.25171435493598437, -1.398030157552344832 ) ) ;
#54054=CARTESIAN_POINT ( 'NONE',  ( 3.518657424384978416, -85.83735716284299144, -1.566607219110048188 ) ) ;
#54058=CARTESIAN_POINT ( 'NONE',  ( -3.437217408589773093, -78.67390000031812747, -1.942147800595485974 ) ) ;
#54070=CARTESIAN_POINT ( 'NONE',  ( -2.347024351938371112, -78.48547955770030171, 3.892553724173937191 ) ) ;
#54108=CARTESIAN_POINT ( 'NONE',  ( 0.1764146904384000236, -85.62493728501499390, 3.585048402307000170 ) ) ;
#54131=CLOSED_SHELL ( 'NONE', ( #37907, #42749, #47329, #5707, #8476, #26195, #30555, #53471, #41022, #35489, #16186, #48319 ) ) ;
#54135=CARTESIAN_POINT ( 'NONE',  ( -1.813145781940000090, -86.12182450217399321, 3.710959265555000108 ) ) ;
#54166=CARTESIAN_POINT ( 'NONE',  ( -0.9905238183362000681, -81.58007094306199747, 3.450015621052000103 ) ) ;
#54179=CARTESIAN_POINT ( 'NONE',  ( 2.636417525263768713, -86.31452044229999387, -3.702674772290223348 ) ) ;
#54186=CARTESIAN_POINT ( 'NONE',  ( 4.161023627692999938, -79.45518468237709442, 0.3097663532143999920 ) ) ;
#54190=CARTESIAN_POINT ( 'NONE',  ( -2.503181846702999813, -81.53082046129100036, 2.513689163497000223 ) ) ;
#54213=CARTESIAN_POINT ( 'NONE',  ( -0.8079786370952000141, -83.47200654646700002, -4.095946834719000229 ) ) ;
#54256=CARTESIAN_POINT ( 'NONE',  ( -2.265188552264999711, -80.12503455456798918, -3.251907382878999719 ) ) ;
#54277=CARTESIAN_POINT ( 'NONE',  ( -3.377828507812000058, -86.23049735065200139, 0.3693357844676999902 ) ) ;
#54283=CARTESIAN_POINT ( 'NONE',  ( 1.572508323189017787, -84.21145834493079008, 3.064032359733801503 ) ) ;
#54345=EDGE_CURVE ( 'NONE', #35853, #16460, #32305, .T. ) ;
#54348=CARTESIAN_POINT ( 'NONE',  ( -3.480234241935690864, -85.80681307243298761, 1.471539517285068932 ) ) ;
#54352=CARTESIAN_POINT ( 'NONE',  ( -3.399395987256420781, -78.70000000000000284, 0.06408526995191715647 ) ) ;
#54362=CARTESIAN_POINT ( 'NONE',  ( -3.957349787215346471, -78.48547955770030171, 2.236041248680080251 ) ) ;
#54404=CARTESIAN_POINT ( 'NONE',  ( 3.588901577296000234, -82.25792565754399277, -0.05646313095269000354 ) ) ;
#54417=CARTESIAN_POINT ( 'NONE',  ( 3.451879464910977191, -85.80681307243298761, -1.536875756006051752 ) ) ;
#54433=CARTESIAN_POINT ( 'NONE',  ( -3.975696890031999331, -86.15517953870899248, 0.4347074241009999951 ) ) ;
#54460=CARTESIAN_POINT ( 'NONE',  ( -1.373083971518393565, -81.97604165108509733, -3.122541964024958094 ) ) ;
#54462=CARTESIAN_POINT ( 'NONE',  ( 3.582810207382000289, -82.77871570665098488, 0.3614056475548999559 ) ) ;
#54473=AXIS2_PLACEMENT_3D ( 'NONE', #40105, #13536, #3240 ) ;
#54474=CARTESIAN_POINT ( 'NONE',  ( 3.654181830570633949, -86.09999999999978115, -1.626946572303283656 ) ) ;
#54475=CARTESIAN_POINT ( 'NONE',  ( -2.381013104730116403, -86.03776559246422551, 3.227344833870573915 ) ) ;
#54480=CARTESIAN_POINT ( 'NONE',  ( -1.152093420842999816, -81.44824379153999416, 4.012765998397000544 ) ) ;
#54484=CARTESIAN_POINT ( 'NONE',  ( -1.757625406357000042, -79.96757046129098967, 3.081445367595999407 ) ) ;
#54486=CARTESIAN_POINT ( 'NONE',  ( 0.000000000000000000, -86.09999999999999432, 0.000000000000000000 ) ) ;
#54509=CARTESIAN_POINT ( 'NONE',  ( 3.997213461646000443, -83.70093064074599454, -1.039614356706999976 ) ) ;
#54516=CARTESIAN_POINT ( 'NONE',  ( 3.962812355711000212, -78.85171438276199751, -4.853045467043058701E-16 ) ) ;
#54531=EDGE_LOOP ( 'NONE', ( #38535, #21037, #49888, #45444 ) ) ;
#54534=CARTESIAN_POINT ( 'NONE',  ( 2.322889840689335017, -78.69999999999998863, -4.022071228304438861 ) ) ;
#54546=CARTESIAN_POINT ( 'NONE',  ( -3.867633442252000009, -81.44778455456800259, -0.8645186538081999217 ) ) ;
#54570=CARTESIAN_POINT ( 'NONE',  ( 3.161565914092999918, -85.52057450217398582, -1.699481856679999847 ) ) ;
#54574=CARTESIAN_POINT ( 'NONE',  ( 1.017700374863836688, -85.75312500679751793, 3.277910159453279348 ) ) ;
#54603=PRODUCT_DEFINITION ( 'UNKNOWN', '', #9353, #16836 ) ;
#54608=CARTESIAN_POINT ( 'NONE',  ( 2.551980763918843653, -79.23958331830202440, -3.097208638987810403 ) ) ;
#54637=CARTESIAN_POINT ( 'NONE',  ( -3.138103972814559217, -86.02148120184399716, 1.326877354891812244 ) ) ;
#54640=CARTESIAN_POINT ( 'NONE',  ( 2.194290298650410698, -78.40681307243319509, -3.799401814995372995 ) ) ;
#54688=CARTESIAN_POINT ( 'NONE',  ( -3.306587955628999875, -83.23150571593299674, -1.277281160637999902 ) ) ;
#54698=CARTESIAN_POINT ( 'NONE',  ( 0.3488014753759141051, -85.88547957940599531, -7.786004205606935180 ) ) ;
#54713=CARTESIAN_POINT ( 'NONE',  ( 1.268460950069999926, -83.62992953870899271, -3.974613432138999869 ) ) ;
#54739=CARTESIAN_POINT ( 'NONE',  ( -2.311705299946139380, -81.89895831805255000, -2.551961939471520946 ) ) ;
#54752=CARTESIAN_POINT ( 'NONE',  ( 3.528139790557236477, -85.82128727395084411, 1.440633993175003402 ) ) ;
#54760=CARTESIAN_POINT ( 'NONE',  ( 0.6660276224462000627, -82.16974633842799847, -4.121401291365000219 ) ) ;
#54764=CARTESIAN_POINT ( 'NONE',  ( 2.359885590755999907, -81.17007046129099024, 2.648677523046000015 ) ) ;
#54788=CARTESIAN_POINT ( 'NONE',  ( -0.7993309613926999901, -83.34017939494499672, -4.052108522299000093 ) ) ;
#54797=CARTESIAN_POINT ( 'NONE',  ( -3.962812355711033074, -78.85171438276199751, 7.925624711422019075 ) ) ;
#54831=CARTESIAN_POINT ( 'NONE',  ( 0.9178498446945000389, -81.08317549782599087, 4.026916334423999544 ) ) ;
#54848=CARTESIAN_POINT ( 'NONE',  ( 1.091293945889000083, -83.83707450217399071, -3.419475842359000151 ) ) ;
#54883=CARTESIAN_POINT ( 'NONE',  ( -3.621447497675000182, -78.40681307390448751, -1.372262476832999913E-09 ) ) ;
#54887=CARTESIAN_POINT ( 'NONE',  ( -4.008544904492841177, -80.16458332861317615, 0.5932793604889254890 ) ) ;
#54914=CARTESIAN_POINT ( 'NONE',  ( 3.241578942234978999, -85.83735717367099483, -1.443243930775044870 ) ) ;
#54930=CARTESIAN_POINT ( 'NONE',  ( 3.621447497675000182, -78.40681307385639798, -4.434994086307880463E-16 ) ) ;
#54949=CARTESIAN_POINT ( 'NONE',  ( -2.278711097333574465, -83.40208334745025809, -2.582645949866041235 ) ) ;
#54973=CARTESIAN_POINT ( 'NONE',  ( 2.573844042005999810, -83.71250737700098909, -2.437272650364000093 ) ) ;
#54986=CARTESIAN_POINT ( 'NONE',  ( -6.254307708149989153, -85.80681307385599155, -5.143738424904902296 ) ) ;
#55000=CARTESIAN_POINT ( 'NONE',  ( 1.268589096840999852, -83.63619503318798820, -3.975014969037000689 ) ) ;
#55042=CARTESIAN_POINT ( 'NONE',  ( 3.554131759373959643, -85.81848765646206800, 1.355124311572487139 ) ) ;
#55048=CARTESIAN_POINT ( 'NONE',  ( -3.198370537365000210, -78.85393255997098549, -2.679685760545999607 ) ) ;
#55053=CARTESIAN_POINT ( 'NONE',  ( -3.238543791219999690, -78.64482046129089099, 1.037289224933999998 ) ) ;
#55077=CARTESIAN_POINT ( 'NONE',  ( 3.640419752155000133, -83.70479011275499204, 0.9266684177237000108 ) ) ;
#55084=CARTESIAN_POINT ( 'NONE',  ( 3.778552491321002016, -78.99318692756679638, 7.557104982642034230 ) ) ;
#55097=CARTESIAN_POINT ( 'NONE',  ( -2.503149587979999868, -81.49317640407899432, 2.513722780998999706 ) ) ;
#55105=CARTESIAN_POINT ( 'NONE',  ( -2.398287624620532910, -78.69999999999998863, -3.977573462190750142 ) ) ;
#55119=CARTESIAN_POINT ( 'NONE',  ( -0.4142543683532000087, -80.24528455456798781, -3.941367037266000573 ) ) ;
#55137=CARTESIAN_POINT ( 'NONE',  ( -0.7466828201185000680, -84.67496544543098480, 3.892100405984999956 ) ) ;
#55145=CARTESIAN_POINT ( 'NONE',  ( 3.548349909811000291, -78.96264282632948550, 0.000000000000000000 ) ) ;
#55180=CARTESIAN_POINT ( 'NONE',  ( 3.751322949195571077, -86.17851881763701272, 2.724698623987952928 ) ) ;
#55183=CARTESIAN_POINT ( 'NONE',  ( -3.823662190920919635, -80.28020832990246447, -1.341411907055170660 ) ) ;
#55207=CARTESIAN_POINT ( 'NONE',  ( -2.452652587122547523, -85.83735717367099483, 3.310696598561351234 ) ) ;
#55221=CARTESIAN_POINT ( 'NONE',  ( -3.893811115504242970, -78.43735716284257364, 2.200139673516985361 ) ) ;
#55241=CARTESIAN_POINT ( 'NONE',  ( -0.2605555034656120705, -82.84322918252360068, 3.400557700907242520 ) ) ;
#55258=CARTESIAN_POINT ( 'NONE',  ( -1.405028834994999976, -82.01182046129099490, -3.928416441703999507 ) ) ;
#55263=CARTESIAN_POINT ( 'NONE',  ( 1.941413306027000019, -82.70557145154198508, 2.969078086012999940 ) ) ;
#55276=CARTESIAN_POINT ( 'NONE',  ( -6.843851216451987796, -85.94828561723799965, -5.628597459398892333 ) ) ;
#55291=CARTESIAN_POINT ( 'NONE',  ( 3.471920961466000044, -82.30717953870899350, -1.985170305869999874 ) ) ;
#55321=CARTESIAN_POINT ( 'NONE',  ( 3.430463647390288529, -79.47083332752710305, 0.3047064478928679931 ) ) ;
#55335=CARTESIAN_POINT ( 'NONE',  ( 2.736345944437820421, -85.86944366957823149, 2.769272514814725028 ) ) ;
#55340=CIRCLE ( 'NONE', #38385, 3.399999999999999911 ) ;
#55341=CARTESIAN_POINT ( 'NONE',  ( 0.5577297053749999955, -79.16348572639719805, -4.137458692512000269 ) ) ;
#55346=CARTESIAN_POINT ( 'NONE',  ( -3.481077770090000190, -78.76507046129088963, -0.6828731366740999897 ) ) ;
#55369=CARTESIAN_POINT ( 'NONE',  ( 1.160729942571000040, -83.94529094328899532, 3.572684750812999965 ) ) ;
#55388=CARTESIAN_POINT ( 'NONE',  ( -0.3708642736603999790, -80.53743850270798532, -3.527609609179999772 ) ) ;
#55412=CARTESIAN_POINT ( 'NONE',  ( 3.110986529608999795, -80.48578455456799929, -2.455146353428000250 ) ) ;
#55435=CARTESIAN_POINT ( 'NONE',  ( 3.997189897728999686, -84.07757450217398798, -1.039700163341999994 ) ) ;
#55486=CARTESIAN_POINT ( 'NONE',  ( -3.106054555984679499, -86.07390000031791999, 1.382904586457438967 ) ) ;
#55504=CARTESIAN_POINT ( 'NONE',  ( -3.407883501311117946, -85.79678895079199208, 1.440947618426057009 ) ) ;
#55518=CARTESIAN_POINT ( 'NONE',  ( 3.399999999999980815, -78.70000000000000284, -4.163799117100976893E-16 ) ) ;
#55557=CARTESIAN_POINT ( 'NONE',  ( 3.437433312124999585, -84.02206052499799682, 0.8749982434006999821 ) ) ;
#55570=CARTESIAN_POINT ( 'NONE',  ( 3.620209227049975720, -85.94828561723799965, -1.611820994701054222 ) ) ;
#55583=CARTESIAN_POINT ( 'NONE',  ( -3.355836315903201417, -86.06145835254793042, 2.200893284374637826 ) ) ;
#55586=CARTESIAN_POINT ( 'NONE',  ( 2.265192278225999889, -85.19944503318799889, -3.504135580763000135 ) ) ;
#55595=DIRECTION ( 'NONE',  ( -0.9999999999999997780, 0.000000000000000000, 2.125172267659999677E-08 ) ) ;
#55616=CARTESIAN_POINT ( 'NONE',  ( 2.894124890898986280, -79.58645832707598800, 1.867041973107900210 ) ) ;
#55627=CARTESIAN_POINT ( 'NONE',  ( 2.546818232473923249, -85.87759057800617768, 2.955671346788312892 ) ) ;
#55663=CARTESIAN_POINT ( 'NONE',  ( 2.055812863559000281, -82.38203554481998481, 3.144033732121000124 ) ) ;
#55684=ORIENTED_EDGE ( 'NONE', *, *, #41247, .T. ) ;
#55686=CARTESIAN_POINT ( 'NONE',  ( -3.405161111042999789, -81.61969232303898991, 0.9932007693457001185 ) ) ;
#55712=CARTESIAN_POINT ( 'NONE',  ( 3.542352713837999989, -80.72628455456799657, 1.250239712736999964 ) ) ;
#55734=CARTESIAN_POINT ( 'NONE',  ( -2.655941862454000102, -83.59657450217399344, -3.162985355011000088 ) ) ;
#55741=CARTESIAN_POINT ( 'NONE',  ( 4.037784781204999618, -83.90807560421097833, -1.050166339152999839 ) ) ;
#55748=CARTESIAN_POINT ( 'NONE',  ( 2.604727510204928986, -78.97720587346522336, -2.786836471777216495 ) ) ;
#55755=CIRCLE ( 'NONE', #2034, 3.400000000000000799 ) ;
#55777=CARTESIAN_POINT ( 'NONE',  ( 4.029970506843416622, -80.97395833763627593, 0.4115634813596021901 ) ) ;
#55804=CARTESIAN_POINT ( 'NONE',  ( -0.03204405817076169671, -78.70000000000000284, -3.399848993460711899 ) ) ;
#55815=CARTESIAN_POINT ( 'NONE',  ( -0.03204386105641461591, -78.70000000000000284, 3.399848995318537348 ) ) ;
#55843=ORIENTED_EDGE ( 'NONE', *, *, #15855, .F. ) ;
#55856=CARTESIAN_POINT ( 'NONE',  ( -3.380079031964000169, -86.18656799980000471, 0.3693951276397000050 ) ) ;
#55882=CARTESIAN_POINT ( 'NONE',  ( -2.680836717414254444, -83.40208332392113277, -3.038406753995844145 ) ) ;
#55930=B_SPLINE_CURVE_WITH_KNOTS ( 'NONE', 3,
 ( #38894, #16763, #30889, #34163, #7031, #17041, #48352, #25032, #38610, #7892, #56625, #34741, #11755, #29734, #52769 ),
 .UNSPECIFIED., .F., .F.,
 ( 4, 1, 1, 1, 1, 1, 1, 1, 1, 1, 1, 1, 4 ),
 ( 0.000000000000000000, 0.08333611588665000569, 0.1666676715620999949, 0.2500039875833999781, 0.3333306964953999807, 0.4166666792817999565, 0.4999999999924999994, 0.5833333197091999933, 0.6666692694150000431, 0.7499959719902999922, 0.8333323089881000678, 0.9166638425153998959, 1.000000000000000000 ),
 .UNSPECIFIED. ) ;
#55959=CARTESIAN_POINT ( 'NONE',  ( -3.689388438892000188, -84.30604218908899838, 1.447205210676999920 ) ) ;
#55980=CARTESIAN_POINT ( 'NONE',  ( -0.3709083427993999926, -80.53117300822900404, -3.528028788725999565 ) ) ;
#56004=CARTESIAN_POINT ( 'NONE',  ( 3.582810602826999702, -82.16928455456799441, 0.3614017272707000239 ) ) ;
#56009=CARTESIAN_POINT ( 'NONE',  ( -3.399999999999999911, -78.69999997992952956, 5.715921273723000819E-07 ) ) ;
#56023=CARTESIAN_POINT ( 'NONE',  ( -3.707169433487000454, -86.43863211209799147, 1.047003938644999854 ) ) ;
#56037=CARTESIAN_POINT ( 'NONE',  ( 2.402961585942242184, -78.97529329368650508, -2.655007460227098992 ) ) ;
#56062=CARTESIAN_POINT ( 'NONE',  ( -3.399395987256130347, -78.72609999968184979, 0.06408526995191166087 ) ) ;
#56107=CARTESIAN_POINT ( 'NONE',  ( 1.978577013961021702, -78.62148120184446043, 3.425895126264470125 ) ) ;
#56113=CARTESIAN_POINT ( 'NONE',  ( 3.715424088830954208, -82.09527493484321781, -0.7897374049847233346 ) ) ;
#56148=CARTESIAN_POINT ( 'NONE',  ( -0.6864729959702000617, -83.54105886393099922, -3.479989155495999853 ) ) ;
#56172=CARTESIAN_POINT ( 'NONE',  ( 0.3829117639031977549, -85.09791667550908301, -4.033878987895386459 ) ) ;
#56191=FILL_AREA_STYLE ('',( #29588 ) ) ;
#56193=ORIENTED_EDGE ( 'NONE', *, *, #8089, .T. ) ;
#56268=DIRECTION ( 'NONE',  ( 0.000000000000000000, -1.000000000000000000, 0.000000000000000000 ) ) ;
#56270=CARTESIAN_POINT ( 'NONE',  ( -3.412272945380999900, -78.65351518583565849, 0.4936653998998999926 ) ) ;
#56292=CARTESIAN_POINT ( 'NONE',  ( 2.948832248429000380, -80.48578455456799929, -2.327176499381999886 ) ) ;
#56297=CARTESIAN_POINT ( 'NONE',  ( 3.232998594844000539, -82.42258068398498949, -1.191363634767000024 ) ) ;
#56313=CARTESIAN_POINT ( 'NONE',  ( 0.2778302777538999568, -85.39646544543099083, -3.953326594592999843 ) ) ;
#56322=CARTESIAN_POINT ( 'NONE',  ( -3.349471176857000021, -83.06632269734298291, 2.487488346166999875 ) ) ;
#56327=CARTESIAN_POINT ( 'NONE',  ( -2.593635880370856572, -78.78614491170810652, -2.240786627949076237 ) ) ;
#56358=CARTESIAN_POINT ( 'NONE',  ( -3.740889684922000136, -80.32832046129098558, -1.847238338933999913 ) ) ;
#56436=CARTESIAN_POINT ( 'NONE',  ( 0.2671998652489999682, -82.82582186680899383, 3.537396816914999853 ) ) ;
#56461=CARTESIAN_POINT ( 'NONE',  ( -1.539461606647227976, -84.98229167426450203, -3.748297833576170746 ) ) ;
#56501=CARTESIAN_POINT ( 'NONE',  ( -3.684198380124090733, -86.12610001270965654, 1.557781209248569221 ) ) ;
#56532=CARTESIAN_POINT ( 'NONE',  ( -4.043784919593939264, -78.67389998729011324, 2.284880126142478485 ) ) ;
#56555=CARTESIAN_POINT ( 'NONE',  ( 2.782519347732000270, -80.84699166913398471, -2.196032187189999707 ) ) ;
#56568=CARTESIAN_POINT ( 'NONE',  ( -3.085863646355653689, -86.17851879815594884, 1.444211070176307565 ) ) ;
#56579=CARTESIAN_POINT ( 'NONE',  ( 3.384763024812000420, -80.84267549782599360, 1.194619930221000104 ) ) ;
#56583=CARTESIAN_POINT ( 'NONE',  ( -2.856781450715000226, -84.90774735065198797, -2.098514601310999872 ) ) ;
#56612=CARTESIAN_POINT ( 'NONE',  ( 0.8389761809808545800, -78.91645938753869416, -3.390143433233239190 ) ) ;
#56625=CARTESIAN_POINT ( 'NONE',  ( -3.576074390260000069, -86.31452044231799903, 1.592170898656000144 ) ) ;
#56638=CARTESIAN_POINT ( 'NONE',  ( -4.000000000000000000, -78.67389998644428317, 2.834003763004000336E-08 ) ) ;
#56642=CARTESIAN_POINT ( 'NONE',  ( 2.622047509604808369, -80.74270833505833878, -3.088315007378679589 ) ) ;
#56645=CARTESIAN_POINT ( 'NONE',  ( 3.275079823525000045, -80.80932046129099433, -2.584646448766000137 ) ) ;
#56681=CARTESIAN_POINT ( 'NONE',  ( -2.042798482360907997, -78.62148120184446043, 3.387993325967679770 ) ) ;
#56688=CARTESIAN_POINT ( 'NONE',  ( 3.521764644577042080, -82.09527493484321781, -0.7485738383772502225 ) ) ;
#56706=CARTESIAN_POINT ( 'NONE',  ( -2.350111744379427048, -86.09999999999998010, 3.172282531659214033 ) ) ;
#56750=CARTESIAN_POINT ( 'NONE',  ( 1.036720466796444917, -85.13645834259065737, -3.915773151610196567 ) ) ;
#56790=CARTESIAN_POINT ( 'NONE',  ( 1.592434616855475493, -86.09999999999978115, 3.669353075276663656 ) ) ;
#56846=CARTESIAN_POINT ( 'NONE',  ( 0.7877959022907999875, -81.32799336705899407, 3.456059736074999833 ) ) ;
#56869=CARTESIAN_POINT ( 'NONE',  ( 3.705853105876000253, -80.60603455456799793, -0.6148291195716999447 ) ) ;
#56875=CARTESIAN_POINT ( 'NONE',  ( -3.380460507093999478, -86.15517953870899248, 0.3696235703980000342 ) ) ;
#56891=CARTESIAN_POINT ( 'NONE',  ( 3.380118192976000469, -85.79678895079199208, -1.504925579245999900 ) ) ;
#56896=CARTESIAN_POINT ( 'NONE',  ( -0.7862640713001000092, -84.38281177079799988, 4.097787363367999980 ) ) ;
#56902=CARTESIAN_POINT ( 'NONE',  ( 3.003961014100700044, -78.99951684686710962, -2.201084085522161171 ) ) ;
#56921=CARTESIAN_POINT ( 'NONE',  ( 3.485499217012000273, -78.91452042059380290, -1.287490079826536515E-15 ) ) ;
#56928=CARTESIAN_POINT ( 'NONE',  ( -3.770920640554758840, -81.78333334665865095, -1.371725514654604350 ) ) ;
#56930=CARTESIAN_POINT ( 'NONE',  ( 3.934265133962999705, -81.04982046129099160, 1.388561475457000149 ) ) ;
#56964=CARTESIAN_POINT ( 'NONE',  ( 3.437187628289000152, -78.54828564506388489, 0.000000000000000000 ) ) ;
#56989=ORIENTED_EDGE ( 'NONE', *, *, #46934, .T. ) ;
#57029=CARTESIAN_POINT ( 'NONE',  ( 3.962812355711000212, -78.54828561723799396, -1.463672932855430986E-15 ) ) ;
#57128=CARTESIAN_POINT ( 'NONE',  ( -1.193759951361000216, -82.04949591394598940, -3.337651942004999484 ) ) ;
#57142=CARTESIAN_POINT ( 'NONE',  ( -1.427561782742997831, -86.25171435493597016, -3.126711714967702171 ) ) ;
#57152=CARTESIAN_POINT ( 'NONE',  ( 1.377051302669000110, -80.61375264934798679, -3.266296602878999700 ) ) ;
#57154=CARTESIAN_POINT ( 'NONE',  ( 1.096098671195999907, -84.23744503318798138, 3.373444835455999602 ) ) ;
#57175=CARTESIAN_POINT ( 'NONE',  ( 4.043590400160999465, -84.02206052499799682, 1.029295458530999907 ) ) ;
#57182=CARTESIAN_POINT ( 'NONE',  ( -3.485499217011999828, -78.91452042059380290, -1.462502484024984119E-14 ) ) ;
#57199=EDGE_LOOP ( 'NONE', ( #26383, #20364, #23547, #48927 ) ) ;
#57201=CARTESIAN_POINT ( 'NONE',  ( 3.621447497675000182, -78.99318692614357929, -1.355252715606880543E-15 ) ) ;
#57211=CARTESIAN_POINT ( 'NONE',  ( 3.494616459463999902, -79.60055496681158616, 2.279850439600000112 ) ) ;
#57295=CARTESIAN_POINT ( 'NONE',  ( -3.740947899408999966, -80.29067215926599488, -1.847123254877999887 ) ) ;
#57316=CARTESIAN_POINT ( 'NONE',  ( 3.999999999999885425, -78.69999999999998863, -1.477225460011499791E-15 ) ) ;
#57393=CARTESIAN_POINT ( 'NONE',  ( 4.174648323465000033, -85.50899735065199536, 0.04371857074945000032 ) ) ;
#57434=CARTESIAN_POINT ( 'NONE',  ( -0.6316792277967039348, -85.98317637962277615, 3.377175175332928880 ) ) ;
#57438=EDGE_CURVE ( 'NONE', #35853, #50685, #1071, .T. ) ;
#57440=CARTESIAN_POINT ( 'NONE',  ( -4.030735489442000663, -81.94082221650599251, -0.9009357681566000364 ) ) ;
#57443=CARTESIAN_POINT ( 'NONE',  ( -0.05200060359788999387, -79.84105496681198133, 3.546668618212000190 ) ) ;
#57446=CARTESIAN_POINT ( 'NONE',  ( 3.133033872897999839, -82.55394503318800048, 1.663074877879000102 ) ) ;
#57463=CARTESIAN_POINT ( 'NONE',  ( 0.2926765216785000012, -85.10431426239898656, -4.162260556948999657 ) ) ;
#57469=CARTESIAN_POINT ( 'NONE',  ( 1.111733232284327855, -78.92199391444442824, -3.740299636916243564 ) ) ;
#57486=CARTESIAN_POINT ( 'NONE',  ( 3.851650068367000745, -78.96264283715740362, -1.429791614965258972E-15 ) ) ;
#57497=CARTESIAN_POINT ( 'NONE',  ( -1.508376887600999972, -78.93025264934789220, -3.892856298602999754 ) ) ;
#57535=CARTESIAN_POINT ( 'NONE',  ( -2.266963109989999836, -84.47167953870898316, 2.728631686324999972 ) ) ;
#57557=CARTESIAN_POINT ( 'NONE',  ( 4.358902656273683007, -86.39318692756700102, 0.5003316865777546196 ) ) ;
#57575=CARTESIAN_POINT ( 'NONE',  ( 3.979600690714999889, -82.46144529440799431, 0.4014307432961000122 ) ) ;
#57583=MANIFOLD_SOLID_BREP ( 'Stock-MAS-694-1', #54131 ) ;
#57590=EDGE_CURVE ( 'NONE', #36712, #34390, #55755, .T. ) ;
#57592=CARTESIAN_POINT ( 'NONE',  ( -2.759932835650348526, -86.02148118236286223, 3.725476775316406641 ) ) ;
#57625=B_SPLINE_CURVE_WITH_KNOTS ( 'NONE', 3,
 ( #32442, #18892, #50487, #19184, #1773, #1482, #18609, #19472, #41909, #14734, #36885, #32733, #37465, #55486, #41035 ),
 .UNSPECIFIED., .F., .F.,
 ( 4, 1, 1, 1, 1, 1, 1, 1, 1, 1, 1, 1, 4 ),
 ( 0.000000000000000000, 0.08333615544490723115, 0.1666676869327075872, 0.2500040218909077572, 0.3333307224267462732, 0.4166666700929356204, 0.4999999877701112316, 0.5833333064412306035, 0.6666692871879731364, 0.7499959940605083197, 0.8333323080421526363, 0.9166638616780954374, 1.000000000000000000 ),
 .UNSPECIFIED. ) ;
#57673=CARTESIAN_POINT ( 'NONE',  ( 3.687580507110999939, -82.62299735065199968, 1.957438939482999851 ) ) ;
#57704=CARTESIAN_POINT ( 'NONE',  ( 3.643490673409000014, -82.73863223182399906, -0.2401527247155999800 ) ) ;
#57714=CARTESIAN_POINT ( 'NONE',  ( 2.694001289665987287, -86.09999999999979536, -3.783547376762387060 ) ) ;
#57715=CARTESIAN_POINT ( 'NONE',  ( 3.286810233406375126, -85.82387870112127359, 1.426083493365460475 ) ) ;
#57721=CARTESIAN_POINT ( 'NONE',  ( -2.046211057035999481, -80.13706584928699783, 3.587692015901000175 ) ) ;
#57725=CARTESIAN_POINT ( 'NONE',  ( 2.782570779226999580, -80.73400264934798543, -2.195965310924000047 ) ) ;
#57750=CARTESIAN_POINT ( 'NONE',  ( 3.044567270945999660, -84.14231094026499136, 2.853188146245999590 ) ) ;
#57756=CARTESIAN_POINT ( 'NONE',  ( -3.485499217012028694, -78.91452042059381711, 6.970998434024015644 ) ) ;
#57776=CARTESIAN_POINT ( 'NONE',  ( -0.03689308533088261205, -78.91452044229970397, -3.914326904521404860 ) ) ;
#57787=CARTESIAN_POINT ( 'NONE',  ( -3.741267609786000481, -80.32205496681199008, -1.847424956918999772 ) ) ;
#57826=CARTESIAN_POINT ( 'NONE',  ( 2.588536891983000299, -84.11092953870900146, 2.425701832561999893 ) ) ;
#57850=CARTESIAN_POINT ( 'NONE',  ( 3.184161977317844894, -86.31452042059399332, -1.417680250971349754 ) ) ;
#57884=CARTESIAN_POINT ( 'NONE',  ( -3.605449341531122176, -85.88547955769999476, 1.524483932633625027 ) ) ;
#57890=CARTESIAN_POINT ( 'NONE',  ( 2.318769295210185710, -78.62148118236265759, -4.014936526035610243 ) ) ;
#57969=CARTESIAN_POINT ( 'NONE',  ( -3.863495128750999985, -86.32224116883999443, 1.091154501922000142 ) ) ;
#57996=CARTESIAN_POINT ( 'NONE',  ( -3.399818433794747019, -78.73854166371795316, -0.5489011716033136423 ) ) ;
#57999=CARTESIAN_POINT ( 'NONE',  ( 2.948777743849000377, -81.09520976391398506, -2.327247371573999857 ) ) ;
#58009=CARTESIAN_POINT ( 'NONE',  ( -3.667511737244591785, -86.36264283715696877, -2.559636160674789718 ) ) ;
#58010=CARTESIAN_POINT ( 'NONE',  ( 2.126156167813490150, -85.88434721301992170, 2.769575613414034798 ) ) ;
#58017=CARTESIAN_POINT ( 'NONE',  ( -3.959055338030000204, -80.49395764150798982, 0.1785245326323999793 ) ) ;
#58021=CARTESIAN_POINT ( 'NONE',  ( -1.193739508925000026, -81.93650264934798599, -3.337658129978000154 ) ) ;
#58042=CARTESIAN_POINT ( 'NONE',  ( 0.2897064650623000226, -84.90343479341399302, -4.120022288451000492 ) ) ;
#58070=CARTESIAN_POINT ( 'NONE',  ( -3.523652525393907720, -78.91452042059378869, -1.990986658322625669 ) ) ;
#58081=CARTESIAN_POINT ( 'NONE',  ( -4.072048464454999461, -81.76505496681200214, -0.9102108328765000644 ) ) ;
#58087=CARTESIAN_POINT ( 'NONE',  ( -3.517590690533999975, -84.74982851107797899, -0.4594732892919000111 ) ) ;
#58107=CARTESIAN_POINT ( 'NONE',  ( -1.159355627281299705, -85.90729167298438540, 3.242290418978912570 ) ) ;
#58145=CARTESIAN_POINT ( 'NONE',  ( 1.473002020459766470, -86.40321104920799655, 3.394151594327763366 ) ) ;
#58178=CARTESIAN_POINT ( 'NONE',  ( 3.751322949195259326, -86.02148118236286223, 2.724698623988329071 ) ) ;
#58183=CARTESIAN_POINT ( 'NONE',  ( 3.485499217012000273, -78.48547957940618858, -1.287490079826536515E-15 ) ) ;
#58264=CARTESIAN_POINT ( 'NONE',  ( 4.040434065196999214, -83.94574735065199889, -1.050948307445999985 ) ) ;
#58297=CARTESIAN_POINT ( 'NONE',  ( 1.764864478548999971, -80.01295594358298047, 3.316115785640000091 ) ) ;
#58309=CARTESIAN_POINT ( 'NONE',  ( -3.808769407548595165, -86.12610001270962812, -2.658222959242257044 ) ) ;
#58310=CARTESIAN_POINT ( 'NONE',  ( -3.106054822367000146, -86.10000002299598520, 1.382903988153999952 ) ) ;
#58316=CARTESIAN_POINT ( 'NONE',  ( 3.737172096265999777, -81.33571061287598525, 1.318914288780999922 ) ) ;
#58319=CARTESIAN_POINT ( 'NONE',  ( -2.717002840909000128, -78.81000264934789357, -2.276623835180000111 ) ) ;
#58341=CARTESIAN_POINT ( 'NONE',  ( -3.328554525807000175, -84.66293396287998974, -2.445248093468999961 ) ) ;
#58348=CARTESIAN_POINT ( 'NONE',  ( -3.962812355711000212, -78.85171438276199751, -1.662781298490902161E-14 ) ) ;
#58367=CARTESIAN_POINT ( 'NONE',  ( -3.962108358898298821, -78.85171438276199751, 0.07469349987780400657 ) ) ;
#58378=CARTESIAN_POINT ( 'NONE',  ( 0.5579309975780000208, -79.05050264934789084, -4.137430296115999440 ) ) ;
#58384=CARTESIAN_POINT ( 'NONE',  ( -2.858933815907000131, -84.87007892634498774, -2.100251748468999757 ) ) ;
#58401=CARTESIAN_POINT ( 'NONE',  ( -2.400545987948000004, -84.79521544543099765, 2.889418808065000288 ) ) ;
#58405=CARTESIAN_POINT ( 'NONE',  ( -3.317802080653412311, -84.63541667694400417, 0.9251688977279969306 ) ) ;
ENDSEC;
END-ISO-10303-21;
